ISO-10303-21;
HEADER;
/* Generated by software containing ST-Developer
 * from STEP Tools, Inc. (www.steptools.com) 
 */
/* OPTION: using custom renumber hook */

FILE_DESCRIPTION(
/* description */ ('STEP AP242 Edition 2', 'CAx-IF Rec.Pracs.---Representation and Presentation of Product Manufa
cturing Information (PMI)---4.0---2014-10-13', 'CAx-IF Rec.Pracs.---3D Tessellated Geometry---0.4---2014-09-14', '2;1', 'CAx-IF Rec.Pracs.---User Defined Attributes---1.5---2016-08-15'),
/* implementation_level */ '2;1');

FILE_NAME(
/* name */ 'cassette body__ DE    15749.step',
/* time_stamp */ '2026-10-09T00:23:50Z',
/* author */ (''),
/* organization */ (''),
/* preprocessor_version */ 'ST-DEVELOPER v20',
/* originating_system */ 'ONSHAPE BY PTC INC, 1.221',
/* authorisation */ '  ');

FILE_SCHEMA (('AP242_MANAGED_MODEL_BASED_3D_ENGINEERING_MIM_LF { 1 0 10303 442 3 1 4 }'));
ENDSEC;

DATA;
#143=SHAPE_REPRESENTATION_RELATIONSHIP('','',#8233,#149);
#149=ADVANCED_BREP_SHAPE_REPRESENTATION('',(#8219),#18811);
#155=B_SPLINE_CURVE_WITH_KNOTS('',3,(#11114,#11115,#11116,#11117),
 .UNSPECIFIED.,.F.,.F.,(4,4),(0.,1.),.UNSPECIFIED.);
#156=B_SPLINE_CURVE_WITH_KNOTS('',3,(#11121,#11122,#11123,#11124),
 .UNSPECIFIED.,.F.,.F.,(4,4),(0.,1.),.UNSPECIFIED.);
#157=B_SPLINE_CURVE_WITH_KNOTS('',3,(#11128,#11129,#11130,#11131),
 .UNSPECIFIED.,.F.,.F.,(4,4),(0.,1.),.UNSPECIFIED.);
#158=B_SPLINE_CURVE_WITH_KNOTS('',3,(#11135,#11136,#11137,#11138),
 .UNSPECIFIED.,.F.,.F.,(4,4),(0.,1.),.UNSPECIFIED.);
#159=B_SPLINE_CURVE_WITH_KNOTS('',3,(#11142,#11143,#11144,#11145),
 .UNSPECIFIED.,.F.,.F.,(4,4),(0.,1.),.UNSPECIFIED.);
#160=B_SPLINE_CURVE_WITH_KNOTS('',3,(#11149,#11150,#11151,#11152),
 .UNSPECIFIED.,.F.,.F.,(4,4),(0.,1.),.UNSPECIFIED.);
#161=B_SPLINE_CURVE_WITH_KNOTS('',3,(#11156,#11157,#11158,#11159),
 .UNSPECIFIED.,.F.,.F.,(4,4),(0.,1.),.UNSPECIFIED.);
#162=B_SPLINE_CURVE_WITH_KNOTS('',3,(#11163,#11164,#11165,#11166),
 .UNSPECIFIED.,.F.,.F.,(4,4),(0.,1.),.UNSPECIFIED.);
#163=B_SPLINE_CURVE_WITH_KNOTS('',3,(#11170,#11171,#11172,#11173),
 .UNSPECIFIED.,.F.,.F.,(4,4),(0.,1.),.UNSPECIFIED.);
#164=B_SPLINE_CURVE_WITH_KNOTS('',3,(#11177,#11178,#11179,#11180),
 .UNSPECIFIED.,.F.,.F.,(4,4),(0.,1.),.UNSPECIFIED.);
#165=B_SPLINE_CURVE_WITH_KNOTS('',3,(#11184,#11185,#11186,#11187),
 .UNSPECIFIED.,.F.,.F.,(4,4),(0.,1.),.UNSPECIFIED.);
#166=B_SPLINE_CURVE_WITH_KNOTS('',3,(#11191,#11192,#11193,#11194),
 .UNSPECIFIED.,.F.,.F.,(4,4),(0.,1.),.UNSPECIFIED.);
#167=B_SPLINE_CURVE_WITH_KNOTS('',3,(#11198,#11199,#11200,#11201),
 .UNSPECIFIED.,.F.,.F.,(4,4),(0.,1.),.UNSPECIFIED.);
#168=B_SPLINE_CURVE_WITH_KNOTS('',3,(#11205,#11206,#11207,#11208),
 .UNSPECIFIED.,.F.,.F.,(4,4),(0.,1.),.UNSPECIFIED.);
#169=B_SPLINE_CURVE_WITH_KNOTS('',3,(#11212,#11213,#11214,#11215),
 .UNSPECIFIED.,.F.,.F.,(4,4),(0.,1.),.UNSPECIFIED.);
#170=B_SPLINE_CURVE_WITH_KNOTS('',3,(#11219,#11220,#11221,#11222),
 .UNSPECIFIED.,.F.,.F.,(4,4),(0.,1.),.UNSPECIFIED.);
#171=B_SPLINE_CURVE_WITH_KNOTS('',3,(#11226,#11227,#11228,#11229),
 .UNSPECIFIED.,.F.,.F.,(4,4),(0.,1.),.UNSPECIFIED.);
#172=B_SPLINE_CURVE_WITH_KNOTS('',3,(#11233,#11234,#11235,#11236),
 .UNSPECIFIED.,.F.,.F.,(4,4),(0.,1.),.UNSPECIFIED.);
#173=B_SPLINE_CURVE_WITH_KNOTS('',3,(#11240,#11241,#11242,#11243),
 .UNSPECIFIED.,.F.,.F.,(4,4),(0.,1.),.UNSPECIFIED.);
#174=B_SPLINE_CURVE_WITH_KNOTS('',3,(#11247,#11248,#11249,#11250),
 .UNSPECIFIED.,.F.,.F.,(4,4),(0.,1.),.UNSPECIFIED.);
#175=B_SPLINE_CURVE_WITH_KNOTS('',3,(#11254,#11255,#11256,#11257),
 .UNSPECIFIED.,.F.,.F.,(4,4),(0.,1.),.UNSPECIFIED.);
#176=B_SPLINE_CURVE_WITH_KNOTS('',3,(#11261,#11262,#11263,#11264),
 .UNSPECIFIED.,.F.,.F.,(4,4),(0.,1.),.UNSPECIFIED.);
#177=B_SPLINE_CURVE_WITH_KNOTS('',3,(#11268,#11269,#11270,#11271),
 .UNSPECIFIED.,.F.,.F.,(4,4),(0.,1.),.UNSPECIFIED.);
#178=B_SPLINE_CURVE_WITH_KNOTS('',3,(#11275,#11276,#11277,#11278),
 .UNSPECIFIED.,.F.,.F.,(4,4),(0.,1.),.UNSPECIFIED.);
#179=B_SPLINE_CURVE_WITH_KNOTS('',3,(#11282,#11283,#11284,#11285),
 .UNSPECIFIED.,.F.,.F.,(4,4),(0.,1.),.UNSPECIFIED.);
#180=B_SPLINE_CURVE_WITH_KNOTS('',3,(#11289,#11290,#11291,#11292),
 .UNSPECIFIED.,.F.,.F.,(4,4),(0.,1.),.UNSPECIFIED.);
#181=B_SPLINE_CURVE_WITH_KNOTS('',3,(#11296,#11297,#11298,#11299),
 .UNSPECIFIED.,.F.,.F.,(4,4),(0.,1.),.UNSPECIFIED.);
#182=B_SPLINE_CURVE_WITH_KNOTS('',3,(#11303,#11304,#11305,#11306),
 .UNSPECIFIED.,.F.,.F.,(4,4),(0.,1.),.UNSPECIFIED.);
#183=B_SPLINE_CURVE_WITH_KNOTS('',3,(#11310,#11311,#11312,#11313),
 .UNSPECIFIED.,.F.,.F.,(4,4),(0.,1.),.UNSPECIFIED.);
#184=B_SPLINE_CURVE_WITH_KNOTS('',3,(#11317,#11318,#11319,#11320),
 .UNSPECIFIED.,.F.,.F.,(4,4),(0.,1.),.UNSPECIFIED.);
#185=B_SPLINE_CURVE_WITH_KNOTS('',3,(#11324,#11325,#11326,#11327),
 .UNSPECIFIED.,.F.,.F.,(4,4),(0.,1.),.UNSPECIFIED.);
#186=B_SPLINE_CURVE_WITH_KNOTS('',3,(#11331,#11332,#11333,#11334),
 .UNSPECIFIED.,.F.,.F.,(4,4),(0.,1.),.UNSPECIFIED.);
#187=B_SPLINE_CURVE_WITH_KNOTS('',3,(#11338,#11339,#11340,#11341),
 .UNSPECIFIED.,.F.,.F.,(4,4),(0.,1.),.UNSPECIFIED.);
#188=B_SPLINE_CURVE_WITH_KNOTS('',3,(#11345,#11346,#11347,#11348),
 .UNSPECIFIED.,.F.,.F.,(4,4),(0.,1.),.UNSPECIFIED.);
#189=B_SPLINE_CURVE_WITH_KNOTS('',3,(#11352,#11353,#11354,#11355),
 .UNSPECIFIED.,.F.,.F.,(4,4),(0.,1.),.UNSPECIFIED.);
#190=B_SPLINE_CURVE_WITH_KNOTS('',3,(#11359,#11360,#11361,#11362),
 .UNSPECIFIED.,.F.,.F.,(4,4),(0.,1.),.UNSPECIFIED.);
#191=B_SPLINE_CURVE_WITH_KNOTS('',3,(#11366,#11367,#11368,#11369),
 .UNSPECIFIED.,.F.,.F.,(4,4),(0.,1.),.UNSPECIFIED.);
#192=B_SPLINE_CURVE_WITH_KNOTS('',3,(#11373,#11374,#11375,#11376),
 .UNSPECIFIED.,.F.,.F.,(4,4),(0.,1.),.UNSPECIFIED.);
#193=B_SPLINE_CURVE_WITH_KNOTS('',3,(#11380,#11381,#11382,#11383),
 .UNSPECIFIED.,.F.,.F.,(4,4),(0.,1.),.UNSPECIFIED.);
#194=B_SPLINE_CURVE_WITH_KNOTS('',3,(#11387,#11388,#11389,#11390),
 .UNSPECIFIED.,.F.,.F.,(4,4),(0.,1.),.UNSPECIFIED.);
#195=B_SPLINE_CURVE_WITH_KNOTS('',3,(#11395,#11396,#11397,#11398),
 .UNSPECIFIED.,.F.,.F.,(4,4),(2.69917730509592E-7,1.),.UNSPECIFIED.);
#196=B_SPLINE_CURVE_WITH_KNOTS('',3,(#11402,#11403,#11404,#11405),
 .UNSPECIFIED.,.F.,.F.,(4,4),(2.30141280936843E-7,0.999999729513626),
 .UNSPECIFIED.);
#197=B_SPLINE_CURVE_WITH_KNOTS('',3,(#11407,#11408,#11409,#11410),
 .UNSPECIFIED.,.F.,.F.,(4,4),(0.,1.),.UNSPECIFIED.);
#198=B_SPLINE_CURVE_WITH_KNOTS('',3,(#11412,#11413,#11414,#11415),
 .UNSPECIFIED.,.F.,.F.,(4,4),(0.,1.),.UNSPECIFIED.);
#199=B_SPLINE_CURVE_WITH_KNOTS('',3,(#11417,#11418,#11419,#11420),
 .UNSPECIFIED.,.F.,.F.,(4,4),(0.,1.),.UNSPECIFIED.);
#200=B_SPLINE_CURVE_WITH_KNOTS('',3,(#11425,#11426,#11427,#11428),
 .UNSPECIFIED.,.F.,.F.,(4,4),(0.,0.999999968269152),.UNSPECIFIED.);
#201=B_SPLINE_CURVE_WITH_KNOTS('',3,(#11430,#11431,#11432,#11433),
 .UNSPECIFIED.,.F.,.F.,(4,4),(2.28432714197121E-7,1.),.UNSPECIFIED.);
#202=B_SPLINE_CURVE_WITH_KNOTS('',3,(#11434,#11435,#11436,#11437),
 .UNSPECIFIED.,.F.,.F.,(4,4),(-5.00258413789748E-10,1.),.UNSPECIFIED.);
#203=B_SPLINE_CURVE_WITH_KNOTS('',3,(#11439,#11440,#11441,#11442),
 .UNSPECIFIED.,.F.,.F.,(4,4),(0.,1.),.UNSPECIFIED.);
#204=B_SPLINE_CURVE_WITH_KNOTS('',3,(#11444,#11445,#11446,#11447),
 .UNSPECIFIED.,.F.,.F.,(4,4),(0.,1.),.UNSPECIFIED.);
#205=B_SPLINE_CURVE_WITH_KNOTS('',3,(#11449,#11450,#11451,#11452),
 .UNSPECIFIED.,.F.,.F.,(4,4),(4.98889504924982E-7,1.),.UNSPECIFIED.);
#206=B_SPLINE_CURVE_WITH_KNOTS('',3,(#11456,#11457,#11458,#11459),
 .UNSPECIFIED.,.F.,.F.,(4,4),(2.30314042019811E-7,0.999999729964527),
 .UNSPECIFIED.);
#207=B_SPLINE_CURVE_WITH_KNOTS('',3,(#11461,#11462,#11463,#11464),
 .UNSPECIFIED.,.F.,.F.,(4,4),(-4.2053902482023E-16,1.),.UNSPECIFIED.);
#208=B_SPLINE_CURVE_WITH_KNOTS('',3,(#11466,#11467,#11468,#11469),
 .UNSPECIFIED.,.F.,.F.,(4,4),(0.,1.),.UNSPECIFIED.);
#209=B_SPLINE_CURVE_WITH_KNOTS('',3,(#11471,#11472,#11473,#11474),
 .UNSPECIFIED.,.F.,.F.,(4,4),(0.,1.),.UNSPECIFIED.);
#210=B_SPLINE_CURVE_WITH_KNOTS('',3,(#11476,#11477,#11478,#11479),
 .UNSPECIFIED.,.F.,.F.,(4,4),(-1.657448313855E-10,1.),.UNSPECIFIED.);
#211=B_SPLINE_CURVE_WITH_KNOTS('',3,(#11483,#11484,#11485,#11486),
 .UNSPECIFIED.,.F.,.F.,(4,4),(0.,0.999999968338702),.UNSPECIFIED.);
#212=B_SPLINE_CURVE_WITH_KNOTS('',3,(#11488,#11489,#11490,#11491),
 .UNSPECIFIED.,.F.,.F.,(4,4),(2.29200229973547E-7,1.),.UNSPECIFIED.);
#213=B_SPLINE_CURVE_WITH_KNOTS('',3,(#11493,#11494,#11495,#11496),
 .UNSPECIFIED.,.F.,.F.,(4,4),(0.,1.),.UNSPECIFIED.);
#214=B_SPLINE_CURVE_WITH_KNOTS('',3,(#11498,#11499,#11500,#11501),
 .UNSPECIFIED.,.F.,.F.,(4,4),(0.,1.),.UNSPECIFIED.);
#215=B_SPLINE_CURVE_WITH_KNOTS('',3,(#11503,#11504,#11505,#11506),
 .UNSPECIFIED.,.F.,.F.,(4,4),(4.99050153655672E-7,1.),.UNSPECIFIED.);
#216=B_SPLINE_CURVE_WITH_KNOTS('',3,(#11510,#11511,#11512,#11513),
 .UNSPECIFIED.,.F.,.F.,(4,4),(2.31126409748052E-7,0.999999730391103),
 .UNSPECIFIED.);
#217=B_SPLINE_CURVE_WITH_KNOTS('',3,(#11515,#11516,#11517,#11518),
 .UNSPECIFIED.,.F.,.F.,(4,4),(2.10269512148046E-16,1.),.UNSPECIFIED.);
#218=B_SPLINE_CURVE_WITH_KNOTS('',3,(#11520,#11521,#11522,#11523),
 .UNSPECIFIED.,.F.,.F.,(4,4),(0.,1.),.UNSPECIFIED.);
#219=B_SPLINE_CURVE_WITH_KNOTS('',3,(#11525,#11526,#11527,#11528),
 .UNSPECIFIED.,.F.,.F.,(4,4),(0.,1.),.UNSPECIFIED.);
#220=B_SPLINE_CURVE_WITH_KNOTS('',3,(#11530,#11531,#11532,#11533),
 .UNSPECIFIED.,.F.,.F.,(4,4),(-9.6786794648492E-11,1.),.UNSPECIFIED.);
#221=B_SPLINE_CURVE_WITH_KNOTS('',3,(#11537,#11538,#11539,#11540),
 .UNSPECIFIED.,.F.,.F.,(4,4),(0.,0.999999967972051),.UNSPECIFIED.);
#222=B_SPLINE_CURVE_WITH_KNOTS('',3,(#11542,#11543,#11544,#11545),
 .UNSPECIFIED.,.F.,.F.,(4,4),(2.2911260788884E-7,1.),.UNSPECIFIED.);
#223=B_SPLINE_CURVE_WITH_KNOTS('',3,(#11547,#11548,#11549,#11550),
 .UNSPECIFIED.,.F.,.F.,(4,4),(0.,1.),.UNSPECIFIED.);
#224=B_SPLINE_CURVE_WITH_KNOTS('',3,(#11552,#11553,#11554,#11555),
 .UNSPECIFIED.,.F.,.F.,(4,4),(0.,1.),.UNSPECIFIED.);
#225=B_SPLINE_CURVE_WITH_KNOTS('',3,(#11557,#11558,#11559,#11560),
 .UNSPECIFIED.,.F.,.F.,(4,4),(4.98268763671896E-7,1.),.UNSPECIFIED.);
#226=B_SPLINE_CURVE_WITH_KNOTS('',3,(#11564,#11565,#11566,#11567),
 .UNSPECIFIED.,.F.,.F.,(4,4),(2.29530257614294E-7,0.999999730208141),
 .UNSPECIFIED.);
#227=B_SPLINE_CURVE_WITH_KNOTS('',3,(#11569,#11570,#11571,#11572),
 .UNSPECIFIED.,.F.,.F.,(4,4),(-4.20539024606654E-16,1.),.UNSPECIFIED.);
#228=B_SPLINE_CURVE_WITH_KNOTS('',3,(#11574,#11575,#11576,#11577),
 .UNSPECIFIED.,.F.,.F.,(4,4),(0.,1.),.UNSPECIFIED.);
#229=B_SPLINE_CURVE_WITH_KNOTS('',3,(#11579,#11580,#11581,#11582),
 .UNSPECIFIED.,.F.,.F.,(4,4),(0.,1.),.UNSPECIFIED.);
#230=B_SPLINE_CURVE_WITH_KNOTS('',3,(#11584,#11585,#11586,#11587),
 .UNSPECIFIED.,.F.,.F.,(4,4),(-2.43327398011773E-10,1.),.UNSPECIFIED.);
#231=B_SPLINE_CURVE_WITH_KNOTS('',3,(#11591,#11592,#11593,#11594),
 .UNSPECIFIED.,.F.,.F.,(4,4),(0.,0.999999968299911),.UNSPECIFIED.);
#232=B_SPLINE_CURVE_WITH_KNOTS('',3,(#11596,#11597,#11598,#11599),
 .UNSPECIFIED.,.F.,.F.,(4,4),(2.27426734378615E-7,1.),.UNSPECIFIED.);
#233=B_SPLINE_CURVE_WITH_KNOTS('',3,(#11601,#11602,#11603,#11604),
 .UNSPECIFIED.,.F.,.F.,(4,4),(0.,1.),.UNSPECIFIED.);
#234=B_SPLINE_CURVE_WITH_KNOTS('',3,(#11606,#11607,#11608,#11609),
 .UNSPECIFIED.,.F.,.F.,(4,4),(0.,1.),.UNSPECIFIED.);
#235=B_SPLINE_CURVE_WITH_KNOTS('',3,(#11611,#11612,#11613,#11614),
 .UNSPECIFIED.,.F.,.F.,(4,4),(4.98476028789599E-7,1.),.UNSPECIFIED.);
#236=B_SPLINE_CURVE_WITH_KNOTS('',3,(#11618,#11619,#11620,#11621),
 .UNSPECIFIED.,.F.,.F.,(4,4),(2.30300781159193E-7,0.999999730293526),
 .UNSPECIFIED.);
#237=B_SPLINE_CURVE_WITH_KNOTS('',3,(#11623,#11624,#11625,#11626),
 .UNSPECIFIED.,.F.,.F.,(4,4),(6.0851059371599E-30,1.),.UNSPECIFIED.);
#238=B_SPLINE_CURVE_WITH_KNOTS('',3,(#11628,#11629,#11630,#11631),
 .UNSPECIFIED.,.F.,.F.,(4,4),(0.,1.),.UNSPECIFIED.);
#239=B_SPLINE_CURVE_WITH_KNOTS('',3,(#11633,#11634,#11635,#11636),
 .UNSPECIFIED.,.F.,.F.,(4,4),(0.,1.),.UNSPECIFIED.);
#240=B_SPLINE_CURVE_WITH_KNOTS('',3,(#11638,#11639,#11640,#11641),
 .UNSPECIFIED.,.F.,.F.,(4,4),(-2.08522840277463E-10,1.),.UNSPECIFIED.);
#241=B_SPLINE_CURVE_WITH_KNOTS('',3,(#11645,#11646,#11647,#11648),
 .UNSPECIFIED.,.F.,.F.,(4,4),(0.,0.999999968243275),.UNSPECIFIED.);
#242=B_SPLINE_CURVE_WITH_KNOTS('',3,(#11650,#11651,#11652,#11653),
 .UNSPECIFIED.,.F.,.F.,(4,4),(2.3069334227709E-7,1.),.UNSPECIFIED.);
#243=B_SPLINE_CURVE_WITH_KNOTS('',3,(#11655,#11656,#11657,#11658),
 .UNSPECIFIED.,.F.,.F.,(4,4),(0.,1.),.UNSPECIFIED.);
#244=B_SPLINE_CURVE_WITH_KNOTS('',3,(#11660,#11661,#11662,#11663),
 .UNSPECIFIED.,.F.,.F.,(4,4),(0.,1.),.UNSPECIFIED.);
#245=B_SPLINE_CURVE_WITH_KNOTS('',3,(#11665,#11666,#11667,#11668),
 .UNSPECIFIED.,.F.,.F.,(4,4),(4.9864286811645E-7,1.),.UNSPECIFIED.);
#246=B_SPLINE_CURVE_WITH_KNOTS('',3,(#11672,#11673,#11674,#11675),
 .UNSPECIFIED.,.F.,.F.,(4,4),(2.30141256725537E-7,0.999999729718004),
 .UNSPECIFIED.);
#247=B_SPLINE_CURVE_WITH_KNOTS('',3,(#11677,#11678,#11679,#11680),
 .UNSPECIFIED.,.F.,.F.,(4,4),(0.,1.),.UNSPECIFIED.);
#248=B_SPLINE_CURVE_WITH_KNOTS('',3,(#11682,#11683,#11684,#11685),
 .UNSPECIFIED.,.F.,.F.,(4,4),(0.,1.),.UNSPECIFIED.);
#249=B_SPLINE_CURVE_WITH_KNOTS('',3,(#11687,#11688,#11689,#11690),
 .UNSPECIFIED.,.F.,.F.,(4,4),(0.,1.),.UNSPECIFIED.);
#250=B_SPLINE_CURVE_WITH_KNOTS('',3,(#11692,#11693,#11694,#11695),
 .UNSPECIFIED.,.F.,.F.,(4,4),(-5.18885638844573E-10,1.),.UNSPECIFIED.);
#251=B_SPLINE_CURVE_WITH_KNOTS('',3,(#11699,#11700,#11701,#11702),
 .UNSPECIFIED.,.F.,.F.,(4,4),(0.,0.999999968088093),.UNSPECIFIED.);
#252=B_SPLINE_CURVE_WITH_KNOTS('',3,(#11704,#11705,#11706,#11707),
 .UNSPECIFIED.,.F.,.F.,(4,4),(2.28637183361211E-7,1.),.UNSPECIFIED.);
#253=B_SPLINE_CURVE_WITH_KNOTS('',3,(#11709,#11710,#11711,#11712),
 .UNSPECIFIED.,.F.,.F.,(4,4),(0.,1.),.UNSPECIFIED.);
#254=B_SPLINE_CURVE_WITH_KNOTS('',3,(#11714,#11715,#11716,#11717),
 .UNSPECIFIED.,.F.,.F.,(4,4),(0.,1.),.UNSPECIFIED.);
#255=B_SPLINE_CURVE_WITH_KNOTS('',3,(#11719,#11720,#11721,#11722),
 .UNSPECIFIED.,.F.,.F.,(4,4),(4.98889504924982E-7,1.),.UNSPECIFIED.);
#256=B_SPLINE_CURVE_WITH_KNOTS('',3,(#11726,#11727,#11728,#11729),
 .UNSPECIFIED.,.F.,.F.,(4,4),(2.3031404033356E-7,0.999999730169011),
 .UNSPECIFIED.);
#257=B_SPLINE_CURVE_WITH_KNOTS('',3,(#11731,#11732,#11733,#11734),
 .UNSPECIFIED.,.F.,.F.,(4,4),(-4.2053902482023E-16,1.),.UNSPECIFIED.);
#258=B_SPLINE_CURVE_WITH_KNOTS('',3,(#11736,#11737,#11738,#11739),
 .UNSPECIFIED.,.F.,.F.,(4,4),(0.,1.),.UNSPECIFIED.);
#259=B_SPLINE_CURVE_WITH_KNOTS('',3,(#11741,#11742,#11743,#11744),
 .UNSPECIFIED.,.F.,.F.,(4,4),(0.,1.),.UNSPECIFIED.);
#260=B_SPLINE_CURVE_WITH_KNOTS('',3,(#11746,#11747,#11748,#11749),
 .UNSPECIFIED.,.F.,.F.,(4,4),(-4.53984320462827E-11,1.),.UNSPECIFIED.);
#261=B_SPLINE_CURVE_WITH_KNOTS('',3,(#11753,#11754,#11755,#11756),
 .UNSPECIFIED.,.F.,.F.,(4,4),(0.,0.999999968398876),.UNSPECIFIED.);
#262=B_SPLINE_CURVE_WITH_KNOTS('',3,(#11758,#11759,#11760,#11761),
 .UNSPECIFIED.,.F.,.F.,(4,4),(2.29404699546038E-7,1.),.UNSPECIFIED.);
#263=B_SPLINE_CURVE_WITH_KNOTS('',3,(#11763,#11764,#11765,#11766),
 .UNSPECIFIED.,.F.,.F.,(4,4),(0.,1.),.UNSPECIFIED.);
#264=B_SPLINE_CURVE_WITH_KNOTS('',3,(#11768,#11769,#11770,#11771),
 .UNSPECIFIED.,.F.,.F.,(4,4),(0.,1.),.UNSPECIFIED.);
#265=B_SPLINE_CURVE_WITH_KNOTS('',3,(#11773,#11774,#11775,#11776),
 .UNSPECIFIED.,.F.,.F.,(4,4),(4.99050153655672E-7,1.),.UNSPECIFIED.);
#266=B_SPLINE_CURVE_WITH_KNOTS('',3,(#11780,#11781,#11782,#11783),
 .UNSPECIFIED.,.F.,.F.,(4,4),(2.31126399320472E-7,0.999999730595559),
 .UNSPECIFIED.);
#267=B_SPLINE_CURVE_WITH_KNOTS('',3,(#11785,#11786,#11787,#11788),
 .UNSPECIFIED.,.F.,.F.,(4,4),(2.10269512148046E-16,1.),.UNSPECIFIED.);
#268=B_SPLINE_CURVE_WITH_KNOTS('',3,(#11790,#11791,#11792,#11793),
 .UNSPECIFIED.,.F.,.F.,(4,4),(0.,1.),.UNSPECIFIED.);
#269=B_SPLINE_CURVE_WITH_KNOTS('',3,(#11795,#11796,#11797,#11798),
 .UNSPECIFIED.,.F.,.F.,(4,4),(0.,1.),.UNSPECIFIED.);
#270=B_SPLINE_CURVE_WITH_KNOTS('',3,(#11800,#11801,#11802,#11803),
 .UNSPECIFIED.,.F.,.F.,(4,4),(2.35598693893978E-11,1.),.UNSPECIFIED.);
#271=B_SPLINE_CURVE_WITH_KNOTS('',3,(#11807,#11808,#11809,#11810),
 .UNSPECIFIED.,.F.,.F.,(4,4),(0.,0.999999968032225),.UNSPECIFIED.);
#272=B_SPLINE_CURVE_WITH_KNOTS('',3,(#11812,#11813,#11814,#11815),
 .UNSPECIFIED.,.F.,.F.,(4,4),(2.29317079764804E-7,1.),.UNSPECIFIED.);
#273=B_SPLINE_CURVE_WITH_KNOTS('',3,(#11817,#11818,#11819,#11820),
 .UNSPECIFIED.,.F.,.F.,(4,4),(0.,1.),.UNSPECIFIED.);
#274=B_SPLINE_CURVE_WITH_KNOTS('',3,(#11822,#11823,#11824,#11825),
 .UNSPECIFIED.,.F.,.F.,(4,4),(0.,1.),.UNSPECIFIED.);
#275=B_SPLINE_CURVE_WITH_KNOTS('',3,(#11827,#11828,#11829,#11830),
 .UNSPECIFIED.,.F.,.F.,(4,4),(4.98268763671896E-7,1.),.UNSPECIFIED.);
#276=B_SPLINE_CURVE_WITH_KNOTS('',3,(#11834,#11835,#11836,#11837),
 .UNSPECIFIED.,.F.,.F.,(4,4),(2.2953026600887E-7,0.999999729415713),
 .UNSPECIFIED.);
#277=B_SPLINE_CURVE_WITH_KNOTS('',3,(#11839,#11840,#11841,#11842),
 .UNSPECIFIED.,.F.,.F.,(4,4),(-4.20539024606654E-16,1.),.UNSPECIFIED.);
#278=B_SPLINE_CURVE_WITH_KNOTS('',3,(#11844,#11845,#11846,#11847),
 .UNSPECIFIED.,.F.,.F.,(4,4),(0.,1.),.UNSPECIFIED.);
#279=B_SPLINE_CURVE_WITH_KNOTS('',3,(#11849,#11850,#11851,#11852),
 .UNSPECIFIED.,.F.,.F.,(4,4),(0.,1.),.UNSPECIFIED.);
#280=B_SPLINE_CURVE_WITH_KNOTS('',3,(#11854,#11855,#11856,#11857),
 .UNSPECIFIED.,.F.,.F.,(4,4),(-7.09741890607156E-10,1.),.UNSPECIFIED.);
#281=B_SPLINE_CURVE_WITH_KNOTS('',3,(#11861,#11862,#11863,#11864),
 .UNSPECIFIED.,.F.,.F.,(4,4),(0.,0.999999968360085),.UNSPECIFIED.);
#282=B_SPLINE_CURVE_WITH_KNOTS('',3,(#11866,#11867,#11868,#11869),
 .UNSPECIFIED.,.F.,.F.,(4,4),(2.27631205482384E-7,1.),.UNSPECIFIED.);
#283=B_SPLINE_CURVE_WITH_KNOTS('',3,(#11871,#11872,#11873,#11874),
 .UNSPECIFIED.,.F.,.F.,(4,4),(0.,1.),.UNSPECIFIED.);
#284=B_SPLINE_CURVE_WITH_KNOTS('',3,(#11876,#11877,#11878,#11879),
 .UNSPECIFIED.,.F.,.F.,(4,4),(0.,1.),.UNSPECIFIED.);
#285=B_SPLINE_CURVE_WITH_KNOTS('',3,(#11881,#11882,#11883,#11884),
 .UNSPECIFIED.,.F.,.F.,(4,4),(4.98476028789599E-7,1.),.UNSPECIFIED.);
#286=B_SPLINE_CURVE_WITH_KNOTS('',3,(#11888,#11889,#11890,#11891),
 .UNSPECIFIED.,.F.,.F.,(4,4),(2.30300785517478E-7,0.999999730498011),
 .UNSPECIFIED.);
#287=B_SPLINE_CURVE_WITH_KNOTS('',3,(#11893,#11894,#11895,#11896),
 .UNSPECIFIED.,.F.,.F.,(4,4),(6.0851059371599E-30,1.),.UNSPECIFIED.);
#288=B_SPLINE_CURVE_WITH_KNOTS('',3,(#11898,#11899,#11900,#11901),
 .UNSPECIFIED.,.F.,.F.,(4,4),(0.,1.),.UNSPECIFIED.);
#289=B_SPLINE_CURVE_WITH_KNOTS('',3,(#11903,#11904,#11905,#11906),
 .UNSPECIFIED.,.F.,.F.,(4,4),(0.,1.),.UNSPECIFIED.);
#290=B_SPLINE_CURVE_WITH_KNOTS('',3,(#11908,#11909,#11910,#11911),
 .UNSPECIFIED.,.F.,.F.,(4,4),(-8.81759770831403E-11,1.),.UNSPECIFIED.);
#291=B_SPLINE_CURVE_WITH_KNOTS('',3,(#11915,#11916,#11917,#11918),
 .UNSPECIFIED.,.F.,.F.,(4,4),(0.,0.999999968303448),.UNSPECIFIED.);
#292=B_SPLINE_CURVE_WITH_KNOTS('',3,(#11920,#11921,#11922,#11923),
 .UNSPECIFIED.,.F.,.F.,(4,4),(2.30897813509391E-7,1.),.UNSPECIFIED.);
#293=B_SPLINE_CURVE_WITH_KNOTS('',3,(#11925,#11926,#11927,#11928),
 .UNSPECIFIED.,.F.,.F.,(4,4),(0.,1.),.UNSPECIFIED.);
#294=B_SPLINE_CURVE_WITH_KNOTS('',3,(#11930,#11931,#11932,#11933),
 .UNSPECIFIED.,.F.,.F.,(4,4),(0.,1.),.UNSPECIFIED.);
#295=B_SPLINE_CURVE_WITH_KNOTS('',3,(#11935,#11936,#11937,#11938),
 .UNSPECIFIED.,.F.,.F.,(4,4),(4.98642861198939E-7,1.),.UNSPECIFIED.);
#296=B_SPLINE_CURVE_WITH_KNOTS('',3,(#11942,#11943,#11944,#11945),
 .UNSPECIFIED.,.F.,.F.,(4,4),(2.30141277478068E-7,0.999999730101521),
 .UNSPECIFIED.);
#297=B_SPLINE_CURVE_WITH_KNOTS('',3,(#11947,#11948,#11949,#11950),
 .UNSPECIFIED.,.F.,.F.,(4,4),(0.,1.),.UNSPECIFIED.);
#298=B_SPLINE_CURVE_WITH_KNOTS('',3,(#11952,#11953,#11954,#11955),
 .UNSPECIFIED.,.F.,.F.,(4,4),(0.,1.),.UNSPECIFIED.);
#299=B_SPLINE_CURVE_WITH_KNOTS('',3,(#11957,#11958,#11959,#11960),
 .UNSPECIFIED.,.F.,.F.,(4,4),(0.,1.),.UNSPECIFIED.);
#300=B_SPLINE_CURVE_WITH_KNOTS('',3,(#11962,#11963,#11964,#11965),
 .UNSPECIFIED.,.F.,.F.,(4,4),(-3.27223686180977E-10,1.),.UNSPECIFIED.);
#301=B_SPLINE_CURVE_WITH_KNOTS('',3,(#11969,#11970,#11971,#11972),
 .UNSPECIFIED.,.F.,.F.,(4,4),(0.,0.999999968200953),.UNSPECIFIED.);
#302=B_SPLINE_CURVE_WITH_KNOTS('',3,(#11974,#11975,#11976,#11977),
 .UNSPECIFIED.,.F.,.F.,(4,4),(2.2802376939114E-7,1.),.UNSPECIFIED.);
#303=B_SPLINE_CURVE_WITH_KNOTS('',3,(#11979,#11980,#11981,#11982),
 .UNSPECIFIED.,.F.,.F.,(4,4),(0.,1.),.UNSPECIFIED.);
#304=B_SPLINE_CURVE_WITH_KNOTS('',3,(#11984,#11985,#11986,#11987),
 .UNSPECIFIED.,.F.,.F.,(4,4),(0.,1.),.UNSPECIFIED.);
#305=B_SPLINE_CURVE_WITH_KNOTS('',3,(#11989,#11990,#11991,#11992),
 .UNSPECIFIED.,.F.,.F.,(4,4),(4.98889504924982E-7,1.),.UNSPECIFIED.);
#306=B_SPLINE_CURVE_WITH_KNOTS('',3,(#11996,#11997,#11998,#11999),
 .UNSPECIFIED.,.F.,.F.,(4,4),(2.30314046378096E-7,0.99999972955559),
 .UNSPECIFIED.);
#307=B_SPLINE_CURVE_WITH_KNOTS('',3,(#12001,#12002,#12003,#12004),
 .UNSPECIFIED.,.F.,.F.,(4,4),(-4.2053902482023E-16,1.),.UNSPECIFIED.);
#308=B_SPLINE_CURVE_WITH_KNOTS('',3,(#12006,#12007,#12008,#12009),
 .UNSPECIFIED.,.F.,.F.,(4,4),(0.,1.),.UNSPECIFIED.);
#309=B_SPLINE_CURVE_WITH_KNOTS('',3,(#12011,#12012,#12013,#12014),
 .UNSPECIFIED.,.F.,.F.,(4,4),(0.,1.),.UNSPECIFIED.);
#310=B_SPLINE_CURVE_WITH_KNOTS('',3,(#12016,#12017,#12018,#12019),
 .UNSPECIFIED.,.F.,.F.,(4,4),(-4.06438355921804E-10,1.),.UNSPECIFIED.);
#311=B_SPLINE_CURVE_WITH_KNOTS('',3,(#12023,#12024,#12025,#12026),
 .UNSPECIFIED.,.F.,.F.,(4,4),(0.,0.999999968218356),.UNSPECIFIED.);
#312=B_SPLINE_CURVE_WITH_KNOTS('',3,(#12028,#12029,#12030,#12031),
 .UNSPECIFIED.,.F.,.F.,(4,4),(2.29788204199464E-7,1.),.UNSPECIFIED.);
#313=B_SPLINE_CURVE_WITH_KNOTS('',3,(#12033,#12034,#12035,#12036),
 .UNSPECIFIED.,.F.,.F.,(4,4),(0.,1.),.UNSPECIFIED.);
#314=B_SPLINE_CURVE_WITH_KNOTS('',3,(#12038,#12039,#12040,#12041),
 .UNSPECIFIED.,.F.,.F.,(4,4),(0.,1.),.UNSPECIFIED.);
#315=B_SPLINE_CURVE_WITH_KNOTS('',3,(#12043,#12044,#12045,#12046),
 .UNSPECIFIED.,.F.,.F.,(4,4),(4.99050153655672E-7,1.),.UNSPECIFIED.);
#316=B_SPLINE_CURVE_WITH_KNOTS('',3,(#12050,#12051,#12052,#12053),
 .UNSPECIFIED.,.F.,.F.,(4,4),(2.3112639881784E-7,0.999999730979069),
 .UNSPECIFIED.);
#317=B_SPLINE_CURVE_WITH_KNOTS('',3,(#12055,#12056,#12057,#12058),
 .UNSPECIFIED.,.F.,.F.,(4,4),(2.10269512148046E-16,1.),.UNSPECIFIED.);
#318=B_SPLINE_CURVE_WITH_KNOTS('',3,(#12060,#12061,#12062,#12063),
 .UNSPECIFIED.,.F.,.F.,(4,4),(0.,1.),.UNSPECIFIED.);
#319=B_SPLINE_CURVE_WITH_KNOTS('',3,(#12065,#12066,#12067,#12068),
 .UNSPECIFIED.,.F.,.F.,(4,4),(0.,1.),.UNSPECIFIED.);
#320=B_SPLINE_CURVE_WITH_KNOTS('',3,(#12070,#12071,#12072,#12073),
 .UNSPECIFIED.,.F.,.F.,(4,4),(2.49280919609535E-10,1.),.UNSPECIFIED.);
#321=B_SPLINE_CURVE_WITH_KNOTS('',3,(#12077,#12078,#12079,#12080),
 .UNSPECIFIED.,.F.,.F.,(4,4),(0.,0.999999968145085),.UNSPECIFIED.);
#322=B_SPLINE_CURVE_WITH_KNOTS('',3,(#12082,#12083,#12084,#12085),
 .UNSPECIFIED.,.F.,.F.,(4,4),(2.29700583941174E-7,1.),.UNSPECIFIED.);
#323=B_SPLINE_CURVE_WITH_KNOTS('',3,(#12087,#12088,#12089,#12090),
 .UNSPECIFIED.,.F.,.F.,(4,4),(0.,1.),.UNSPECIFIED.);
#324=B_SPLINE_CURVE_WITH_KNOTS('',3,(#12092,#12093,#12094,#12095),
 .UNSPECIFIED.,.F.,.F.,(4,4),(0.,1.),.UNSPECIFIED.);
#325=B_SPLINE_CURVE_WITH_KNOTS('',3,(#12097,#12098,#12099,#12100),
 .UNSPECIFIED.,.F.,.F.,(4,4),(4.98268763671896E-7,1.),.UNSPECIFIED.);
#326=B_SPLINE_CURVE_WITH_KNOTS('',3,(#12104,#12105,#12106,#12107),
 .UNSPECIFIED.,.F.,.F.,(4,4),(2.29530277201637E-7,0.999999729799226),
 .UNSPECIFIED.);
#327=B_SPLINE_CURVE_WITH_KNOTS('',3,(#12109,#12110,#12111,#12112),
 .UNSPECIFIED.,.F.,.F.,(4,4),(-4.20539024606654E-16,1.),.UNSPECIFIED.);
#328=B_SPLINE_CURVE_WITH_KNOTS('',3,(#12114,#12115,#12116,#12117),
 .UNSPECIFIED.,.F.,.F.,(4,4),(0.,1.),.UNSPECIFIED.);
#329=B_SPLINE_CURVE_WITH_KNOTS('',3,(#12119,#12120,#12121,#12122),
 .UNSPECIFIED.,.F.,.F.,(4,4),(0.,1.),.UNSPECIFIED.);
#330=B_SPLINE_CURVE_WITH_KNOTS('',3,(#12124,#12125,#12126,#12127),
 .UNSPECIFIED.,.F.,.F.,(4,4),(-4.84020982613384E-10,1.),.UNSPECIFIED.);
#331=B_SPLINE_CURVE_WITH_KNOTS('',3,(#12131,#12132,#12133,#12134),
 .UNSPECIFIED.,.F.,.F.,(4,4),(0.,0.999999968179565),.UNSPECIFIED.);
#332=B_SPLINE_CURVE_WITH_KNOTS('',3,(#12136,#12137,#12138,#12139),
 .UNSPECIFIED.,.F.,.F.,(4,4),(2.27017792871544E-7,1.),.UNSPECIFIED.);
#333=B_SPLINE_CURVE_WITH_KNOTS('',3,(#12141,#12142,#12143,#12144),
 .UNSPECIFIED.,.F.,.F.,(4,4),(0.,1.),.UNSPECIFIED.);
#334=B_SPLINE_CURVE_WITH_KNOTS('',3,(#12146,#12147,#12148,#12149),
 .UNSPECIFIED.,.F.,.F.,(4,4),(0.,1.),.UNSPECIFIED.);
#335=B_SPLINE_CURVE_WITH_KNOTS('',3,(#12151,#12152,#12153,#12154),
 .UNSPECIFIED.,.F.,.F.,(4,4),(4.98476028789599E-7,1.),.UNSPECIFIED.);
#336=B_SPLINE_CURVE_WITH_KNOTS('',3,(#12158,#12159,#12160,#12161),
 .UNSPECIFIED.,.F.,.F.,(4,4),(2.30300766849461E-7,0.999999729884583),
 .UNSPECIFIED.);
#337=B_SPLINE_CURVE_WITH_KNOTS('',3,(#12163,#12164,#12165,#12166),
 .UNSPECIFIED.,.F.,.F.,(4,4),(6.0851059371599E-30,1.),.UNSPECIFIED.);
#338=B_SPLINE_CURVE_WITH_KNOTS('',3,(#12168,#12169,#12170,#12171),
 .UNSPECIFIED.,.F.,.F.,(4,4),(0.,1.),.UNSPECIFIED.);
#339=B_SPLINE_CURVE_WITH_KNOTS('',3,(#12173,#12174,#12175,#12176),
 .UNSPECIFIED.,.F.,.F.,(4,4),(0.,1.),.UNSPECIFIED.);
#340=B_SPLINE_CURVE_WITH_KNOTS('',3,(#12178,#12179,#12180,#12181),
 .UNSPECIFIED.,.F.,.F.,(4,4),(-4.49216403355802E-10,1.),.UNSPECIFIED.);
#341=B_SPLINE_CURVE_WITH_KNOTS('',3,(#12185,#12186,#12187,#12188),
 .UNSPECIFIED.,.F.,.F.,(4,4),(0.,0.999999968416308),.UNSPECIFIED.);
#342=B_SPLINE_CURVE_WITH_KNOTS('',3,(#12190,#12191,#12192,#12193),
 .UNSPECIFIED.,.F.,.F.,(4,4),(2.31281316829358E-7,1.),.UNSPECIFIED.);
#343=B_SPLINE_CURVE_WITH_KNOTS('',3,(#12195,#12196,#12197,#12198),
 .UNSPECIFIED.,.F.,.F.,(4,4),(0.,1.),.UNSPECIFIED.);
#344=B_SPLINE_CURVE_WITH_KNOTS('',3,(#12200,#12201,#12202,#12203),
 .UNSPECIFIED.,.F.,.F.,(4,4),(0.,1.),.UNSPECIFIED.);
#345=B_SPLINE_CURVE_WITH_KNOTS('',3,(#12205,#12206,#12207,#12208),
 .UNSPECIFIED.,.F.,.F.,(4,4),(4.98642861198939E-7,1.),.UNSPECIFIED.);
#346=B_SPLINE_CURVE_WITH_KNOTS('',3,(#12212,#12213,#12214,#12215),
 .UNSPECIFIED.,.F.,.F.,(4,4),(2.30141291313089E-7,0.99999973030602),
 .UNSPECIFIED.);
#347=B_SPLINE_CURVE_WITH_KNOTS('',3,(#12217,#12218,#12219,#12220),
 .UNSPECIFIED.,.F.,.F.,(4,4),(0.,1.),.UNSPECIFIED.);
#348=B_SPLINE_CURVE_WITH_KNOTS('',3,(#12222,#12223,#12224,#12225),
 .UNSPECIFIED.,.F.,.F.,(4,4),(0.,1.),.UNSPECIFIED.);
#349=B_SPLINE_CURVE_WITH_KNOTS('',3,(#12227,#12228,#12229,#12230),
 .UNSPECIFIED.,.F.,.F.,(4,4),(0.,1.),.UNSPECIFIED.);
#350=B_SPLINE_CURVE_WITH_KNOTS('',3,(#12232,#12233,#12234,#12235),
 .UNSPECIFIED.,.F.,.F.,(4,4),(-1.72817946408447E-10,1.),.UNSPECIFIED.);
#351=B_SPLINE_CURVE_WITH_KNOTS('',3,(#12239,#12240,#12241,#12242),
 .UNSPECIFIED.,.F.,.F.,(4,4),(0.,0.999999968261127),.UNSPECIFIED.);
#352=B_SPLINE_CURVE_WITH_KNOTS('',3,(#12244,#12245,#12246,#12247),
 .UNSPECIFIED.,.F.,.F.,(4,4),(2.28228239255696E-7,1.),.UNSPECIFIED.);
#353=B_SPLINE_CURVE_WITH_KNOTS('',3,(#12249,#12250,#12251,#12252),
 .UNSPECIFIED.,.F.,.F.,(4,4),(0.,1.),.UNSPECIFIED.);
#354=B_SPLINE_CURVE_WITH_KNOTS('',3,(#12254,#12255,#12256,#12257),
 .UNSPECIFIED.,.F.,.F.,(4,4),(0.,1.),.UNSPECIFIED.);
#355=B_SPLINE_CURVE_WITH_KNOTS('',3,(#12259,#12260,#12261,#12262),
 .UNSPECIFIED.,.F.,.F.,(4,4),(4.98889504924982E-7,1.),.UNSPECIFIED.);
#356=B_SPLINE_CURVE_WITH_KNOTS('',3,(#12266,#12267,#12268,#12269),
 .UNSPECIFIED.,.F.,.F.,(4,4),(2.30314020679759E-7,0.999999729760012),
 .UNSPECIFIED.);
#357=B_SPLINE_CURVE_WITH_KNOTS('',3,(#12271,#12272,#12273,#12274),
 .UNSPECIFIED.,.F.,.F.,(4,4),(-4.2053902482023E-16,1.),.UNSPECIFIED.);
#358=B_SPLINE_CURVE_WITH_KNOTS('',3,(#12276,#12277,#12278,#12279),
 .UNSPECIFIED.,.F.,.F.,(4,4),(0.,1.),.UNSPECIFIED.);
#359=B_SPLINE_CURVE_WITH_KNOTS('',3,(#12281,#12282,#12283,#12284),
 .UNSPECIFIED.,.F.,.F.,(4,4),(0.,1.),.UNSPECIFIED.);
#360=B_SPLINE_CURVE_WITH_KNOTS('',3,(#12286,#12287,#12288,#12289),
 .UNSPECIFIED.,.F.,.F.,(4,4),(-2.86092757243134E-10,1.),.UNSPECIFIED.);
#361=B_SPLINE_CURVE_WITH_KNOTS('',3,(#12293,#12294,#12295,#12296),
 .UNSPECIFIED.,.F.,.F.,(4,4),(0.,0.999999968278529),.UNSPECIFIED.);
#362=B_SPLINE_CURVE_WITH_KNOTS('',3,(#12298,#12299,#12300,#12301),
 .UNSPECIFIED.,.F.,.F.,(4,4),(2.28995756837677E-7,1.),.UNSPECIFIED.);
#363=B_SPLINE_CURVE_WITH_KNOTS('',3,(#12303,#12304,#12305,#12306),
 .UNSPECIFIED.,.F.,.F.,(4,4),(0.,1.),.UNSPECIFIED.);
#364=B_SPLINE_CURVE_WITH_KNOTS('',3,(#12308,#12309,#12310,#12311),
 .UNSPECIFIED.,.F.,.F.,(4,4),(0.,1.),.UNSPECIFIED.);
#365=B_SPLINE_CURVE_WITH_KNOTS('',3,(#12313,#12314,#12315,#12316),
 .UNSPECIFIED.,.F.,.F.,(4,4),(4.99050153655672E-7,1.),.UNSPECIFIED.);
#366=B_SPLINE_CURVE_WITH_KNOTS('',3,(#12320,#12321,#12322,#12323),
 .UNSPECIFIED.,.F.,.F.,(4,4),(2.31126418142628E-7,0.999999730186638),
 .UNSPECIFIED.);
#367=B_SPLINE_CURVE_WITH_KNOTS('',3,(#12325,#12326,#12327,#12328),
 .UNSPECIFIED.,.F.,.F.,(4,4),(2.10269512148046E-16,1.),.UNSPECIFIED.);
#368=B_SPLINE_CURVE_WITH_KNOTS('',3,(#12330,#12331,#12332,#12333),
 .UNSPECIFIED.,.F.,.F.,(4,4),(0.,1.),.UNSPECIFIED.);
#369=B_SPLINE_CURVE_WITH_KNOTS('',3,(#12335,#12336,#12337,#12338),
 .UNSPECIFIED.,.F.,.F.,(4,4),(0.,1.),.UNSPECIFIED.);
#370=B_SPLINE_CURVE_WITH_KNOTS('',3,(#12340,#12341,#12342,#12343),
 .UNSPECIFIED.,.F.,.F.,(4,4),(-2.17133087511602E-10,1.),.UNSPECIFIED.);
#371=B_SPLINE_CURVE_WITH_KNOTS('',3,(#12347,#12348,#12349,#12350),
 .UNSPECIFIED.,.F.,.F.,(4,4),(0.,0.999999968205259),.UNSPECIFIED.);
#372=B_SPLINE_CURVE_WITH_KNOTS('',3,(#12352,#12353,#12354,#12355),
 .UNSPECIFIED.,.F.,.F.,(4,4),(2.29905056582326E-7,1.),.UNSPECIFIED.);
#373=B_SPLINE_CURVE_WITH_KNOTS('',3,(#12357,#12358,#12359,#12360),
 .UNSPECIFIED.,.F.,.F.,(4,4),(0.,1.),.UNSPECIFIED.);
#374=B_SPLINE_CURVE_WITH_KNOTS('',3,(#12362,#12363,#12364,#12365),
 .UNSPECIFIED.,.F.,.F.,(4,4),(0.,1.),.UNSPECIFIED.);
#375=B_SPLINE_CURVE_WITH_KNOTS('',3,(#12367,#12368,#12369,#12370),
 .UNSPECIFIED.,.F.,.F.,(4,4),(4.98268763671896E-7,1.),.UNSPECIFIED.);
#376=B_SPLINE_CURVE_WITH_KNOTS('',3,(#12374,#12375,#12376,#12377),
 .UNSPECIFIED.,.F.,.F.,(4,4),(2.29530257876848E-7,0.99999973000367),
 .UNSPECIFIED.);
#377=B_SPLINE_CURVE_WITH_KNOTS('',3,(#12379,#12380,#12381,#12382),
 .UNSPECIFIED.,.F.,.F.,(4,4),(-4.20539024606654E-16,1.),.UNSPECIFIED.);
#378=B_SPLINE_CURVE_WITH_KNOTS('',3,(#12384,#12385,#12386,#12387),
 .UNSPECIFIED.,.F.,.F.,(4,4),(0.,1.),.UNSPECIFIED.);
#379=B_SPLINE_CURVE_WITH_KNOTS('',3,(#12389,#12390,#12391,#12392),
 .UNSPECIFIED.,.F.,.F.,(4,4),(0.,1.),.UNSPECIFIED.);
#380=B_SPLINE_CURVE_WITH_KNOTS('',3,(#12394,#12395,#12396,#12397),
 .UNSPECIFIED.,.F.,.F.,(4,4),(-3.63673936213342E-10,1.),.UNSPECIFIED.);
#381=B_SPLINE_CURVE_WITH_KNOTS('',3,(#12401,#12402,#12403,#12404),
 .UNSPECIFIED.,.F.,.F.,(4,4),(0.,0.999999968239738),.UNSPECIFIED.);
#382=B_SPLINE_CURVE_WITH_KNOTS('',3,(#12406,#12407,#12408,#12409),
 .UNSPECIFIED.,.F.,.F.,(4,4),(2.27222261671625E-7,1.),.UNSPECIFIED.);
#383=B_SPLINE_CURVE_WITH_KNOTS('',3,(#12411,#12412,#12413,#12414),
 .UNSPECIFIED.,.F.,.F.,(4,4),(0.,1.),.UNSPECIFIED.);
#384=B_SPLINE_CURVE_WITH_KNOTS('',3,(#12416,#12417,#12418,#12419),
 .UNSPECIFIED.,.F.,.F.,(4,4),(0.,1.),.UNSPECIFIED.);
#385=B_SPLINE_CURVE_WITH_KNOTS('',3,(#12421,#12422,#12423,#12424),
 .UNSPECIFIED.,.F.,.F.,(4,4),(4.98476028789599E-7,1.),.UNSPECIFIED.);
#386=B_SPLINE_CURVE_WITH_KNOTS('',3,(#12428,#12429,#12430,#12431),
 .UNSPECIFIED.,.F.,.F.,(4,4),(2.30300789875764E-7,0.999999730089088),
 .UNSPECIFIED.);
#387=B_SPLINE_CURVE_WITH_KNOTS('',3,(#12433,#12434,#12435,#12436),
 .UNSPECIFIED.,.F.,.F.,(4,4),(6.0851059371599E-30,1.),.UNSPECIFIED.);
#388=B_SPLINE_CURVE_WITH_KNOTS('',3,(#12438,#12439,#12440,#12441),
 .UNSPECIFIED.,.F.,.F.,(4,4),(0.,1.),.UNSPECIFIED.);
#389=B_SPLINE_CURVE_WITH_KNOTS('',3,(#12443,#12444,#12445,#12446),
 .UNSPECIFIED.,.F.,.F.,(4,4),(0.,1.),.UNSPECIFIED.);
#390=B_SPLINE_CURVE_WITH_KNOTS('',3,(#12448,#12449,#12450,#12451),
 .UNSPECIFIED.,.F.,.F.,(4,4),(-3.28868497233371E-10,1.),.UNSPECIFIED.);
#391=B_SPLINE_CURVE_WITH_KNOTS('',3,(#12455,#12456,#12457,#12458),
 .UNSPECIFIED.,.F.,.F.,(4,4),(0.,0.999999968183101),.UNSPECIFIED.);
#392=B_SPLINE_CURVE_WITH_KNOTS('',3,(#12460,#12461,#12462,#12463),
 .UNSPECIFIED.,.F.,.F.,(4,4),(2.30488871044787E-7,1.),.UNSPECIFIED.);
#393=B_SPLINE_CURVE_WITH_KNOTS('',3,(#12465,#12466,#12467,#12468),
 .UNSPECIFIED.,.F.,.F.,(4,4),(0.,1.),.UNSPECIFIED.);
#394=B_SPLINE_CURVE_WITH_KNOTS('',3,(#12470,#12471,#12472,#12473),
 .UNSPECIFIED.,.F.,.F.,(4,4),(0.,0.999999996212121),.UNSPECIFIED.);
#395=B_SPLINE_CURVE_WITH_KNOTS('',3,(#12480,#12481,#12482,#12483),
 .UNSPECIFIED.,.F.,.F.,(4,4),(1.24500014464512E-7,0.999999750000014),
 .UNSPECIFIED.);
#396=B_SPLINE_CURVE_WITH_KNOTS('',3,(#12485,#12486,#12487,#12488),
 .UNSPECIFIED.,.F.,.F.,(4,4),(1.6055290347619E-11,1.),.UNSPECIFIED.);
#397=B_SPLINE_CURVE_WITH_KNOTS('',3,(#12490,#12491,#12492,#12493),
 .UNSPECIFIED.,.F.,.F.,(4,4),(-1.38777878078144E-14,0.999999999999986),
 .UNSPECIFIED.);
#398=B_SPLINE_CURVE_WITH_KNOTS('',3,(#12495,#12496,#12497,#12498),
 .UNSPECIFIED.,.F.,.F.,(4,4),(0.,0.999999945331273),.UNSPECIFIED.);
#399=B_SPLINE_CURVE_WITH_KNOTS('',3,(#12500,#12501,#12502,#12503),
 .UNSPECIFIED.,.F.,.F.,(4,4),(1.24500014464512E-7,0.999999750000014),
 .UNSPECIFIED.);
#400=B_SPLINE_CURVE_WITH_KNOTS('',3,(#12507,#12508,#12509,#12510),
 .UNSPECIFIED.,.F.,.F.,(4,4),(0.,1.),.UNSPECIFIED.);
#401=B_SPLINE_CURVE_WITH_KNOTS('',3,(#12511,#12512,#12513,#12514),
 .UNSPECIFIED.,.F.,.F.,(4,4),(0.,1.),.UNSPECIFIED.);
#402=B_SPLINE_CURVE_WITH_KNOTS('',3,(#12518,#12519,#12520,#12521),
 .UNSPECIFIED.,.F.,.F.,(4,4),(0.,1.),.UNSPECIFIED.);
#403=B_SPLINE_CURVE_WITH_KNOTS('',3,(#12522,#12523,#12524,#12525),
 .UNSPECIFIED.,.F.,.F.,(4,4),(0.,1.),.UNSPECIFIED.);
#404=B_SPLINE_CURVE_WITH_KNOTS('',3,(#12529,#12530,#12531,#12532),
 .UNSPECIFIED.,.F.,.F.,(4,4),(0.,1.),.UNSPECIFIED.);
#405=B_SPLINE_CURVE_WITH_KNOTS('',3,(#12533,#12534,#12535,#12536),
 .UNSPECIFIED.,.F.,.F.,(4,4),(0.,1.),.UNSPECIFIED.);
#406=B_SPLINE_CURVE_WITH_KNOTS('',3,(#12540,#12541,#12542,#12543),
 .UNSPECIFIED.,.F.,.F.,(4,4),(0.,1.),.UNSPECIFIED.);
#407=B_SPLINE_CURVE_WITH_KNOTS('',3,(#12544,#12545,#12546,#12547),
 .UNSPECIFIED.,.F.,.F.,(4,4),(0.,1.),.UNSPECIFIED.);
#408=B_SPLINE_CURVE_WITH_KNOTS('',3,(#12551,#12552,#12553,#12554),
 .UNSPECIFIED.,.F.,.F.,(4,4),(0.,1.),.UNSPECIFIED.);
#409=B_SPLINE_CURVE_WITH_KNOTS('',3,(#12555,#12556,#12557,#12558),
 .UNSPECIFIED.,.F.,.F.,(4,4),(0.,1.),.UNSPECIFIED.);
#410=B_SPLINE_CURVE_WITH_KNOTS('',3,(#12562,#12563,#12564,#12565),
 .UNSPECIFIED.,.F.,.F.,(4,4),(0.,1.),.UNSPECIFIED.);
#411=B_SPLINE_CURVE_WITH_KNOTS('',3,(#12566,#12567,#12568,#12569),
 .UNSPECIFIED.,.F.,.F.,(4,4),(0.,1.),.UNSPECIFIED.);
#412=B_SPLINE_CURVE_WITH_KNOTS('',3,(#12573,#12574,#12575,#12576),
 .UNSPECIFIED.,.F.,.F.,(4,4),(0.,1.),.UNSPECIFIED.);
#413=B_SPLINE_CURVE_WITH_KNOTS('',3,(#12577,#12578,#12579,#12580),
 .UNSPECIFIED.,.F.,.F.,(4,4),(0.,1.),.UNSPECIFIED.);
#414=B_SPLINE_CURVE_WITH_KNOTS('',3,(#12584,#12585,#12586,#12587),
 .UNSPECIFIED.,.F.,.F.,(4,4),(0.,1.),.UNSPECIFIED.);
#415=B_SPLINE_CURVE_WITH_KNOTS('',3,(#12588,#12589,#12590,#12591),
 .UNSPECIFIED.,.F.,.F.,(4,4),(0.,1.),.UNSPECIFIED.);
#416=B_SPLINE_CURVE_WITH_KNOTS('',3,(#12595,#12596,#12597,#12598),
 .UNSPECIFIED.,.F.,.F.,(4,4),(0.,1.),.UNSPECIFIED.);
#417=B_SPLINE_CURVE_WITH_KNOTS('',3,(#12599,#12600,#12601,#12602),
 .UNSPECIFIED.,.F.,.F.,(4,4),(0.,1.),.UNSPECIFIED.);
#418=B_SPLINE_CURVE_WITH_KNOTS('',3,(#12607,#12608,#12609,#12610),
 .UNSPECIFIED.,.F.,.F.,(4,4),(0.,1.),.UNSPECIFIED.);
#419=B_SPLINE_CURVE_WITH_KNOTS('',3,(#12611,#12612,#12613,#12614),
 .UNSPECIFIED.,.F.,.F.,(4,4),(0.,1.),.UNSPECIFIED.);
#420=B_SPLINE_CURVE_WITH_KNOTS('',3,(#12618,#12619,#12620,#12621),
 .UNSPECIFIED.,.F.,.F.,(4,4),(0.,1.),.UNSPECIFIED.);
#421=B_SPLINE_CURVE_WITH_KNOTS('',3,(#12622,#12623,#12624,#12625),
 .UNSPECIFIED.,.F.,.F.,(4,4),(0.,1.),.UNSPECIFIED.);
#422=B_SPLINE_CURVE_WITH_KNOTS('',3,(#12629,#12630,#12631,#12632),
 .UNSPECIFIED.,.F.,.F.,(4,4),(0.,1.),.UNSPECIFIED.);
#423=B_SPLINE_CURVE_WITH_KNOTS('',3,(#12633,#12634,#12635,#12636),
 .UNSPECIFIED.,.F.,.F.,(4,4),(0.,1.),.UNSPECIFIED.);
#424=B_SPLINE_CURVE_WITH_KNOTS('',3,(#12640,#12641,#12642,#12643),
 .UNSPECIFIED.,.F.,.F.,(4,4),(0.,1.),.UNSPECIFIED.);
#425=B_SPLINE_CURVE_WITH_KNOTS('',3,(#12644,#12645,#12646,#12647),
 .UNSPECIFIED.,.F.,.F.,(4,4),(0.,1.),.UNSPECIFIED.);
#426=B_SPLINE_CURVE_WITH_KNOTS('',3,(#12651,#12652,#12653,#12654),
 .UNSPECIFIED.,.F.,.F.,(4,4),(0.,1.),.UNSPECIFIED.);
#427=B_SPLINE_CURVE_WITH_KNOTS('',3,(#12655,#12656,#12657,#12658),
 .UNSPECIFIED.,.F.,.F.,(4,4),(0.,1.),.UNSPECIFIED.);
#428=B_SPLINE_CURVE_WITH_KNOTS('',3,(#12662,#12663,#12664,#12665),
 .UNSPECIFIED.,.F.,.F.,(4,4),(0.,1.),.UNSPECIFIED.);
#429=B_SPLINE_CURVE_WITH_KNOTS('',3,(#12666,#12667,#12668,#12669),
 .UNSPECIFIED.,.F.,.F.,(4,4),(0.,1.),.UNSPECIFIED.);
#430=B_SPLINE_CURVE_WITH_KNOTS('',3,(#12673,#12674,#12675,#12676),
 .UNSPECIFIED.,.F.,.F.,(4,4),(0.,1.),.UNSPECIFIED.);
#431=B_SPLINE_CURVE_WITH_KNOTS('',3,(#12677,#12678,#12679,#12680),
 .UNSPECIFIED.,.F.,.F.,(4,4),(0.,1.),.UNSPECIFIED.);
#432=B_SPLINE_CURVE_WITH_KNOTS('',3,(#12684,#12685,#12686,#12687),
 .UNSPECIFIED.,.F.,.F.,(4,4),(0.,1.),.UNSPECIFIED.);
#433=B_SPLINE_CURVE_WITH_KNOTS('',3,(#12688,#12689,#12690,#12691),
 .UNSPECIFIED.,.F.,.F.,(4,4),(0.,1.),.UNSPECIFIED.);
#434=B_SPLINE_CURVE_WITH_KNOTS('',3,(#12695,#12696,#12697,#12698),
 .UNSPECIFIED.,.F.,.F.,(4,4),(0.,1.),.UNSPECIFIED.);
#435=B_SPLINE_CURVE_WITH_KNOTS('',3,(#12699,#12700,#12701,#12702),
 .UNSPECIFIED.,.F.,.F.,(4,4),(0.,1.),.UNSPECIFIED.);
#436=B_SPLINE_CURVE_WITH_KNOTS('',3,(#12706,#12707,#12708,#12709),
 .UNSPECIFIED.,.F.,.F.,(4,4),(0.,1.),.UNSPECIFIED.);
#437=B_SPLINE_CURVE_WITH_KNOTS('',3,(#12715,#12716,#12717,#12718),
 .UNSPECIFIED.,.F.,.F.,(4,4),(0.,1.),.UNSPECIFIED.);
#438=B_SPLINE_CURVE_WITH_KNOTS('',3,(#12720,#12721,#12722,#12723),
 .UNSPECIFIED.,.F.,.F.,(4,4),(0.,1.),.UNSPECIFIED.);
#439=B_SPLINE_CURVE_WITH_KNOTS('',3,(#12727,#12728,#12729,#12730),
 .UNSPECIFIED.,.F.,.F.,(4,4),(0.,1.),.UNSPECIFIED.);
#440=B_SPLINE_CURVE_WITH_KNOTS('',3,(#12732,#12733,#12734,#12735),
 .UNSPECIFIED.,.F.,.F.,(4,4),(0.,0.999999999884541),.UNSPECIFIED.);
#441=B_SPLINE_CURVE_WITH_KNOTS('',3,(#12739,#12740,#12741,#12742),
 .UNSPECIFIED.,.F.,.F.,(4,4),(0.,1.),.UNSPECIFIED.);
#442=B_SPLINE_CURVE_WITH_KNOTS('',3,(#12744,#12745,#12746,#12747),
 .UNSPECIFIED.,.F.,.F.,(4,4),(0.,1.),.UNSPECIFIED.);
#443=B_SPLINE_CURVE_WITH_KNOTS('',3,(#12751,#12752,#12753,#12754),
 .UNSPECIFIED.,.F.,.F.,(4,4),(0.,1.),.UNSPECIFIED.);
#444=B_SPLINE_CURVE_WITH_KNOTS('',3,(#12756,#12757,#12758,#12759),
 .UNSPECIFIED.,.F.,.F.,(4,4),(0.,0.999999999942397),.UNSPECIFIED.);
#445=B_SPLINE_CURVE_WITH_KNOTS('',3,(#12763,#12764,#12765,#12766),
 .UNSPECIFIED.,.F.,.F.,(4,4),(0.,1.),.UNSPECIFIED.);
#446=B_SPLINE_CURVE_WITH_KNOTS('',3,(#12768,#12769,#12770,#12771),
 .UNSPECIFIED.,.F.,.F.,(4,4),(0.,0.999999999818942),.UNSPECIFIED.);
#447=B_SPLINE_CURVE_WITH_KNOTS('',3,(#12775,#12776,#12777,#12778),
 .UNSPECIFIED.,.F.,.F.,(4,4),(0.,1.),.UNSPECIFIED.);
#448=B_SPLINE_CURVE_WITH_KNOTS('',3,(#12780,#12781,#12782,#12783),
 .UNSPECIFIED.,.F.,.F.,(4,4),(0.,1.),.UNSPECIFIED.);
#449=B_SPLINE_CURVE_WITH_KNOTS('',3,(#12787,#12788,#12789,#12790),
 .UNSPECIFIED.,.F.,.F.,(4,4),(0.,1.),.UNSPECIFIED.);
#450=B_SPLINE_CURVE_WITH_KNOTS('',3,(#12792,#12793,#12794,#12795),
 .UNSPECIFIED.,.F.,.F.,(4,4),(0.,0.999999999944715),.UNSPECIFIED.);
#451=B_SPLINE_CURVE_WITH_KNOTS('',3,(#12799,#12800,#12801,#12802),
 .UNSPECIFIED.,.F.,.F.,(4,4),(0.,1.),.UNSPECIFIED.);
#452=B_SPLINE_CURVE_WITH_KNOTS('',3,(#12804,#12805,#12806,#12807),
 .UNSPECIFIED.,.F.,.F.,(4,4),(0.,1.),.UNSPECIFIED.);
#453=B_SPLINE_CURVE_WITH_KNOTS('',3,(#12811,#12812,#12813,#12814),
 .UNSPECIFIED.,.F.,.F.,(4,4),(0.,1.),.UNSPECIFIED.);
#454=B_SPLINE_CURVE_WITH_KNOTS('',3,(#12816,#12817,#12818,#12819),
 .UNSPECIFIED.,.F.,.F.,(4,4),(0.,1.00000000000257),.UNSPECIFIED.);
#455=B_SPLINE_CURVE_WITH_KNOTS('',3,(#12823,#12824,#12825,#12826),
 .UNSPECIFIED.,.F.,.F.,(4,4),(1.6055290347619E-11,1.),.UNSPECIFIED.);
#456=B_SPLINE_CURVE_WITH_KNOTS('',3,(#12828,#12829,#12830,#12831),
 .UNSPECIFIED.,.F.,.F.,(4,4),(0.,0.999999999931802),.UNSPECIFIED.);
#457=B_SPLINE_CURVE_WITH_KNOTS('',3,(#12835,#12836,#12837,#12838),
 .UNSPECIFIED.,.F.,.F.,(4,4),(0.,1.),.UNSPECIFIED.);
#458=B_SPLINE_CURVE_WITH_KNOTS('',3,(#12840,#12841,#12842,#12843),
 .UNSPECIFIED.,.F.,.F.,(4,4),(0.,0.999999999920396),.UNSPECIFIED.);
#459=B_SPLINE_CURVE_WITH_KNOTS('',3,(#12847,#12848,#12849,#12850),
 .UNSPECIFIED.,.F.,.F.,(4,4),(0.,1.),.UNSPECIFIED.);
#460=B_SPLINE_CURVE_WITH_KNOTS('',3,(#12852,#12853,#12854,#12855),
 .UNSPECIFIED.,.F.,.F.,(4,4),(0.,1.),.UNSPECIFIED.);
#461=B_SPLINE_CURVE_WITH_KNOTS('',3,(#12859,#12860,#12861,#12862),
 .UNSPECIFIED.,.F.,.F.,(4,4),(0.,1.),.UNSPECIFIED.);
#462=B_SPLINE_CURVE_WITH_KNOTS('',3,(#12864,#12865,#12866,#12867),
 .UNSPECIFIED.,.F.,.F.,(4,4),(0.,0.999999999923948),.UNSPECIFIED.);
#463=B_SPLINE_CURVE_WITH_KNOTS('',3,(#12871,#12872,#12873,#12874),
 .UNSPECIFIED.,.F.,.F.,(4,4),(0.,1.),.UNSPECIFIED.);
#464=B_SPLINE_CURVE_WITH_KNOTS('',3,(#12876,#12877,#12878,#12879),
 .UNSPECIFIED.,.F.,.F.,(4,4),(0.,1.),.UNSPECIFIED.);
#465=B_SPLINE_CURVE_WITH_KNOTS('',3,(#12883,#12884,#12885,#12886),
 .UNSPECIFIED.,.F.,.F.,(4,4),(0.,1.),.UNSPECIFIED.);
#466=B_SPLINE_CURVE_WITH_KNOTS('',3,(#12888,#12889,#12890,#12891),
 .UNSPECIFIED.,.F.,.F.,(4,4),(0.,0.999999999991978),.UNSPECIFIED.);
#467=B_SPLINE_CURVE_WITH_KNOTS('',3,(#12895,#12896,#12897,#12898),
 .UNSPECIFIED.,.F.,.F.,(4,4),(0.,1.),.UNSPECIFIED.);
#468=B_SPLINE_CURVE_WITH_KNOTS('',3,(#12900,#12901,#12902,#12903),
 .UNSPECIFIED.,.F.,.F.,(4,4),(0.,0.999999999980569),.UNSPECIFIED.);
#469=B_SPLINE_CURVE_WITH_KNOTS('',3,(#12907,#12908,#12909,#12910),
 .UNSPECIFIED.,.F.,.F.,(4,4),(0.,1.),.UNSPECIFIED.);
#470=B_SPLINE_CURVE_WITH_KNOTS('',3,(#12912,#12913,#12914,#12915),
 .UNSPECIFIED.,.F.,.F.,(4,4),(0.,1.),.UNSPECIFIED.);
#471=B_SPLINE_CURVE_WITH_KNOTS('',3,(#12919,#12920,#12921,#12922),
 .UNSPECIFIED.,.F.,.F.,(4,4),(0.,1.),.UNSPECIFIED.);
#472=B_SPLINE_CURVE_WITH_KNOTS('',3,(#12924,#12925,#12926,#12927),
 .UNSPECIFIED.,.F.,.F.,(4,4),(0.,0.999999999984122),.UNSPECIFIED.);
#473=B_SPLINE_CURVE_WITH_KNOTS('',3,(#12931,#12932,#12933,#12934),
 .UNSPECIFIED.,.F.,.F.,(4,4),(0.,1.),.UNSPECIFIED.);
#474=B_SPLINE_CURVE_WITH_KNOTS('',3,(#12936,#12937,#12938,#12939),
 .UNSPECIFIED.,.F.,.F.,(4,4),(0.,0.999999999882221),.UNSPECIFIED.);
#888=PLANE('',#8243);
#889=PLANE('',#8245);
#890=PLANE('',#8290);
#891=PLANE('',#8292);
#892=PLANE('',#8293);
#893=PLANE('',#8295);
#894=PLANE('',#8296);
#895=PLANE('',#8298);
#896=PLANE('',#8299);
#897=PLANE('',#8301);
#898=PLANE('',#8302);
#899=PLANE('',#8304);
#900=PLANE('',#8305);
#901=PLANE('',#8307);
#902=PLANE('',#8308);
#903=PLANE('',#8310);
#904=PLANE('',#8311);
#905=PLANE('',#8313);
#906=PLANE('',#8314);
#907=PLANE('',#8316);
#908=PLANE('',#8317);
#909=PLANE('',#8319);
#910=PLANE('',#8320);
#911=PLANE('',#8322);
#912=PLANE('',#8323);
#913=PLANE('',#8325);
#914=PLANE('',#8326);
#915=PLANE('',#8328);
#916=PLANE('',#8329);
#917=PLANE('',#8331);
#918=PLANE('',#8332);
#919=PLANE('',#8334);
#920=PLANE('',#8335);
#921=PLANE('',#8337);
#922=PLANE('',#8338);
#923=PLANE('',#8340);
#924=PLANE('',#8341);
#925=PLANE('',#8343);
#926=PLANE('',#8344);
#927=PLANE('',#8346);
#928=PLANE('',#8347);
#929=PLANE('',#8349);
#930=PLANE('',#8350);
#931=PLANE('',#8352);
#932=PLANE('',#8353);
#933=PLANE('',#8355);
#934=PLANE('',#8356);
#935=PLANE('',#8358);
#936=PLANE('',#8359);
#937=PLANE('',#8361);
#938=PLANE('',#8362);
#939=PLANE('',#8364);
#940=PLANE('',#8365);
#941=PLANE('',#8367);
#942=PLANE('',#8368);
#943=PLANE('',#8370);
#944=PLANE('',#8371);
#945=PLANE('',#8373);
#946=PLANE('',#8374);
#947=PLANE('',#8376);
#948=PLANE('',#8377);
#949=PLANE('',#8379);
#950=PLANE('',#8380);
#951=PLANE('',#8382);
#952=PLANE('',#8383);
#953=PLANE('',#8385);
#954=PLANE('',#8386);
#955=PLANE('',#8388);
#956=PLANE('',#8389);
#957=PLANE('',#8391);
#958=PLANE('',#8392);
#959=PLANE('',#8394);
#960=PLANE('',#8395);
#961=PLANE('',#8397);
#962=PLANE('',#8398);
#963=PLANE('',#8400);
#964=PLANE('',#8401);
#965=PLANE('',#8403);
#966=PLANE('',#8404);
#967=PLANE('',#8406);
#968=PLANE('',#8407);
#969=PLANE('',#8409);
#970=PLANE('',#8410);
#971=PLANE('',#8414);
#972=PLANE('',#8415);
#973=PLANE('',#8440);
#974=PLANE('',#8441);
#975=PLANE('',#8444);
#976=PLANE('',#8445);
#977=PLANE('',#8448);
#978=PLANE('',#8449);
#979=PLANE('',#8452);
#980=PLANE('',#8453);
#981=PLANE('',#8456);
#982=PLANE('',#8457);
#983=PLANE('',#8460);
#984=PLANE('',#8461);
#985=PLANE('',#8464);
#986=PLANE('',#8465);
#987=PLANE('',#8468);
#988=PLANE('',#8469);
#989=PLANE('',#8472);
#990=PLANE('',#8473);
#991=PLANE('',#8476);
#992=PLANE('',#8477);
#993=PLANE('',#8480);
#994=PLANE('',#8481);
#995=PLANE('',#8484);
#996=PLANE('',#8485);
#997=PLANE('',#8488);
#998=PLANE('',#8489);
#999=PLANE('',#8492);
#1000=PLANE('',#8493);
#1001=PLANE('',#8496);
#1002=PLANE('',#8497);
#1003=PLANE('',#8500);
#1004=PLANE('',#8501);
#1005=PLANE('',#8504);
#1006=PLANE('',#8505);
#1007=PLANE('',#8508);
#1008=PLANE('',#8509);
#1009=PLANE('',#8512);
#1010=PLANE('',#8513);
#1011=PLANE('',#8516);
#1012=PLANE('',#8517);
#1013=PLANE('',#8518);
#1014=PLANE('',#8520);
#1015=PLANE('',#8521);
#1016=PLANE('',#8522);
#1017=PLANE('',#8523);
#1018=PLANE('',#8524);
#1019=PLANE('',#8525);
#1020=PLANE('',#8526);
#1021=PLANE('',#8527);
#1022=PLANE('',#8528);
#1023=PLANE('',#8529);
#1024=PLANE('',#8530);
#1025=PLANE('',#8531);
#1026=PLANE('',#8532);
#1027=PLANE('',#8533);
#1028=PLANE('',#8534);
#1029=PLANE('',#8535);
#1030=PLANE('',#8536);
#1031=PLANE('',#8537);
#1032=PLANE('',#8538);
#1094=ORIENTED_EDGE('',*,*,#3468,.F.);
#1095=ORIENTED_EDGE('',*,*,#3469,.F.);
#1096=ORIENTED_EDGE('',*,*,#3470,.F.);
#1097=ORIENTED_EDGE('',*,*,#3468,.T.);
#1098=ORIENTED_EDGE('',*,*,#3471,.F.);
#1099=ORIENTED_EDGE('',*,*,#3469,.T.);
#1100=ORIENTED_EDGE('',*,*,#3470,.T.);
#1101=ORIENTED_EDGE('',*,*,#3472,.T.);
#1102=ORIENTED_EDGE('',*,*,#3473,.T.);
#1103=ORIENTED_EDGE('',*,*,#3474,.T.);
#1104=ORIENTED_EDGE('',*,*,#3475,.T.);
#1105=ORIENTED_EDGE('',*,*,#3476,.T.);
#1106=ORIENTED_EDGE('',*,*,#3477,.T.);
#1107=ORIENTED_EDGE('',*,*,#3478,.T.);
#1108=ORIENTED_EDGE('',*,*,#3479,.T.);
#1109=ORIENTED_EDGE('',*,*,#3480,.T.);
#1110=ORIENTED_EDGE('',*,*,#3481,.T.);
#1111=ORIENTED_EDGE('',*,*,#3482,.T.);
#1112=ORIENTED_EDGE('',*,*,#3483,.T.);
#1113=ORIENTED_EDGE('',*,*,#3484,.T.);
#1114=ORIENTED_EDGE('',*,*,#3485,.T.);
#1115=ORIENTED_EDGE('',*,*,#3486,.T.);
#1116=ORIENTED_EDGE('',*,*,#3487,.T.);
#1117=ORIENTED_EDGE('',*,*,#3488,.T.);
#1118=ORIENTED_EDGE('',*,*,#3489,.T.);
#1119=ORIENTED_EDGE('',*,*,#3490,.T.);
#1120=ORIENTED_EDGE('',*,*,#3491,.T.);
#1121=ORIENTED_EDGE('',*,*,#3492,.T.);
#1122=ORIENTED_EDGE('',*,*,#3493,.T.);
#1123=ORIENTED_EDGE('',*,*,#3494,.T.);
#1124=ORIENTED_EDGE('',*,*,#3495,.T.);
#1125=ORIENTED_EDGE('',*,*,#3496,.T.);
#1126=ORIENTED_EDGE('',*,*,#3497,.T.);
#1127=ORIENTED_EDGE('',*,*,#3498,.T.);
#1128=ORIENTED_EDGE('',*,*,#3499,.T.);
#1129=ORIENTED_EDGE('',*,*,#3500,.T.);
#1130=ORIENTED_EDGE('',*,*,#3501,.T.);
#1131=ORIENTED_EDGE('',*,*,#3502,.T.);
#1132=ORIENTED_EDGE('',*,*,#3503,.T.);
#1133=ORIENTED_EDGE('',*,*,#3504,.T.);
#1134=ORIENTED_EDGE('',*,*,#3505,.T.);
#1135=ORIENTED_EDGE('',*,*,#3506,.T.);
#1136=ORIENTED_EDGE('',*,*,#3507,.T.);
#1137=ORIENTED_EDGE('',*,*,#3508,.T.);
#1138=ORIENTED_EDGE('',*,*,#3509,.T.);
#1139=ORIENTED_EDGE('',*,*,#3510,.T.);
#1140=ORIENTED_EDGE('',*,*,#3511,.T.);
#1141=ORIENTED_EDGE('',*,*,#3512,.T.);
#1142=ORIENTED_EDGE('',*,*,#3513,.T.);
#1143=ORIENTED_EDGE('',*,*,#3514,.T.);
#1144=ORIENTED_EDGE('',*,*,#3515,.T.);
#1145=ORIENTED_EDGE('',*,*,#3516,.T.);
#1146=ORIENTED_EDGE('',*,*,#3517,.T.);
#1147=ORIENTED_EDGE('',*,*,#3518,.T.);
#1148=ORIENTED_EDGE('',*,*,#3519,.T.);
#1149=ORIENTED_EDGE('',*,*,#3520,.T.);
#1150=ORIENTED_EDGE('',*,*,#3521,.T.);
#1151=ORIENTED_EDGE('',*,*,#3522,.T.);
#1152=ORIENTED_EDGE('',*,*,#3523,.T.);
#1153=ORIENTED_EDGE('',*,*,#3524,.T.);
#1154=ORIENTED_EDGE('',*,*,#3525,.T.);
#1155=ORIENTED_EDGE('',*,*,#3526,.T.);
#1156=ORIENTED_EDGE('',*,*,#3527,.T.);
#1157=ORIENTED_EDGE('',*,*,#3528,.T.);
#1158=ORIENTED_EDGE('',*,*,#3529,.T.);
#1159=ORIENTED_EDGE('',*,*,#3530,.T.);
#1160=ORIENTED_EDGE('',*,*,#3531,.T.);
#1161=ORIENTED_EDGE('',*,*,#3532,.T.);
#1162=ORIENTED_EDGE('',*,*,#3533,.T.);
#1163=ORIENTED_EDGE('',*,*,#3534,.T.);
#1164=ORIENTED_EDGE('',*,*,#3535,.T.);
#1165=ORIENTED_EDGE('',*,*,#3536,.T.);
#1166=ORIENTED_EDGE('',*,*,#3537,.T.);
#1167=ORIENTED_EDGE('',*,*,#3538,.T.);
#1168=ORIENTED_EDGE('',*,*,#3539,.T.);
#1169=ORIENTED_EDGE('',*,*,#3540,.T.);
#1170=ORIENTED_EDGE('',*,*,#3541,.T.);
#1171=ORIENTED_EDGE('',*,*,#3542,.T.);
#1172=ORIENTED_EDGE('',*,*,#3543,.T.);
#1173=ORIENTED_EDGE('',*,*,#3544,.T.);
#1174=ORIENTED_EDGE('',*,*,#3545,.T.);
#1175=ORIENTED_EDGE('',*,*,#3546,.T.);
#1176=ORIENTED_EDGE('',*,*,#3547,.T.);
#1177=ORIENTED_EDGE('',*,*,#3548,.T.);
#1178=ORIENTED_EDGE('',*,*,#3549,.T.);
#1179=ORIENTED_EDGE('',*,*,#3550,.T.);
#1180=ORIENTED_EDGE('',*,*,#3551,.T.);
#1181=ORIENTED_EDGE('',*,*,#3552,.T.);
#1182=ORIENTED_EDGE('',*,*,#3471,.T.);
#1183=ORIENTED_EDGE('',*,*,#3512,.F.);
#1184=ORIENTED_EDGE('',*,*,#3553,.T.);
#1185=ORIENTED_EDGE('',*,*,#3554,.T.);
#1186=ORIENTED_EDGE('',*,*,#3555,.T.);
#1187=ORIENTED_EDGE('',*,*,#3513,.F.);
#1188=ORIENTED_EDGE('',*,*,#3555,.F.);
#1189=ORIENTED_EDGE('',*,*,#3556,.T.);
#1190=ORIENTED_EDGE('',*,*,#3557,.T.);
#1191=ORIENTED_EDGE('',*,*,#3558,.T.);
#1192=ORIENTED_EDGE('',*,*,#3559,.F.);
#1193=ORIENTED_EDGE('',*,*,#3560,.F.);
#1194=ORIENTED_EDGE('',*,*,#3561,.F.);
#1195=ORIENTED_EDGE('',*,*,#3514,.F.);
#1196=ORIENTED_EDGE('',*,*,#3558,.F.);
#1197=ORIENTED_EDGE('',*,*,#3562,.F.);
#1198=ORIENTED_EDGE('',*,*,#3563,.T.);
#1199=ORIENTED_EDGE('',*,*,#3564,.T.);
#1200=ORIENTED_EDGE('',*,*,#3565,.T.);
#1201=ORIENTED_EDGE('',*,*,#3515,.F.);
#1202=ORIENTED_EDGE('',*,*,#3561,.T.);
#1203=ORIENTED_EDGE('',*,*,#3516,.F.);
#1204=ORIENTED_EDGE('',*,*,#3565,.F.);
#1205=ORIENTED_EDGE('',*,*,#3566,.T.);
#1206=ORIENTED_EDGE('',*,*,#3567,.T.);
#1207=ORIENTED_EDGE('',*,*,#3517,.F.);
#1208=ORIENTED_EDGE('',*,*,#3567,.F.);
#1209=ORIENTED_EDGE('',*,*,#3568,.T.);
#1210=ORIENTED_EDGE('',*,*,#3569,.T.);
#1211=ORIENTED_EDGE('',*,*,#3570,.T.);
#1212=ORIENTED_EDGE('',*,*,#3570,.F.);
#1213=ORIENTED_EDGE('',*,*,#3571,.F.);
#1214=ORIENTED_EDGE('',*,*,#3572,.F.);
#1215=ORIENTED_EDGE('',*,*,#3573,.F.);
#1216=ORIENTED_EDGE('',*,*,#3574,.F.);
#1217=ORIENTED_EDGE('',*,*,#3518,.F.);
#1218=ORIENTED_EDGE('',*,*,#3575,.T.);
#1219=ORIENTED_EDGE('',*,*,#3576,.T.);
#1220=ORIENTED_EDGE('',*,*,#3577,.T.);
#1221=ORIENTED_EDGE('',*,*,#3519,.F.);
#1222=ORIENTED_EDGE('',*,*,#3574,.T.);
#1223=ORIENTED_EDGE('',*,*,#3520,.F.);
#1224=ORIENTED_EDGE('',*,*,#3577,.F.);
#1225=ORIENTED_EDGE('',*,*,#3578,.T.);
#1226=ORIENTED_EDGE('',*,*,#3579,.T.);
#1227=ORIENTED_EDGE('',*,*,#3521,.F.);
#1228=ORIENTED_EDGE('',*,*,#3579,.F.);
#1229=ORIENTED_EDGE('',*,*,#3580,.T.);
#1230=ORIENTED_EDGE('',*,*,#3581,.T.);
#1231=ORIENTED_EDGE('',*,*,#3582,.T.);
#1232=ORIENTED_EDGE('',*,*,#3582,.F.);
#1233=ORIENTED_EDGE('',*,*,#3583,.F.);
#1234=ORIENTED_EDGE('',*,*,#3584,.F.);
#1235=ORIENTED_EDGE('',*,*,#3585,.F.);
#1236=ORIENTED_EDGE('',*,*,#3586,.F.);
#1237=ORIENTED_EDGE('',*,*,#3522,.F.);
#1238=ORIENTED_EDGE('',*,*,#3587,.T.);
#1239=ORIENTED_EDGE('',*,*,#3588,.T.);
#1240=ORIENTED_EDGE('',*,*,#3589,.T.);
#1241=ORIENTED_EDGE('',*,*,#3523,.F.);
#1242=ORIENTED_EDGE('',*,*,#3586,.T.);
#1243=ORIENTED_EDGE('',*,*,#3524,.F.);
#1244=ORIENTED_EDGE('',*,*,#3589,.F.);
#1245=ORIENTED_EDGE('',*,*,#3590,.T.);
#1246=ORIENTED_EDGE('',*,*,#3591,.T.);
#1247=ORIENTED_EDGE('',*,*,#3525,.F.);
#1248=ORIENTED_EDGE('',*,*,#3591,.F.);
#1249=ORIENTED_EDGE('',*,*,#3592,.T.);
#1250=ORIENTED_EDGE('',*,*,#3593,.T.);
#1251=ORIENTED_EDGE('',*,*,#3594,.T.);
#1252=ORIENTED_EDGE('',*,*,#3594,.F.);
#1253=ORIENTED_EDGE('',*,*,#3595,.F.);
#1254=ORIENTED_EDGE('',*,*,#3596,.F.);
#1255=ORIENTED_EDGE('',*,*,#3597,.F.);
#1256=ORIENTED_EDGE('',*,*,#3598,.F.);
#1257=ORIENTED_EDGE('',*,*,#3526,.F.);
#1258=ORIENTED_EDGE('',*,*,#3599,.T.);
#1259=ORIENTED_EDGE('',*,*,#3600,.T.);
#1260=ORIENTED_EDGE('',*,*,#3601,.T.);
#1261=ORIENTED_EDGE('',*,*,#3527,.F.);
#1262=ORIENTED_EDGE('',*,*,#3598,.T.);
#1263=ORIENTED_EDGE('',*,*,#3528,.F.);
#1264=ORIENTED_EDGE('',*,*,#3601,.F.);
#1265=ORIENTED_EDGE('',*,*,#3602,.T.);
#1266=ORIENTED_EDGE('',*,*,#3603,.T.);
#1267=ORIENTED_EDGE('',*,*,#3529,.F.);
#1268=ORIENTED_EDGE('',*,*,#3603,.F.);
#1269=ORIENTED_EDGE('',*,*,#3604,.T.);
#1270=ORIENTED_EDGE('',*,*,#3605,.T.);
#1271=ORIENTED_EDGE('',*,*,#3606,.T.);
#1272=ORIENTED_EDGE('',*,*,#3606,.F.);
#1273=ORIENTED_EDGE('',*,*,#3607,.F.);
#1274=ORIENTED_EDGE('',*,*,#3608,.F.);
#1275=ORIENTED_EDGE('',*,*,#3609,.F.);
#1276=ORIENTED_EDGE('',*,*,#3610,.F.);
#1277=ORIENTED_EDGE('',*,*,#3530,.F.);
#1278=ORIENTED_EDGE('',*,*,#3611,.T.);
#1279=ORIENTED_EDGE('',*,*,#3612,.T.);
#1280=ORIENTED_EDGE('',*,*,#3613,.T.);
#1281=ORIENTED_EDGE('',*,*,#3531,.F.);
#1282=ORIENTED_EDGE('',*,*,#3610,.T.);
#1283=ORIENTED_EDGE('',*,*,#3532,.F.);
#1284=ORIENTED_EDGE('',*,*,#3613,.F.);
#1285=ORIENTED_EDGE('',*,*,#3614,.T.);
#1286=ORIENTED_EDGE('',*,*,#3615,.T.);
#1287=ORIENTED_EDGE('',*,*,#3533,.F.);
#1288=ORIENTED_EDGE('',*,*,#3615,.F.);
#1289=ORIENTED_EDGE('',*,*,#3616,.T.);
#1290=ORIENTED_EDGE('',*,*,#3617,.T.);
#1291=ORIENTED_EDGE('',*,*,#3618,.T.);
#1292=ORIENTED_EDGE('',*,*,#3618,.F.);
#1293=ORIENTED_EDGE('',*,*,#3619,.F.);
#1294=ORIENTED_EDGE('',*,*,#3620,.F.);
#1295=ORIENTED_EDGE('',*,*,#3621,.F.);
#1296=ORIENTED_EDGE('',*,*,#3622,.F.);
#1297=ORIENTED_EDGE('',*,*,#3534,.F.);
#1298=ORIENTED_EDGE('',*,*,#3623,.T.);
#1299=ORIENTED_EDGE('',*,*,#3624,.T.);
#1300=ORIENTED_EDGE('',*,*,#3625,.T.);
#1301=ORIENTED_EDGE('',*,*,#3535,.F.);
#1302=ORIENTED_EDGE('',*,*,#3622,.T.);
#1303=ORIENTED_EDGE('',*,*,#3536,.F.);
#1304=ORIENTED_EDGE('',*,*,#3625,.F.);
#1305=ORIENTED_EDGE('',*,*,#3626,.T.);
#1306=ORIENTED_EDGE('',*,*,#3627,.T.);
#1307=ORIENTED_EDGE('',*,*,#3537,.F.);
#1308=ORIENTED_EDGE('',*,*,#3627,.F.);
#1309=ORIENTED_EDGE('',*,*,#3628,.T.);
#1310=ORIENTED_EDGE('',*,*,#3629,.T.);
#1311=ORIENTED_EDGE('',*,*,#3630,.T.);
#1312=ORIENTED_EDGE('',*,*,#3630,.F.);
#1313=ORIENTED_EDGE('',*,*,#3631,.F.);
#1314=ORIENTED_EDGE('',*,*,#3632,.F.);
#1315=ORIENTED_EDGE('',*,*,#3633,.F.);
#1316=ORIENTED_EDGE('',*,*,#3634,.F.);
#1317=ORIENTED_EDGE('',*,*,#3538,.F.);
#1318=ORIENTED_EDGE('',*,*,#3635,.T.);
#1319=ORIENTED_EDGE('',*,*,#3636,.T.);
#1320=ORIENTED_EDGE('',*,*,#3637,.T.);
#1321=ORIENTED_EDGE('',*,*,#3539,.F.);
#1322=ORIENTED_EDGE('',*,*,#3634,.T.);
#1323=ORIENTED_EDGE('',*,*,#3540,.F.);
#1324=ORIENTED_EDGE('',*,*,#3637,.F.);
#1325=ORIENTED_EDGE('',*,*,#3638,.T.);
#1326=ORIENTED_EDGE('',*,*,#3639,.T.);
#1327=ORIENTED_EDGE('',*,*,#3541,.F.);
#1328=ORIENTED_EDGE('',*,*,#3639,.F.);
#1329=ORIENTED_EDGE('',*,*,#3640,.T.);
#1330=ORIENTED_EDGE('',*,*,#3641,.T.);
#1331=ORIENTED_EDGE('',*,*,#3642,.T.);
#1332=ORIENTED_EDGE('',*,*,#3642,.F.);
#1333=ORIENTED_EDGE('',*,*,#3643,.F.);
#1334=ORIENTED_EDGE('',*,*,#3644,.F.);
#1335=ORIENTED_EDGE('',*,*,#3645,.F.);
#1336=ORIENTED_EDGE('',*,*,#3646,.F.);
#1337=ORIENTED_EDGE('',*,*,#3542,.F.);
#1338=ORIENTED_EDGE('',*,*,#3647,.T.);
#1339=ORIENTED_EDGE('',*,*,#3648,.T.);
#1340=ORIENTED_EDGE('',*,*,#3649,.T.);
#1341=ORIENTED_EDGE('',*,*,#3543,.F.);
#1342=ORIENTED_EDGE('',*,*,#3646,.T.);
#1343=ORIENTED_EDGE('',*,*,#3544,.F.);
#1344=ORIENTED_EDGE('',*,*,#3649,.F.);
#1345=ORIENTED_EDGE('',*,*,#3650,.T.);
#1346=ORIENTED_EDGE('',*,*,#3651,.T.);
#1347=ORIENTED_EDGE('',*,*,#3545,.F.);
#1348=ORIENTED_EDGE('',*,*,#3651,.F.);
#1349=ORIENTED_EDGE('',*,*,#3652,.T.);
#1350=ORIENTED_EDGE('',*,*,#3653,.T.);
#1351=ORIENTED_EDGE('',*,*,#3654,.T.);
#1352=ORIENTED_EDGE('',*,*,#3654,.F.);
#1353=ORIENTED_EDGE('',*,*,#3655,.F.);
#1354=ORIENTED_EDGE('',*,*,#3656,.F.);
#1355=ORIENTED_EDGE('',*,*,#3657,.F.);
#1356=ORIENTED_EDGE('',*,*,#3658,.F.);
#1357=ORIENTED_EDGE('',*,*,#3546,.F.);
#1358=ORIENTED_EDGE('',*,*,#3659,.T.);
#1359=ORIENTED_EDGE('',*,*,#3660,.T.);
#1360=ORIENTED_EDGE('',*,*,#3661,.T.);
#1361=ORIENTED_EDGE('',*,*,#3547,.F.);
#1362=ORIENTED_EDGE('',*,*,#3658,.T.);
#1363=ORIENTED_EDGE('',*,*,#3548,.F.);
#1364=ORIENTED_EDGE('',*,*,#3661,.F.);
#1365=ORIENTED_EDGE('',*,*,#3662,.T.);
#1366=ORIENTED_EDGE('',*,*,#3663,.T.);
#1367=ORIENTED_EDGE('',*,*,#3549,.F.);
#1368=ORIENTED_EDGE('',*,*,#3663,.F.);
#1369=ORIENTED_EDGE('',*,*,#3664,.T.);
#1370=ORIENTED_EDGE('',*,*,#3665,.T.);
#1371=ORIENTED_EDGE('',*,*,#3666,.T.);
#1372=ORIENTED_EDGE('',*,*,#3666,.F.);
#1373=ORIENTED_EDGE('',*,*,#3667,.F.);
#1374=ORIENTED_EDGE('',*,*,#3668,.F.);
#1375=ORIENTED_EDGE('',*,*,#3669,.F.);
#1376=ORIENTED_EDGE('',*,*,#3670,.F.);
#1377=ORIENTED_EDGE('',*,*,#3550,.F.);
#1378=ORIENTED_EDGE('',*,*,#3671,.T.);
#1379=ORIENTED_EDGE('',*,*,#3672,.T.);
#1380=ORIENTED_EDGE('',*,*,#3673,.T.);
#1381=ORIENTED_EDGE('',*,*,#3551,.F.);
#1382=ORIENTED_EDGE('',*,*,#3670,.T.);
#1383=ORIENTED_EDGE('',*,*,#3472,.F.);
#1384=ORIENTED_EDGE('',*,*,#3673,.F.);
#1385=ORIENTED_EDGE('',*,*,#3674,.T.);
#1386=ORIENTED_EDGE('',*,*,#3675,.T.);
#1387=ORIENTED_EDGE('',*,*,#3473,.F.);
#1388=ORIENTED_EDGE('',*,*,#3675,.F.);
#1389=ORIENTED_EDGE('',*,*,#3676,.T.);
#1390=ORIENTED_EDGE('',*,*,#3677,.T.);
#1391=ORIENTED_EDGE('',*,*,#3678,.T.);
#1392=ORIENTED_EDGE('',*,*,#3678,.F.);
#1393=ORIENTED_EDGE('',*,*,#3679,.F.);
#1394=ORIENTED_EDGE('',*,*,#3680,.F.);
#1395=ORIENTED_EDGE('',*,*,#3681,.F.);
#1396=ORIENTED_EDGE('',*,*,#3682,.F.);
#1397=ORIENTED_EDGE('',*,*,#3474,.F.);
#1398=ORIENTED_EDGE('',*,*,#3683,.T.);
#1399=ORIENTED_EDGE('',*,*,#3684,.T.);
#1400=ORIENTED_EDGE('',*,*,#3685,.T.);
#1401=ORIENTED_EDGE('',*,*,#3475,.F.);
#1402=ORIENTED_EDGE('',*,*,#3682,.T.);
#1403=ORIENTED_EDGE('',*,*,#3476,.F.);
#1404=ORIENTED_EDGE('',*,*,#3685,.F.);
#1405=ORIENTED_EDGE('',*,*,#3686,.T.);
#1406=ORIENTED_EDGE('',*,*,#3687,.T.);
#1407=ORIENTED_EDGE('',*,*,#3477,.F.);
#1408=ORIENTED_EDGE('',*,*,#3687,.F.);
#1409=ORIENTED_EDGE('',*,*,#3688,.T.);
#1410=ORIENTED_EDGE('',*,*,#3689,.T.);
#1411=ORIENTED_EDGE('',*,*,#3690,.T.);
#1412=ORIENTED_EDGE('',*,*,#3690,.F.);
#1413=ORIENTED_EDGE('',*,*,#3691,.F.);
#1414=ORIENTED_EDGE('',*,*,#3692,.F.);
#1415=ORIENTED_EDGE('',*,*,#3693,.F.);
#1416=ORIENTED_EDGE('',*,*,#3694,.F.);
#1417=ORIENTED_EDGE('',*,*,#3478,.F.);
#1418=ORIENTED_EDGE('',*,*,#3695,.T.);
#1419=ORIENTED_EDGE('',*,*,#3696,.T.);
#1420=ORIENTED_EDGE('',*,*,#3697,.T.);
#1421=ORIENTED_EDGE('',*,*,#3479,.F.);
#1422=ORIENTED_EDGE('',*,*,#3694,.T.);
#1423=ORIENTED_EDGE('',*,*,#3480,.F.);
#1424=ORIENTED_EDGE('',*,*,#3697,.F.);
#1425=ORIENTED_EDGE('',*,*,#3698,.T.);
#1426=ORIENTED_EDGE('',*,*,#3699,.T.);
#1427=ORIENTED_EDGE('',*,*,#3481,.F.);
#1428=ORIENTED_EDGE('',*,*,#3699,.F.);
#1429=ORIENTED_EDGE('',*,*,#3700,.T.);
#1430=ORIENTED_EDGE('',*,*,#3701,.T.);
#1431=ORIENTED_EDGE('',*,*,#3702,.T.);
#1432=ORIENTED_EDGE('',*,*,#3702,.F.);
#1433=ORIENTED_EDGE('',*,*,#3703,.F.);
#1434=ORIENTED_EDGE('',*,*,#3704,.F.);
#1435=ORIENTED_EDGE('',*,*,#3705,.F.);
#1436=ORIENTED_EDGE('',*,*,#3706,.F.);
#1437=ORIENTED_EDGE('',*,*,#3482,.F.);
#1438=ORIENTED_EDGE('',*,*,#3707,.T.);
#1439=ORIENTED_EDGE('',*,*,#3708,.T.);
#1440=ORIENTED_EDGE('',*,*,#3709,.T.);
#1441=ORIENTED_EDGE('',*,*,#3483,.F.);
#1442=ORIENTED_EDGE('',*,*,#3706,.T.);
#1443=ORIENTED_EDGE('',*,*,#3484,.F.);
#1444=ORIENTED_EDGE('',*,*,#3709,.F.);
#1445=ORIENTED_EDGE('',*,*,#3710,.T.);
#1446=ORIENTED_EDGE('',*,*,#3711,.T.);
#1447=ORIENTED_EDGE('',*,*,#3485,.F.);
#1448=ORIENTED_EDGE('',*,*,#3711,.F.);
#1449=ORIENTED_EDGE('',*,*,#3712,.T.);
#1450=ORIENTED_EDGE('',*,*,#3713,.T.);
#1451=ORIENTED_EDGE('',*,*,#3714,.T.);
#1452=ORIENTED_EDGE('',*,*,#3714,.F.);
#1453=ORIENTED_EDGE('',*,*,#3715,.F.);
#1454=ORIENTED_EDGE('',*,*,#3716,.F.);
#1455=ORIENTED_EDGE('',*,*,#3717,.F.);
#1456=ORIENTED_EDGE('',*,*,#3718,.F.);
#1457=ORIENTED_EDGE('',*,*,#3486,.F.);
#1458=ORIENTED_EDGE('',*,*,#3719,.T.);
#1459=ORIENTED_EDGE('',*,*,#3720,.T.);
#1460=ORIENTED_EDGE('',*,*,#3721,.T.);
#1461=ORIENTED_EDGE('',*,*,#3487,.F.);
#1462=ORIENTED_EDGE('',*,*,#3718,.T.);
#1463=ORIENTED_EDGE('',*,*,#3488,.F.);
#1464=ORIENTED_EDGE('',*,*,#3721,.F.);
#1465=ORIENTED_EDGE('',*,*,#3722,.T.);
#1466=ORIENTED_EDGE('',*,*,#3723,.T.);
#1467=ORIENTED_EDGE('',*,*,#3489,.F.);
#1468=ORIENTED_EDGE('',*,*,#3723,.F.);
#1469=ORIENTED_EDGE('',*,*,#3724,.T.);
#1470=ORIENTED_EDGE('',*,*,#3725,.T.);
#1471=ORIENTED_EDGE('',*,*,#3726,.T.);
#1472=ORIENTED_EDGE('',*,*,#3726,.F.);
#1473=ORIENTED_EDGE('',*,*,#3727,.F.);
#1474=ORIENTED_EDGE('',*,*,#3728,.F.);
#1475=ORIENTED_EDGE('',*,*,#3729,.F.);
#1476=ORIENTED_EDGE('',*,*,#3730,.F.);
#1477=ORIENTED_EDGE('',*,*,#3490,.F.);
#1478=ORIENTED_EDGE('',*,*,#3731,.T.);
#1479=ORIENTED_EDGE('',*,*,#3732,.T.);
#1480=ORIENTED_EDGE('',*,*,#3733,.T.);
#1481=ORIENTED_EDGE('',*,*,#3491,.F.);
#1482=ORIENTED_EDGE('',*,*,#3730,.T.);
#1483=ORIENTED_EDGE('',*,*,#3492,.F.);
#1484=ORIENTED_EDGE('',*,*,#3733,.F.);
#1485=ORIENTED_EDGE('',*,*,#3734,.T.);
#1486=ORIENTED_EDGE('',*,*,#3735,.T.);
#1487=ORIENTED_EDGE('',*,*,#3493,.F.);
#1488=ORIENTED_EDGE('',*,*,#3735,.F.);
#1489=ORIENTED_EDGE('',*,*,#3736,.T.);
#1490=ORIENTED_EDGE('',*,*,#3737,.T.);
#1491=ORIENTED_EDGE('',*,*,#3738,.T.);
#1492=ORIENTED_EDGE('',*,*,#3738,.F.);
#1493=ORIENTED_EDGE('',*,*,#3739,.F.);
#1494=ORIENTED_EDGE('',*,*,#3740,.F.);
#1495=ORIENTED_EDGE('',*,*,#3741,.F.);
#1496=ORIENTED_EDGE('',*,*,#3742,.F.);
#1497=ORIENTED_EDGE('',*,*,#3494,.F.);
#1498=ORIENTED_EDGE('',*,*,#3743,.T.);
#1499=ORIENTED_EDGE('',*,*,#3744,.T.);
#1500=ORIENTED_EDGE('',*,*,#3745,.T.);
#1501=ORIENTED_EDGE('',*,*,#3495,.F.);
#1502=ORIENTED_EDGE('',*,*,#3742,.T.);
#1503=ORIENTED_EDGE('',*,*,#3496,.F.);
#1504=ORIENTED_EDGE('',*,*,#3745,.F.);
#1505=ORIENTED_EDGE('',*,*,#3746,.T.);
#1506=ORIENTED_EDGE('',*,*,#3747,.T.);
#1507=ORIENTED_EDGE('',*,*,#3497,.F.);
#1508=ORIENTED_EDGE('',*,*,#3747,.F.);
#1509=ORIENTED_EDGE('',*,*,#3748,.T.);
#1510=ORIENTED_EDGE('',*,*,#3749,.T.);
#1511=ORIENTED_EDGE('',*,*,#3750,.T.);
#1512=ORIENTED_EDGE('',*,*,#3750,.F.);
#1513=ORIENTED_EDGE('',*,*,#3751,.F.);
#1514=ORIENTED_EDGE('',*,*,#3752,.F.);
#1515=ORIENTED_EDGE('',*,*,#3753,.F.);
#1516=ORIENTED_EDGE('',*,*,#3754,.F.);
#1517=ORIENTED_EDGE('',*,*,#3498,.F.);
#1518=ORIENTED_EDGE('',*,*,#3755,.T.);
#1519=ORIENTED_EDGE('',*,*,#3756,.T.);
#1520=ORIENTED_EDGE('',*,*,#3757,.T.);
#1521=ORIENTED_EDGE('',*,*,#3499,.F.);
#1522=ORIENTED_EDGE('',*,*,#3754,.T.);
#1523=ORIENTED_EDGE('',*,*,#3500,.F.);
#1524=ORIENTED_EDGE('',*,*,#3757,.F.);
#1525=ORIENTED_EDGE('',*,*,#3758,.T.);
#1526=ORIENTED_EDGE('',*,*,#3759,.T.);
#1527=ORIENTED_EDGE('',*,*,#3501,.F.);
#1528=ORIENTED_EDGE('',*,*,#3759,.F.);
#1529=ORIENTED_EDGE('',*,*,#3760,.T.);
#1530=ORIENTED_EDGE('',*,*,#3761,.T.);
#1531=ORIENTED_EDGE('',*,*,#3762,.T.);
#1532=ORIENTED_EDGE('',*,*,#3762,.F.);
#1533=ORIENTED_EDGE('',*,*,#3763,.F.);
#1534=ORIENTED_EDGE('',*,*,#3764,.F.);
#1535=ORIENTED_EDGE('',*,*,#3765,.F.);
#1536=ORIENTED_EDGE('',*,*,#3766,.F.);
#1537=ORIENTED_EDGE('',*,*,#3502,.F.);
#1538=ORIENTED_EDGE('',*,*,#3767,.T.);
#1539=ORIENTED_EDGE('',*,*,#3768,.T.);
#1540=ORIENTED_EDGE('',*,*,#3769,.T.);
#1541=ORIENTED_EDGE('',*,*,#3503,.F.);
#1542=ORIENTED_EDGE('',*,*,#3766,.T.);
#1543=ORIENTED_EDGE('',*,*,#3504,.F.);
#1544=ORIENTED_EDGE('',*,*,#3769,.F.);
#1545=ORIENTED_EDGE('',*,*,#3770,.T.);
#1546=ORIENTED_EDGE('',*,*,#3771,.T.);
#1547=ORIENTED_EDGE('',*,*,#3505,.F.);
#1548=ORIENTED_EDGE('',*,*,#3771,.F.);
#1549=ORIENTED_EDGE('',*,*,#3772,.T.);
#1550=ORIENTED_EDGE('',*,*,#3773,.T.);
#1551=ORIENTED_EDGE('',*,*,#3774,.T.);
#1552=ORIENTED_EDGE('',*,*,#3774,.F.);
#1553=ORIENTED_EDGE('',*,*,#3775,.F.);
#1554=ORIENTED_EDGE('',*,*,#3776,.F.);
#1555=ORIENTED_EDGE('',*,*,#3777,.F.);
#1556=ORIENTED_EDGE('',*,*,#3778,.F.);
#1557=ORIENTED_EDGE('',*,*,#3506,.F.);
#1558=ORIENTED_EDGE('',*,*,#3779,.T.);
#1559=ORIENTED_EDGE('',*,*,#3780,.T.);
#1560=ORIENTED_EDGE('',*,*,#3781,.T.);
#1561=ORIENTED_EDGE('',*,*,#3507,.F.);
#1562=ORIENTED_EDGE('',*,*,#3778,.T.);
#1563=ORIENTED_EDGE('',*,*,#3508,.F.);
#1564=ORIENTED_EDGE('',*,*,#3781,.F.);
#1565=ORIENTED_EDGE('',*,*,#3782,.T.);
#1566=ORIENTED_EDGE('',*,*,#3783,.T.);
#1567=ORIENTED_EDGE('',*,*,#3509,.F.);
#1568=ORIENTED_EDGE('',*,*,#3783,.F.);
#1569=ORIENTED_EDGE('',*,*,#3784,.T.);
#1570=ORIENTED_EDGE('',*,*,#3785,.T.);
#1571=ORIENTED_EDGE('',*,*,#3786,.T.);
#1572=ORIENTED_EDGE('',*,*,#3786,.F.);
#1573=ORIENTED_EDGE('',*,*,#3787,.F.);
#1574=ORIENTED_EDGE('',*,*,#3788,.F.);
#1575=ORIENTED_EDGE('',*,*,#3789,.F.);
#1576=ORIENTED_EDGE('',*,*,#3790,.F.);
#1577=ORIENTED_EDGE('',*,*,#3510,.F.);
#1578=ORIENTED_EDGE('',*,*,#3791,.T.);
#1579=ORIENTED_EDGE('',*,*,#3792,.T.);
#1580=ORIENTED_EDGE('',*,*,#3553,.F.);
#1581=ORIENTED_EDGE('',*,*,#3511,.F.);
#1582=ORIENTED_EDGE('',*,*,#3790,.T.);
#1583=ORIENTED_EDGE('',*,*,#3793,.F.);
#1584=ORIENTED_EDGE('',*,*,#3552,.F.);
#1585=ORIENTED_EDGE('',*,*,#3554,.F.);
#1586=ORIENTED_EDGE('',*,*,#3792,.F.);
#1587=ORIENTED_EDGE('',*,*,#3794,.T.);
#1588=ORIENTED_EDGE('',*,*,#3556,.F.);
#1589=ORIENTED_EDGE('',*,*,#3795,.F.);
#1590=ORIENTED_EDGE('',*,*,#3562,.T.);
#1591=ORIENTED_EDGE('',*,*,#3557,.F.);
#1592=ORIENTED_EDGE('',*,*,#3796,.F.);
#1593=ORIENTED_EDGE('',*,*,#3563,.F.);
#1594=ORIENTED_EDGE('',*,*,#3560,.T.);
#1595=ORIENTED_EDGE('',*,*,#3797,.F.);
#1596=ORIENTED_EDGE('',*,*,#3798,.F.);
#1597=ORIENTED_EDGE('',*,*,#3799,.T.);
#1598=ORIENTED_EDGE('',*,*,#3800,.T.);
#1599=ORIENTED_EDGE('',*,*,#3801,.T.);
#1600=ORIENTED_EDGE('',*,*,#3668,.T.);
#1601=ORIENTED_EDGE('',*,*,#3802,.T.);
#1602=ORIENTED_EDGE('',*,*,#3803,.T.);
#1603=ORIENTED_EDGE('',*,*,#3804,.T.);
#1604=ORIENTED_EDGE('',*,*,#3656,.T.);
#1605=ORIENTED_EDGE('',*,*,#3805,.T.);
#1606=ORIENTED_EDGE('',*,*,#3806,.T.);
#1607=ORIENTED_EDGE('',*,*,#3807,.T.);
#1608=ORIENTED_EDGE('',*,*,#3644,.T.);
#1609=ORIENTED_EDGE('',*,*,#3808,.T.);
#1610=ORIENTED_EDGE('',*,*,#3809,.T.);
#1611=ORIENTED_EDGE('',*,*,#3810,.T.);
#1612=ORIENTED_EDGE('',*,*,#3632,.T.);
#1613=ORIENTED_EDGE('',*,*,#3811,.T.);
#1614=ORIENTED_EDGE('',*,*,#3812,.T.);
#1615=ORIENTED_EDGE('',*,*,#3813,.T.);
#1616=ORIENTED_EDGE('',*,*,#3620,.T.);
#1617=ORIENTED_EDGE('',*,*,#3814,.T.);
#1618=ORIENTED_EDGE('',*,*,#3815,.T.);
#1619=ORIENTED_EDGE('',*,*,#3816,.T.);
#1620=ORIENTED_EDGE('',*,*,#3608,.T.);
#1621=ORIENTED_EDGE('',*,*,#3817,.T.);
#1622=ORIENTED_EDGE('',*,*,#3818,.T.);
#1623=ORIENTED_EDGE('',*,*,#3819,.T.);
#1624=ORIENTED_EDGE('',*,*,#3596,.T.);
#1625=ORIENTED_EDGE('',*,*,#3820,.T.);
#1626=ORIENTED_EDGE('',*,*,#3821,.T.);
#1627=ORIENTED_EDGE('',*,*,#3822,.T.);
#1628=ORIENTED_EDGE('',*,*,#3584,.T.);
#1629=ORIENTED_EDGE('',*,*,#3823,.T.);
#1630=ORIENTED_EDGE('',*,*,#3824,.T.);
#1631=ORIENTED_EDGE('',*,*,#3825,.T.);
#1632=ORIENTED_EDGE('',*,*,#3572,.T.);
#1633=ORIENTED_EDGE('',*,*,#3826,.T.);
#1634=ORIENTED_EDGE('',*,*,#3827,.T.);
#1635=ORIENTED_EDGE('',*,*,#3797,.T.);
#1636=ORIENTED_EDGE('',*,*,#3559,.T.);
#1637=ORIENTED_EDGE('',*,*,#3795,.T.);
#1638=ORIENTED_EDGE('',*,*,#3828,.T.);
#1639=ORIENTED_EDGE('',*,*,#3829,.T.);
#1640=ORIENTED_EDGE('',*,*,#3788,.T.);
#1641=ORIENTED_EDGE('',*,*,#3830,.T.);
#1642=ORIENTED_EDGE('',*,*,#3831,.T.);
#1643=ORIENTED_EDGE('',*,*,#3832,.T.);
#1644=ORIENTED_EDGE('',*,*,#3776,.T.);
#1645=ORIENTED_EDGE('',*,*,#3833,.T.);
#1646=ORIENTED_EDGE('',*,*,#3834,.T.);
#1647=ORIENTED_EDGE('',*,*,#3835,.T.);
#1648=ORIENTED_EDGE('',*,*,#3764,.T.);
#1649=ORIENTED_EDGE('',*,*,#3836,.T.);
#1650=ORIENTED_EDGE('',*,*,#3837,.T.);
#1651=ORIENTED_EDGE('',*,*,#3838,.T.);
#1652=ORIENTED_EDGE('',*,*,#3752,.T.);
#1653=ORIENTED_EDGE('',*,*,#3839,.T.);
#1654=ORIENTED_EDGE('',*,*,#3840,.T.);
#1655=ORIENTED_EDGE('',*,*,#3841,.T.);
#1656=ORIENTED_EDGE('',*,*,#3740,.T.);
#1657=ORIENTED_EDGE('',*,*,#3842,.T.);
#1658=ORIENTED_EDGE('',*,*,#3843,.T.);
#1659=ORIENTED_EDGE('',*,*,#3844,.T.);
#1660=ORIENTED_EDGE('',*,*,#3728,.T.);
#1661=ORIENTED_EDGE('',*,*,#3845,.T.);
#1662=ORIENTED_EDGE('',*,*,#3846,.T.);
#1663=ORIENTED_EDGE('',*,*,#3847,.T.);
#1664=ORIENTED_EDGE('',*,*,#3716,.T.);
#1665=ORIENTED_EDGE('',*,*,#3848,.T.);
#1666=ORIENTED_EDGE('',*,*,#3849,.T.);
#1667=ORIENTED_EDGE('',*,*,#3850,.T.);
#1668=ORIENTED_EDGE('',*,*,#3704,.T.);
#1669=ORIENTED_EDGE('',*,*,#3851,.T.);
#1670=ORIENTED_EDGE('',*,*,#3852,.T.);
#1671=ORIENTED_EDGE('',*,*,#3853,.T.);
#1672=ORIENTED_EDGE('',*,*,#3692,.T.);
#1673=ORIENTED_EDGE('',*,*,#3854,.T.);
#1674=ORIENTED_EDGE('',*,*,#3855,.T.);
#1675=ORIENTED_EDGE('',*,*,#3856,.T.);
#1676=ORIENTED_EDGE('',*,*,#3680,.T.);
#1677=ORIENTED_EDGE('',*,*,#3857,.T.);
#1678=ORIENTED_EDGE('',*,*,#3564,.F.);
#1679=ORIENTED_EDGE('',*,*,#3858,.T.);
#1680=ORIENTED_EDGE('',*,*,#3568,.F.);
#1681=ORIENTED_EDGE('',*,*,#3566,.F.);
#1682=ORIENTED_EDGE('',*,*,#3826,.F.);
#1683=ORIENTED_EDGE('',*,*,#3571,.T.);
#1684=ORIENTED_EDGE('',*,*,#3569,.F.);
#1685=ORIENTED_EDGE('',*,*,#3859,.F.);
#1686=ORIENTED_EDGE('',*,*,#3575,.F.);
#1687=ORIENTED_EDGE('',*,*,#3573,.T.);
#1688=ORIENTED_EDGE('',*,*,#3825,.F.);
#1689=ORIENTED_EDGE('',*,*,#3860,.F.);
#1690=ORIENTED_EDGE('',*,*,#3576,.F.);
#1691=ORIENTED_EDGE('',*,*,#3861,.T.);
#1692=ORIENTED_EDGE('',*,*,#3580,.F.);
#1693=ORIENTED_EDGE('',*,*,#3578,.F.);
#1694=ORIENTED_EDGE('',*,*,#3823,.F.);
#1695=ORIENTED_EDGE('',*,*,#3583,.T.);
#1696=ORIENTED_EDGE('',*,*,#3581,.F.);
#1697=ORIENTED_EDGE('',*,*,#3862,.F.);
#1698=ORIENTED_EDGE('',*,*,#3587,.F.);
#1699=ORIENTED_EDGE('',*,*,#3585,.T.);
#1700=ORIENTED_EDGE('',*,*,#3822,.F.);
#1701=ORIENTED_EDGE('',*,*,#3863,.F.);
#1702=ORIENTED_EDGE('',*,*,#3588,.F.);
#1703=ORIENTED_EDGE('',*,*,#3864,.T.);
#1704=ORIENTED_EDGE('',*,*,#3592,.F.);
#1705=ORIENTED_EDGE('',*,*,#3590,.F.);
#1706=ORIENTED_EDGE('',*,*,#3820,.F.);
#1707=ORIENTED_EDGE('',*,*,#3595,.T.);
#1708=ORIENTED_EDGE('',*,*,#3593,.F.);
#1709=ORIENTED_EDGE('',*,*,#3865,.F.);
#1710=ORIENTED_EDGE('',*,*,#3599,.F.);
#1711=ORIENTED_EDGE('',*,*,#3597,.T.);
#1712=ORIENTED_EDGE('',*,*,#3819,.F.);
#1713=ORIENTED_EDGE('',*,*,#3866,.F.);
#1714=ORIENTED_EDGE('',*,*,#3600,.F.);
#1715=ORIENTED_EDGE('',*,*,#3867,.T.);
#1716=ORIENTED_EDGE('',*,*,#3604,.F.);
#1717=ORIENTED_EDGE('',*,*,#3602,.F.);
#1718=ORIENTED_EDGE('',*,*,#3817,.F.);
#1719=ORIENTED_EDGE('',*,*,#3607,.T.);
#1720=ORIENTED_EDGE('',*,*,#3605,.F.);
#1721=ORIENTED_EDGE('',*,*,#3868,.F.);
#1722=ORIENTED_EDGE('',*,*,#3611,.F.);
#1723=ORIENTED_EDGE('',*,*,#3609,.T.);
#1724=ORIENTED_EDGE('',*,*,#3816,.F.);
#1725=ORIENTED_EDGE('',*,*,#3869,.F.);
#1726=ORIENTED_EDGE('',*,*,#3612,.F.);
#1727=ORIENTED_EDGE('',*,*,#3870,.T.);
#1728=ORIENTED_EDGE('',*,*,#3616,.F.);
#1729=ORIENTED_EDGE('',*,*,#3614,.F.);
#1730=ORIENTED_EDGE('',*,*,#3814,.F.);
#1731=ORIENTED_EDGE('',*,*,#3619,.T.);
#1732=ORIENTED_EDGE('',*,*,#3617,.F.);
#1733=ORIENTED_EDGE('',*,*,#3871,.F.);
#1734=ORIENTED_EDGE('',*,*,#3623,.F.);
#1735=ORIENTED_EDGE('',*,*,#3621,.T.);
#1736=ORIENTED_EDGE('',*,*,#3813,.F.);
#1737=ORIENTED_EDGE('',*,*,#3872,.F.);
#1738=ORIENTED_EDGE('',*,*,#3624,.F.);
#1739=ORIENTED_EDGE('',*,*,#3873,.T.);
#1740=ORIENTED_EDGE('',*,*,#3628,.F.);
#1741=ORIENTED_EDGE('',*,*,#3626,.F.);
#1742=ORIENTED_EDGE('',*,*,#3811,.F.);
#1743=ORIENTED_EDGE('',*,*,#3631,.T.);
#1744=ORIENTED_EDGE('',*,*,#3629,.F.);
#1745=ORIENTED_EDGE('',*,*,#3874,.F.);
#1746=ORIENTED_EDGE('',*,*,#3635,.F.);
#1747=ORIENTED_EDGE('',*,*,#3633,.T.);
#1748=ORIENTED_EDGE('',*,*,#3810,.F.);
#1749=ORIENTED_EDGE('',*,*,#3875,.F.);
#1750=ORIENTED_EDGE('',*,*,#3636,.F.);
#1751=ORIENTED_EDGE('',*,*,#3876,.T.);
#1752=ORIENTED_EDGE('',*,*,#3640,.F.);
#1753=ORIENTED_EDGE('',*,*,#3638,.F.);
#1754=ORIENTED_EDGE('',*,*,#3808,.F.);
#1755=ORIENTED_EDGE('',*,*,#3643,.T.);
#1756=ORIENTED_EDGE('',*,*,#3641,.F.);
#1757=ORIENTED_EDGE('',*,*,#3877,.F.);
#1758=ORIENTED_EDGE('',*,*,#3647,.F.);
#1759=ORIENTED_EDGE('',*,*,#3645,.T.);
#1760=ORIENTED_EDGE('',*,*,#3807,.F.);
#1761=ORIENTED_EDGE('',*,*,#3878,.F.);
#1762=ORIENTED_EDGE('',*,*,#3648,.F.);
#1763=ORIENTED_EDGE('',*,*,#3879,.T.);
#1764=ORIENTED_EDGE('',*,*,#3652,.F.);
#1765=ORIENTED_EDGE('',*,*,#3650,.F.);
#1766=ORIENTED_EDGE('',*,*,#3805,.F.);
#1767=ORIENTED_EDGE('',*,*,#3655,.T.);
#1768=ORIENTED_EDGE('',*,*,#3653,.F.);
#1769=ORIENTED_EDGE('',*,*,#3880,.F.);
#1770=ORIENTED_EDGE('',*,*,#3659,.F.);
#1771=ORIENTED_EDGE('',*,*,#3657,.T.);
#1772=ORIENTED_EDGE('',*,*,#3804,.F.);
#1773=ORIENTED_EDGE('',*,*,#3881,.F.);
#1774=ORIENTED_EDGE('',*,*,#3660,.F.);
#1775=ORIENTED_EDGE('',*,*,#3882,.T.);
#1776=ORIENTED_EDGE('',*,*,#3664,.F.);
#1777=ORIENTED_EDGE('',*,*,#3662,.F.);
#1778=ORIENTED_EDGE('',*,*,#3802,.F.);
#1779=ORIENTED_EDGE('',*,*,#3667,.T.);
#1780=ORIENTED_EDGE('',*,*,#3665,.F.);
#1781=ORIENTED_EDGE('',*,*,#3883,.F.);
#1782=ORIENTED_EDGE('',*,*,#3671,.F.);
#1783=ORIENTED_EDGE('',*,*,#3669,.T.);
#1784=ORIENTED_EDGE('',*,*,#3801,.F.);
#1785=ORIENTED_EDGE('',*,*,#3884,.F.);
#1786=ORIENTED_EDGE('',*,*,#3672,.F.);
#1787=ORIENTED_EDGE('',*,*,#3885,.T.);
#1788=ORIENTED_EDGE('',*,*,#3676,.F.);
#1789=ORIENTED_EDGE('',*,*,#3674,.F.);
#1790=ORIENTED_EDGE('',*,*,#3799,.F.);
#1791=ORIENTED_EDGE('',*,*,#3679,.T.);
#1792=ORIENTED_EDGE('',*,*,#3677,.F.);
#1793=ORIENTED_EDGE('',*,*,#3886,.F.);
#1794=ORIENTED_EDGE('',*,*,#3683,.F.);
#1795=ORIENTED_EDGE('',*,*,#3681,.T.);
#1796=ORIENTED_EDGE('',*,*,#3856,.F.);
#1797=ORIENTED_EDGE('',*,*,#3887,.F.);
#1798=ORIENTED_EDGE('',*,*,#3684,.F.);
#1799=ORIENTED_EDGE('',*,*,#3888,.T.);
#1800=ORIENTED_EDGE('',*,*,#3688,.F.);
#1801=ORIENTED_EDGE('',*,*,#3686,.F.);
#1802=ORIENTED_EDGE('',*,*,#3854,.F.);
#1803=ORIENTED_EDGE('',*,*,#3691,.T.);
#1804=ORIENTED_EDGE('',*,*,#3689,.F.);
#1805=ORIENTED_EDGE('',*,*,#3889,.F.);
#1806=ORIENTED_EDGE('',*,*,#3695,.F.);
#1807=ORIENTED_EDGE('',*,*,#3693,.T.);
#1808=ORIENTED_EDGE('',*,*,#3853,.F.);
#1809=ORIENTED_EDGE('',*,*,#3890,.F.);
#1810=ORIENTED_EDGE('',*,*,#3696,.F.);
#1811=ORIENTED_EDGE('',*,*,#3891,.T.);
#1812=ORIENTED_EDGE('',*,*,#3700,.F.);
#1813=ORIENTED_EDGE('',*,*,#3698,.F.);
#1814=ORIENTED_EDGE('',*,*,#3851,.F.);
#1815=ORIENTED_EDGE('',*,*,#3703,.T.);
#1816=ORIENTED_EDGE('',*,*,#3701,.F.);
#1817=ORIENTED_EDGE('',*,*,#3892,.F.);
#1818=ORIENTED_EDGE('',*,*,#3707,.F.);
#1819=ORIENTED_EDGE('',*,*,#3705,.T.);
#1820=ORIENTED_EDGE('',*,*,#3850,.F.);
#1821=ORIENTED_EDGE('',*,*,#3893,.F.);
#1822=ORIENTED_EDGE('',*,*,#3708,.F.);
#1823=ORIENTED_EDGE('',*,*,#3894,.T.);
#1824=ORIENTED_EDGE('',*,*,#3712,.F.);
#1825=ORIENTED_EDGE('',*,*,#3710,.F.);
#1826=ORIENTED_EDGE('',*,*,#3848,.F.);
#1827=ORIENTED_EDGE('',*,*,#3715,.T.);
#1828=ORIENTED_EDGE('',*,*,#3713,.F.);
#1829=ORIENTED_EDGE('',*,*,#3895,.F.);
#1830=ORIENTED_EDGE('',*,*,#3719,.F.);
#1831=ORIENTED_EDGE('',*,*,#3717,.T.);
#1832=ORIENTED_EDGE('',*,*,#3847,.F.);
#1833=ORIENTED_EDGE('',*,*,#3896,.F.);
#1834=ORIENTED_EDGE('',*,*,#3720,.F.);
#1835=ORIENTED_EDGE('',*,*,#3897,.T.);
#1836=ORIENTED_EDGE('',*,*,#3724,.F.);
#1837=ORIENTED_EDGE('',*,*,#3722,.F.);
#1838=ORIENTED_EDGE('',*,*,#3845,.F.);
#1839=ORIENTED_EDGE('',*,*,#3727,.T.);
#1840=ORIENTED_EDGE('',*,*,#3725,.F.);
#1841=ORIENTED_EDGE('',*,*,#3898,.F.);
#1842=ORIENTED_EDGE('',*,*,#3731,.F.);
#1843=ORIENTED_EDGE('',*,*,#3729,.T.);
#1844=ORIENTED_EDGE('',*,*,#3844,.F.);
#1845=ORIENTED_EDGE('',*,*,#3899,.F.);
#1846=ORIENTED_EDGE('',*,*,#3732,.F.);
#1847=ORIENTED_EDGE('',*,*,#3900,.T.);
#1848=ORIENTED_EDGE('',*,*,#3736,.F.);
#1849=ORIENTED_EDGE('',*,*,#3734,.F.);
#1850=ORIENTED_EDGE('',*,*,#3842,.F.);
#1851=ORIENTED_EDGE('',*,*,#3739,.T.);
#1852=ORIENTED_EDGE('',*,*,#3737,.F.);
#1853=ORIENTED_EDGE('',*,*,#3901,.F.);
#1854=ORIENTED_EDGE('',*,*,#3743,.F.);
#1855=ORIENTED_EDGE('',*,*,#3741,.T.);
#1856=ORIENTED_EDGE('',*,*,#3841,.F.);
#1857=ORIENTED_EDGE('',*,*,#3902,.F.);
#1858=ORIENTED_EDGE('',*,*,#3744,.F.);
#1859=ORIENTED_EDGE('',*,*,#3903,.T.);
#1860=ORIENTED_EDGE('',*,*,#3748,.F.);
#1861=ORIENTED_EDGE('',*,*,#3746,.F.);
#1862=ORIENTED_EDGE('',*,*,#3839,.F.);
#1863=ORIENTED_EDGE('',*,*,#3751,.T.);
#1864=ORIENTED_EDGE('',*,*,#3749,.F.);
#1865=ORIENTED_EDGE('',*,*,#3904,.F.);
#1866=ORIENTED_EDGE('',*,*,#3755,.F.);
#1867=ORIENTED_EDGE('',*,*,#3753,.T.);
#1868=ORIENTED_EDGE('',*,*,#3838,.F.);
#1869=ORIENTED_EDGE('',*,*,#3905,.F.);
#1870=ORIENTED_EDGE('',*,*,#3756,.F.);
#1871=ORIENTED_EDGE('',*,*,#3906,.T.);
#1872=ORIENTED_EDGE('',*,*,#3760,.F.);
#1873=ORIENTED_EDGE('',*,*,#3758,.F.);
#1874=ORIENTED_EDGE('',*,*,#3836,.F.);
#1875=ORIENTED_EDGE('',*,*,#3763,.T.);
#1876=ORIENTED_EDGE('',*,*,#3761,.F.);
#1877=ORIENTED_EDGE('',*,*,#3907,.F.);
#1878=ORIENTED_EDGE('',*,*,#3767,.F.);
#1879=ORIENTED_EDGE('',*,*,#3765,.T.);
#1880=ORIENTED_EDGE('',*,*,#3835,.F.);
#1881=ORIENTED_EDGE('',*,*,#3908,.F.);
#1882=ORIENTED_EDGE('',*,*,#3768,.F.);
#1883=ORIENTED_EDGE('',*,*,#3909,.T.);
#1884=ORIENTED_EDGE('',*,*,#3772,.F.);
#1885=ORIENTED_EDGE('',*,*,#3770,.F.);
#1886=ORIENTED_EDGE('',*,*,#3833,.F.);
#1887=ORIENTED_EDGE('',*,*,#3775,.T.);
#1888=ORIENTED_EDGE('',*,*,#3773,.F.);
#1889=ORIENTED_EDGE('',*,*,#3910,.F.);
#1890=ORIENTED_EDGE('',*,*,#3779,.F.);
#1891=ORIENTED_EDGE('',*,*,#3777,.T.);
#1892=ORIENTED_EDGE('',*,*,#3832,.F.);
#1893=ORIENTED_EDGE('',*,*,#3911,.F.);
#1894=ORIENTED_EDGE('',*,*,#3780,.F.);
#1895=ORIENTED_EDGE('',*,*,#3912,.T.);
#1896=ORIENTED_EDGE('',*,*,#3784,.F.);
#1897=ORIENTED_EDGE('',*,*,#3782,.F.);
#1898=ORIENTED_EDGE('',*,*,#3830,.F.);
#1899=ORIENTED_EDGE('',*,*,#3787,.T.);
#1900=ORIENTED_EDGE('',*,*,#3785,.F.);
#1901=ORIENTED_EDGE('',*,*,#3913,.F.);
#1902=ORIENTED_EDGE('',*,*,#3791,.F.);
#1903=ORIENTED_EDGE('',*,*,#3789,.T.);
#1904=ORIENTED_EDGE('',*,*,#3829,.F.);
#1905=ORIENTED_EDGE('',*,*,#3914,.F.);
#1906=ORIENTED_EDGE('',*,*,#3793,.T.);
#1907=ORIENTED_EDGE('',*,*,#3915,.T.);
#1908=ORIENTED_EDGE('',*,*,#3794,.F.);
#1909=ORIENTED_EDGE('',*,*,#3914,.T.);
#1910=ORIENTED_EDGE('',*,*,#3828,.F.);
#1911=ORIENTED_EDGE('',*,*,#3796,.T.);
#1912=ORIENTED_EDGE('',*,*,#3858,.F.);
#1913=ORIENTED_EDGE('',*,*,#3798,.T.);
#1914=ORIENTED_EDGE('',*,*,#3827,.F.);
#1915=ORIENTED_EDGE('',*,*,#3859,.T.);
#1916=ORIENTED_EDGE('',*,*,#3857,.F.);
#1917=ORIENTED_EDGE('',*,*,#3916,.F.);
#1918=ORIENTED_EDGE('',*,*,#3885,.F.);
#1919=ORIENTED_EDGE('',*,*,#3884,.T.);
#1920=ORIENTED_EDGE('',*,*,#3800,.F.);
#1921=ORIENTED_EDGE('',*,*,#3886,.T.);
#1922=ORIENTED_EDGE('',*,*,#3882,.F.);
#1923=ORIENTED_EDGE('',*,*,#3881,.T.);
#1924=ORIENTED_EDGE('',*,*,#3803,.F.);
#1925=ORIENTED_EDGE('',*,*,#3883,.T.);
#1926=ORIENTED_EDGE('',*,*,#3879,.F.);
#1927=ORIENTED_EDGE('',*,*,#3878,.T.);
#1928=ORIENTED_EDGE('',*,*,#3806,.F.);
#1929=ORIENTED_EDGE('',*,*,#3880,.T.);
#1930=ORIENTED_EDGE('',*,*,#3876,.F.);
#1931=ORIENTED_EDGE('',*,*,#3875,.T.);
#1932=ORIENTED_EDGE('',*,*,#3809,.F.);
#1933=ORIENTED_EDGE('',*,*,#3877,.T.);
#1934=ORIENTED_EDGE('',*,*,#3873,.F.);
#1935=ORIENTED_EDGE('',*,*,#3872,.T.);
#1936=ORIENTED_EDGE('',*,*,#3812,.F.);
#1937=ORIENTED_EDGE('',*,*,#3874,.T.);
#1938=ORIENTED_EDGE('',*,*,#3870,.F.);
#1939=ORIENTED_EDGE('',*,*,#3869,.T.);
#1940=ORIENTED_EDGE('',*,*,#3815,.F.);
#1941=ORIENTED_EDGE('',*,*,#3871,.T.);
#1942=ORIENTED_EDGE('',*,*,#3867,.F.);
#1943=ORIENTED_EDGE('',*,*,#3866,.T.);
#1944=ORIENTED_EDGE('',*,*,#3818,.F.);
#1945=ORIENTED_EDGE('',*,*,#3868,.T.);
#1946=ORIENTED_EDGE('',*,*,#3864,.F.);
#1947=ORIENTED_EDGE('',*,*,#3863,.T.);
#1948=ORIENTED_EDGE('',*,*,#3821,.F.);
#1949=ORIENTED_EDGE('',*,*,#3865,.T.);
#1950=ORIENTED_EDGE('',*,*,#3861,.F.);
#1951=ORIENTED_EDGE('',*,*,#3860,.T.);
#1952=ORIENTED_EDGE('',*,*,#3824,.F.);
#1953=ORIENTED_EDGE('',*,*,#3862,.T.);
#1954=ORIENTED_EDGE('',*,*,#3912,.F.);
#1955=ORIENTED_EDGE('',*,*,#3911,.T.);
#1956=ORIENTED_EDGE('',*,*,#3831,.F.);
#1957=ORIENTED_EDGE('',*,*,#3913,.T.);
#1958=ORIENTED_EDGE('',*,*,#3909,.F.);
#1959=ORIENTED_EDGE('',*,*,#3908,.T.);
#1960=ORIENTED_EDGE('',*,*,#3834,.F.);
#1961=ORIENTED_EDGE('',*,*,#3910,.T.);
#1962=ORIENTED_EDGE('',*,*,#3906,.F.);
#1963=ORIENTED_EDGE('',*,*,#3905,.T.);
#1964=ORIENTED_EDGE('',*,*,#3837,.F.);
#1965=ORIENTED_EDGE('',*,*,#3907,.T.);
#1966=ORIENTED_EDGE('',*,*,#3903,.F.);
#1967=ORIENTED_EDGE('',*,*,#3902,.T.);
#1968=ORIENTED_EDGE('',*,*,#3840,.F.);
#1969=ORIENTED_EDGE('',*,*,#3904,.T.);
#1970=ORIENTED_EDGE('',*,*,#3900,.F.);
#1971=ORIENTED_EDGE('',*,*,#3899,.T.);
#1972=ORIENTED_EDGE('',*,*,#3843,.F.);
#1973=ORIENTED_EDGE('',*,*,#3901,.T.);
#1974=ORIENTED_EDGE('',*,*,#3897,.F.);
#1975=ORIENTED_EDGE('',*,*,#3896,.T.);
#1976=ORIENTED_EDGE('',*,*,#3846,.F.);
#1977=ORIENTED_EDGE('',*,*,#3898,.T.);
#1978=ORIENTED_EDGE('',*,*,#3894,.F.);
#1979=ORIENTED_EDGE('',*,*,#3893,.T.);
#1980=ORIENTED_EDGE('',*,*,#3849,.F.);
#1981=ORIENTED_EDGE('',*,*,#3895,.T.);
#1982=ORIENTED_EDGE('',*,*,#3891,.F.);
#1983=ORIENTED_EDGE('',*,*,#3890,.T.);
#1984=ORIENTED_EDGE('',*,*,#3852,.F.);
#1985=ORIENTED_EDGE('',*,*,#3892,.T.);
#1986=ORIENTED_EDGE('',*,*,#3888,.F.);
#1987=ORIENTED_EDGE('',*,*,#3887,.T.);
#1988=ORIENTED_EDGE('',*,*,#3855,.F.);
#1989=ORIENTED_EDGE('',*,*,#3889,.T.);
#1990=ORIENTED_EDGE('',*,*,#3915,.F.);
#1991=ORIENTED_EDGE('',*,*,#3917,.F.);
#1992=ORIENTED_EDGE('',*,*,#3916,.T.);
#1993=ORIENTED_EDGE('',*,*,#3917,.T.);
#3468=EDGE_CURVE('',#4655,#4655,#5499,.F.);
#3469=EDGE_CURVE('',#4656,#4656,#5500,.T.);
#3470=EDGE_CURVE('',#4657,#4657,#5501,.T.);
#3471=EDGE_CURVE('',#4658,#4658,#5502,.F.);
#3472=EDGE_CURVE('',#4659,#4660,#5503,.F.);
#3473=EDGE_CURVE('',#4660,#4661,#155,.F.);
#3474=EDGE_CURVE('',#4661,#4662,#5504,.F.);
#3475=EDGE_CURVE('',#4662,#4663,#156,.F.);
#3476=EDGE_CURVE('',#4663,#4664,#5505,.F.);
#3477=EDGE_CURVE('',#4664,#4665,#157,.F.);
#3478=EDGE_CURVE('',#4665,#4666,#5506,.F.);
#3479=EDGE_CURVE('',#4666,#4667,#158,.F.);
#3480=EDGE_CURVE('',#4667,#4668,#5507,.F.);
#3481=EDGE_CURVE('',#4668,#4669,#159,.F.);
#3482=EDGE_CURVE('',#4669,#4670,#5508,.F.);
#3483=EDGE_CURVE('',#4670,#4671,#160,.F.);
#3484=EDGE_CURVE('',#4671,#4672,#5509,.F.);
#3485=EDGE_CURVE('',#4672,#4673,#161,.F.);
#3486=EDGE_CURVE('',#4673,#4674,#5510,.F.);
#3487=EDGE_CURVE('',#4674,#4675,#162,.F.);
#3488=EDGE_CURVE('',#4675,#4676,#5511,.F.);
#3489=EDGE_CURVE('',#4676,#4677,#163,.F.);
#3490=EDGE_CURVE('',#4677,#4678,#5512,.F.);
#3491=EDGE_CURVE('',#4678,#4679,#164,.F.);
#3492=EDGE_CURVE('',#4679,#4680,#5513,.F.);
#3493=EDGE_CURVE('',#4680,#4681,#165,.F.);
#3494=EDGE_CURVE('',#4681,#4682,#5514,.F.);
#3495=EDGE_CURVE('',#4682,#4683,#166,.F.);
#3496=EDGE_CURVE('',#4683,#4684,#5515,.F.);
#3497=EDGE_CURVE('',#4684,#4685,#167,.F.);
#3498=EDGE_CURVE('',#4685,#4686,#5516,.F.);
#3499=EDGE_CURVE('',#4686,#4687,#168,.F.);
#3500=EDGE_CURVE('',#4687,#4688,#5517,.F.);
#3501=EDGE_CURVE('',#4688,#4689,#169,.F.);
#3502=EDGE_CURVE('',#4689,#4690,#5518,.F.);
#3503=EDGE_CURVE('',#4690,#4691,#170,.F.);
#3504=EDGE_CURVE('',#4691,#4692,#5519,.F.);
#3505=EDGE_CURVE('',#4692,#4693,#171,.F.);
#3506=EDGE_CURVE('',#4693,#4694,#5520,.F.);
#3507=EDGE_CURVE('',#4694,#4695,#172,.F.);
#3508=EDGE_CURVE('',#4695,#4696,#5521,.F.);
#3509=EDGE_CURVE('',#4696,#4697,#173,.F.);
#3510=EDGE_CURVE('',#4697,#4698,#5522,.F.);
#3511=EDGE_CURVE('',#4698,#4699,#174,.F.);
#3512=EDGE_CURVE('',#4699,#4700,#5523,.F.);
#3513=EDGE_CURVE('',#4700,#4701,#175,.F.);
#3514=EDGE_CURVE('',#4701,#4702,#5524,.F.);
#3515=EDGE_CURVE('',#4702,#4703,#176,.F.);
#3516=EDGE_CURVE('',#4703,#4704,#5525,.F.);
#3517=EDGE_CURVE('',#4704,#4705,#177,.F.);
#3518=EDGE_CURVE('',#4705,#4706,#5526,.F.);
#3519=EDGE_CURVE('',#4706,#4707,#178,.F.);
#3520=EDGE_CURVE('',#4707,#4708,#5527,.F.);
#3521=EDGE_CURVE('',#4708,#4709,#179,.F.);
#3522=EDGE_CURVE('',#4709,#4710,#5528,.F.);
#3523=EDGE_CURVE('',#4710,#4711,#180,.F.);
#3524=EDGE_CURVE('',#4711,#4712,#5529,.F.);
#3525=EDGE_CURVE('',#4712,#4713,#181,.F.);
#3526=EDGE_CURVE('',#4713,#4714,#5530,.F.);
#3527=EDGE_CURVE('',#4714,#4715,#182,.F.);
#3528=EDGE_CURVE('',#4715,#4716,#5531,.F.);
#3529=EDGE_CURVE('',#4716,#4717,#183,.F.);
#3530=EDGE_CURVE('',#4717,#4718,#5532,.F.);
#3531=EDGE_CURVE('',#4718,#4719,#184,.F.);
#3532=EDGE_CURVE('',#4719,#4720,#5533,.F.);
#3533=EDGE_CURVE('',#4720,#4721,#185,.F.);
#3534=EDGE_CURVE('',#4721,#4722,#5534,.F.);
#3535=EDGE_CURVE('',#4722,#4723,#186,.F.);
#3536=EDGE_CURVE('',#4723,#4724,#5535,.F.);
#3537=EDGE_CURVE('',#4724,#4725,#187,.F.);
#3538=EDGE_CURVE('',#4725,#4726,#5536,.F.);
#3539=EDGE_CURVE('',#4726,#4727,#188,.F.);
#3540=EDGE_CURVE('',#4727,#4728,#5537,.F.);
#3541=EDGE_CURVE('',#4728,#4729,#189,.F.);
#3542=EDGE_CURVE('',#4729,#4730,#5538,.F.);
#3543=EDGE_CURVE('',#4730,#4731,#190,.F.);
#3544=EDGE_CURVE('',#4731,#4732,#5539,.F.);
#3545=EDGE_CURVE('',#4732,#4733,#191,.F.);
#3546=EDGE_CURVE('',#4733,#4734,#5540,.F.);
#3547=EDGE_CURVE('',#4734,#4735,#192,.F.);
#3548=EDGE_CURVE('',#4735,#4736,#5541,.F.);
#3549=EDGE_CURVE('',#4736,#4737,#193,.F.);
#3550=EDGE_CURVE('',#4737,#4738,#5542,.F.);
#3551=EDGE_CURVE('',#4738,#4659,#194,.F.);
#3552=EDGE_CURVE('',#4739,#4739,#5543,.T.);
#3553=EDGE_CURVE('',#4699,#4740,#195,.T.);
#3554=EDGE_CURVE('',#4740,#4741,#5544,.T.);
#3555=EDGE_CURVE('',#4741,#4700,#196,.T.);
#3556=EDGE_CURVE('',#4741,#4742,#197,.T.);
#3557=EDGE_CURVE('',#4742,#4743,#198,.T.);
#3558=EDGE_CURVE('',#4743,#4701,#199,.T.);
#3559=EDGE_CURVE('',#4744,#4745,#5545,.T.);
#3560=EDGE_CURVE('',#4746,#4744,#200,.T.);
#3561=EDGE_CURVE('',#4702,#4746,#201,.T.);
#3562=EDGE_CURVE('',#4745,#4743,#202,.T.);
#3563=EDGE_CURVE('',#4746,#4747,#203,.T.);
#3564=EDGE_CURVE('',#4747,#4748,#204,.T.);
#3565=EDGE_CURVE('',#4748,#4703,#205,.T.);
#3566=EDGE_CURVE('',#4748,#4749,#5546,.T.);
#3567=EDGE_CURVE('',#4749,#4704,#206,.T.);
#3568=EDGE_CURVE('',#4749,#4750,#207,.T.);
#3569=EDGE_CURVE('',#4750,#4751,#208,.T.);
#3570=EDGE_CURVE('',#4751,#4705,#209,.T.);
#3571=EDGE_CURVE('',#4752,#4751,#210,.T.);
#3572=EDGE_CURVE('',#4753,#4752,#5547,.T.);
#3573=EDGE_CURVE('',#4754,#4753,#211,.T.);
#3574=EDGE_CURVE('',#4706,#4754,#212,.T.);
#3575=EDGE_CURVE('',#4754,#4755,#213,.T.);
#3576=EDGE_CURVE('',#4755,#4756,#214,.T.);
#3577=EDGE_CURVE('',#4756,#4707,#215,.T.);
#3578=EDGE_CURVE('',#4756,#4757,#5548,.T.);
#3579=EDGE_CURVE('',#4757,#4708,#216,.T.);
#3580=EDGE_CURVE('',#4757,#4758,#217,.T.);
#3581=EDGE_CURVE('',#4758,#4759,#218,.T.);
#3582=EDGE_CURVE('',#4759,#4709,#219,.T.);
#3583=EDGE_CURVE('',#4760,#4759,#220,.T.);
#3584=EDGE_CURVE('',#4761,#4760,#5549,.T.);
#3585=EDGE_CURVE('',#4762,#4761,#221,.T.);
#3586=EDGE_CURVE('',#4710,#4762,#222,.T.);
#3587=EDGE_CURVE('',#4762,#4763,#223,.T.);
#3588=EDGE_CURVE('',#4763,#4764,#224,.T.);
#3589=EDGE_CURVE('',#4764,#4711,#225,.T.);
#3590=EDGE_CURVE('',#4764,#4765,#5550,.T.);
#3591=EDGE_CURVE('',#4765,#4712,#226,.T.);
#3592=EDGE_CURVE('',#4765,#4766,#227,.T.);
#3593=EDGE_CURVE('',#4766,#4767,#228,.T.);
#3594=EDGE_CURVE('',#4767,#4713,#229,.T.);
#3595=EDGE_CURVE('',#4768,#4767,#230,.T.);
#3596=EDGE_CURVE('',#4769,#4768,#5551,.T.);
#3597=EDGE_CURVE('',#4770,#4769,#231,.T.);
#3598=EDGE_CURVE('',#4714,#4770,#232,.T.);
#3599=EDGE_CURVE('',#4770,#4771,#233,.T.);
#3600=EDGE_CURVE('',#4771,#4772,#234,.T.);
#3601=EDGE_CURVE('',#4772,#4715,#235,.T.);
#3602=EDGE_CURVE('',#4772,#4773,#5552,.T.);
#3603=EDGE_CURVE('',#4773,#4716,#236,.T.);
#3604=EDGE_CURVE('',#4773,#4774,#237,.T.);
#3605=EDGE_CURVE('',#4774,#4775,#238,.T.);
#3606=EDGE_CURVE('',#4775,#4717,#239,.T.);
#3607=EDGE_CURVE('',#4776,#4775,#240,.T.);
#3608=EDGE_CURVE('',#4777,#4776,#5553,.T.);
#3609=EDGE_CURVE('',#4778,#4777,#241,.T.);
#3610=EDGE_CURVE('',#4718,#4778,#242,.T.);
#3611=EDGE_CURVE('',#4778,#4779,#243,.T.);
#3612=EDGE_CURVE('',#4779,#4780,#244,.T.);
#3613=EDGE_CURVE('',#4780,#4719,#245,.T.);
#3614=EDGE_CURVE('',#4780,#4781,#5554,.T.);
#3615=EDGE_CURVE('',#4781,#4720,#246,.T.);
#3616=EDGE_CURVE('',#4781,#4782,#247,.T.);
#3617=EDGE_CURVE('',#4782,#4783,#248,.T.);
#3618=EDGE_CURVE('',#4783,#4721,#249,.T.);
#3619=EDGE_CURVE('',#4784,#4783,#250,.T.);
#3620=EDGE_CURVE('',#4785,#4784,#5555,.T.);
#3621=EDGE_CURVE('',#4786,#4785,#251,.T.);
#3622=EDGE_CURVE('',#4722,#4786,#252,.T.);
#3623=EDGE_CURVE('',#4786,#4787,#253,.T.);
#3624=EDGE_CURVE('',#4787,#4788,#254,.T.);
#3625=EDGE_CURVE('',#4788,#4723,#255,.T.);
#3626=EDGE_CURVE('',#4788,#4789,#5556,.T.);
#3627=EDGE_CURVE('',#4789,#4724,#256,.T.);
#3628=EDGE_CURVE('',#4789,#4790,#257,.T.);
#3629=EDGE_CURVE('',#4790,#4791,#258,.T.);
#3630=EDGE_CURVE('',#4791,#4725,#259,.T.);
#3631=EDGE_CURVE('',#4792,#4791,#260,.T.);
#3632=EDGE_CURVE('',#4793,#4792,#5557,.T.);
#3633=EDGE_CURVE('',#4794,#4793,#261,.T.);
#3634=EDGE_CURVE('',#4726,#4794,#262,.T.);
#3635=EDGE_CURVE('',#4794,#4795,#263,.T.);
#3636=EDGE_CURVE('',#4795,#4796,#264,.T.);
#3637=EDGE_CURVE('',#4796,#4727,#265,.T.);
#3638=EDGE_CURVE('',#4796,#4797,#5558,.T.);
#3639=EDGE_CURVE('',#4797,#4728,#266,.T.);
#3640=EDGE_CURVE('',#4797,#4798,#267,.T.);
#3641=EDGE_CURVE('',#4798,#4799,#268,.T.);
#3642=EDGE_CURVE('',#4799,#4729,#269,.T.);
#3643=EDGE_CURVE('',#4800,#4799,#270,.T.);
#3644=EDGE_CURVE('',#4801,#4800,#5559,.T.);
#3645=EDGE_CURVE('',#4802,#4801,#271,.T.);
#3646=EDGE_CURVE('',#4730,#4802,#272,.T.);
#3647=EDGE_CURVE('',#4802,#4803,#273,.T.);
#3648=EDGE_CURVE('',#4803,#4804,#274,.T.);
#3649=EDGE_CURVE('',#4804,#4731,#275,.T.);
#3650=EDGE_CURVE('',#4804,#4805,#5560,.T.);
#3651=EDGE_CURVE('',#4805,#4732,#276,.T.);
#3652=EDGE_CURVE('',#4805,#4806,#277,.T.);
#3653=EDGE_CURVE('',#4806,#4807,#278,.T.);
#3654=EDGE_CURVE('',#4807,#4733,#279,.T.);
#3655=EDGE_CURVE('',#4808,#4807,#280,.T.);
#3656=EDGE_CURVE('',#4809,#4808,#5561,.T.);
#3657=EDGE_CURVE('',#4810,#4809,#281,.T.);
#3658=EDGE_CURVE('',#4734,#4810,#282,.T.);
#3659=EDGE_CURVE('',#4810,#4811,#283,.T.);
#3660=EDGE_CURVE('',#4811,#4812,#284,.T.);
#3661=EDGE_CURVE('',#4812,#4735,#285,.T.);
#3662=EDGE_CURVE('',#4812,#4813,#5562,.T.);
#3663=EDGE_CURVE('',#4813,#4736,#286,.T.);
#3664=EDGE_CURVE('',#4813,#4814,#287,.T.);
#3665=EDGE_CURVE('',#4814,#4815,#288,.T.);
#3666=EDGE_CURVE('',#4815,#4737,#289,.T.);
#3667=EDGE_CURVE('',#4816,#4815,#290,.T.);
#3668=EDGE_CURVE('',#4817,#4816,#5563,.T.);
#3669=EDGE_CURVE('',#4818,#4817,#291,.T.);
#3670=EDGE_CURVE('',#4738,#4818,#292,.T.);
#3671=EDGE_CURVE('',#4818,#4819,#293,.T.);
#3672=EDGE_CURVE('',#4819,#4820,#294,.T.);
#3673=EDGE_CURVE('',#4820,#4659,#295,.T.);
#3674=EDGE_CURVE('',#4820,#4821,#5564,.T.);
#3675=EDGE_CURVE('',#4821,#4660,#296,.T.);
#3676=EDGE_CURVE('',#4821,#4822,#297,.T.);
#3677=EDGE_CURVE('',#4822,#4823,#298,.T.);
#3678=EDGE_CURVE('',#4823,#4661,#299,.T.);
#3679=EDGE_CURVE('',#4824,#4823,#300,.T.);
#3680=EDGE_CURVE('',#4825,#4824,#5565,.T.);
#3681=EDGE_CURVE('',#4826,#4825,#301,.T.);
#3682=EDGE_CURVE('',#4662,#4826,#302,.T.);
#3683=EDGE_CURVE('',#4826,#4827,#303,.T.);
#3684=EDGE_CURVE('',#4827,#4828,#304,.T.);
#3685=EDGE_CURVE('',#4828,#4663,#305,.T.);
#3686=EDGE_CURVE('',#4828,#4829,#5566,.T.);
#3687=EDGE_CURVE('',#4829,#4664,#306,.T.);
#3688=EDGE_CURVE('',#4829,#4830,#307,.T.);
#3689=EDGE_CURVE('',#4830,#4831,#308,.T.);
#3690=EDGE_CURVE('',#4831,#4665,#309,.T.);
#3691=EDGE_CURVE('',#4832,#4831,#310,.T.);
#3692=EDGE_CURVE('',#4833,#4832,#5567,.T.);
#3693=EDGE_CURVE('',#4834,#4833,#311,.T.);
#3694=EDGE_CURVE('',#4666,#4834,#312,.T.);
#3695=EDGE_CURVE('',#4834,#4835,#313,.T.);
#3696=EDGE_CURVE('',#4835,#4836,#314,.T.);
#3697=EDGE_CURVE('',#4836,#4667,#315,.T.);
#3698=EDGE_CURVE('',#4836,#4837,#5568,.T.);
#3699=EDGE_CURVE('',#4837,#4668,#316,.T.);
#3700=EDGE_CURVE('',#4837,#4838,#317,.T.);
#3701=EDGE_CURVE('',#4838,#4839,#318,.T.);
#3702=EDGE_CURVE('',#4839,#4669,#319,.T.);
#3703=EDGE_CURVE('',#4840,#4839,#320,.T.);
#3704=EDGE_CURVE('',#4841,#4840,#5569,.T.);
#3705=EDGE_CURVE('',#4842,#4841,#321,.T.);
#3706=EDGE_CURVE('',#4670,#4842,#322,.T.);
#3707=EDGE_CURVE('',#4842,#4843,#323,.T.);
#3708=EDGE_CURVE('',#4843,#4844,#324,.T.);
#3709=EDGE_CURVE('',#4844,#4671,#325,.T.);
#3710=EDGE_CURVE('',#4844,#4845,#5570,.T.);
#3711=EDGE_CURVE('',#4845,#4672,#326,.T.);
#3712=EDGE_CURVE('',#4845,#4846,#327,.T.);
#3713=EDGE_CURVE('',#4846,#4847,#328,.T.);
#3714=EDGE_CURVE('',#4847,#4673,#329,.T.);
#3715=EDGE_CURVE('',#4848,#4847,#330,.T.);
#3716=EDGE_CURVE('',#4849,#4848,#5571,.T.);
#3717=EDGE_CURVE('',#4850,#4849,#331,.T.);
#3718=EDGE_CURVE('',#4674,#4850,#332,.T.);
#3719=EDGE_CURVE('',#4850,#4851,#333,.T.);
#3720=EDGE_CURVE('',#4851,#4852,#334,.T.);
#3721=EDGE_CURVE('',#4852,#4675,#335,.T.);
#3722=EDGE_CURVE('',#4852,#4853,#5572,.T.);
#3723=EDGE_CURVE('',#4853,#4676,#336,.T.);
#3724=EDGE_CURVE('',#4853,#4854,#337,.T.);
#3725=EDGE_CURVE('',#4854,#4855,#338,.T.);
#3726=EDGE_CURVE('',#4855,#4677,#339,.T.);
#3727=EDGE_CURVE('',#4856,#4855,#340,.T.);
#3728=EDGE_CURVE('',#4857,#4856,#5573,.T.);
#3729=EDGE_CURVE('',#4858,#4857,#341,.T.);
#3730=EDGE_CURVE('',#4678,#4858,#342,.T.);
#3731=EDGE_CURVE('',#4858,#4859,#343,.T.);
#3732=EDGE_CURVE('',#4859,#4860,#344,.T.);
#3733=EDGE_CURVE('',#4860,#4679,#345,.T.);
#3734=EDGE_CURVE('',#4860,#4861,#5574,.T.);
#3735=EDGE_CURVE('',#4861,#4680,#346,.T.);
#3736=EDGE_CURVE('',#4861,#4862,#347,.T.);
#3737=EDGE_CURVE('',#4862,#4863,#348,.T.);
#3738=EDGE_CURVE('',#4863,#4681,#349,.T.);
#3739=EDGE_CURVE('',#4864,#4863,#350,.T.);
#3740=EDGE_CURVE('',#4865,#4864,#5575,.T.);
#3741=EDGE_CURVE('',#4866,#4865,#351,.T.);
#3742=EDGE_CURVE('',#4682,#4866,#352,.T.);
#3743=EDGE_CURVE('',#4866,#4867,#353,.T.);
#3744=EDGE_CURVE('',#4867,#4868,#354,.T.);
#3745=EDGE_CURVE('',#4868,#4683,#355,.T.);
#3746=EDGE_CURVE('',#4868,#4869,#5576,.T.);
#3747=EDGE_CURVE('',#4869,#4684,#356,.T.);
#3748=EDGE_CURVE('',#4869,#4870,#357,.T.);
#3749=EDGE_CURVE('',#4870,#4871,#358,.T.);
#3750=EDGE_CURVE('',#4871,#4685,#359,.T.);
#3751=EDGE_CURVE('',#4872,#4871,#360,.T.);
#3752=EDGE_CURVE('',#4873,#4872,#5577,.T.);
#3753=EDGE_CURVE('',#4874,#4873,#361,.T.);
#3754=EDGE_CURVE('',#4686,#4874,#362,.T.);
#3755=EDGE_CURVE('',#4874,#4875,#363,.T.);
#3756=EDGE_CURVE('',#4875,#4876,#364,.T.);
#3757=EDGE_CURVE('',#4876,#4687,#365,.T.);
#3758=EDGE_CURVE('',#4876,#4877,#5578,.T.);
#3759=EDGE_CURVE('',#4877,#4688,#366,.T.);
#3760=EDGE_CURVE('',#4877,#4878,#367,.T.);
#3761=EDGE_CURVE('',#4878,#4879,#368,.T.);
#3762=EDGE_CURVE('',#4879,#4689,#369,.T.);
#3763=EDGE_CURVE('',#4880,#4879,#370,.T.);
#3764=EDGE_CURVE('',#4881,#4880,#5579,.T.);
#3765=EDGE_CURVE('',#4882,#4881,#371,.T.);
#3766=EDGE_CURVE('',#4690,#4882,#372,.T.);
#3767=EDGE_CURVE('',#4882,#4883,#373,.T.);
#3768=EDGE_CURVE('',#4883,#4884,#374,.T.);
#3769=EDGE_CURVE('',#4884,#4691,#375,.T.);
#3770=EDGE_CURVE('',#4884,#4885,#5580,.T.);
#3771=EDGE_CURVE('',#4885,#4692,#376,.T.);
#3772=EDGE_CURVE('',#4885,#4886,#377,.T.);
#3773=EDGE_CURVE('',#4886,#4887,#378,.T.);
#3774=EDGE_CURVE('',#4887,#4693,#379,.T.);
#3775=EDGE_CURVE('',#4888,#4887,#380,.T.);
#3776=EDGE_CURVE('',#4889,#4888,#5581,.T.);
#3777=EDGE_CURVE('',#4890,#4889,#381,.T.);
#3778=EDGE_CURVE('',#4694,#4890,#382,.T.);
#3779=EDGE_CURVE('',#4890,#4891,#383,.T.);
#3780=EDGE_CURVE('',#4891,#4892,#384,.T.);
#3781=EDGE_CURVE('',#4892,#4695,#385,.T.);
#3782=EDGE_CURVE('',#4892,#4893,#5582,.T.);
#3783=EDGE_CURVE('',#4893,#4696,#386,.T.);
#3784=EDGE_CURVE('',#4893,#4894,#387,.T.);
#3785=EDGE_CURVE('',#4894,#4895,#388,.T.);
#3786=EDGE_CURVE('',#4895,#4697,#389,.T.);
#3787=EDGE_CURVE('',#4896,#4895,#390,.T.);
#3788=EDGE_CURVE('',#4897,#4896,#5583,.T.);
#3789=EDGE_CURVE('',#4898,#4897,#391,.T.);
#3790=EDGE_CURVE('',#4698,#4898,#392,.T.);
#3791=EDGE_CURVE('',#4898,#4899,#393,.T.);
#3792=EDGE_CURVE('',#4899,#4740,#394,.T.);
#3793=EDGE_CURVE('',#4900,#4900,#5584,.F.);
#3794=EDGE_CURVE('',#4899,#4742,#5585,.T.);
#3795=EDGE_CURVE('',#4745,#4901,#395,.T.);
#3796=EDGE_CURVE('',#4901,#4742,#396,.T.);
#3797=EDGE_CURVE('',#4902,#4744,#397,.T.);
#3798=EDGE_CURVE('',#4747,#4902,#398,.T.);
#3799=EDGE_CURVE('',#4824,#4903,#399,.T.);
#3800=EDGE_CURVE('',#4903,#4904,#5586,.T.);
#3801=EDGE_CURVE('',#4904,#4817,#400,.F.);
#3802=EDGE_CURVE('',#4816,#4905,#401,.F.);
#3803=EDGE_CURVE('',#4905,#4906,#5587,.T.);
#3804=EDGE_CURVE('',#4906,#4809,#402,.F.);
#3805=EDGE_CURVE('',#4808,#4907,#403,.F.);
#3806=EDGE_CURVE('',#4907,#4908,#5588,.T.);
#3807=EDGE_CURVE('',#4908,#4801,#404,.F.);
#3808=EDGE_CURVE('',#4800,#4909,#405,.F.);
#3809=EDGE_CURVE('',#4909,#4910,#5589,.T.);
#3810=EDGE_CURVE('',#4910,#4793,#406,.F.);
#3811=EDGE_CURVE('',#4792,#4911,#407,.F.);
#3812=EDGE_CURVE('',#4911,#4912,#5590,.T.);
#3813=EDGE_CURVE('',#4912,#4785,#408,.F.);
#3814=EDGE_CURVE('',#4784,#4913,#409,.F.);
#3815=EDGE_CURVE('',#4913,#4914,#5591,.T.);
#3816=EDGE_CURVE('',#4914,#4777,#410,.F.);
#3817=EDGE_CURVE('',#4776,#4915,#411,.F.);
#3818=EDGE_CURVE('',#4915,#4916,#5592,.T.);
#3819=EDGE_CURVE('',#4916,#4769,#412,.F.);
#3820=EDGE_CURVE('',#4768,#4917,#413,.F.);
#3821=EDGE_CURVE('',#4917,#4918,#5593,.T.);
#3822=EDGE_CURVE('',#4918,#4761,#414,.F.);
#3823=EDGE_CURVE('',#4760,#4919,#415,.F.);
#3824=EDGE_CURVE('',#4919,#4920,#5594,.T.);
#3825=EDGE_CURVE('',#4920,#4753,#416,.F.);
#3826=EDGE_CURVE('',#4752,#4921,#417,.F.);
#3827=EDGE_CURVE('',#4921,#4902,#5595,.T.);
#3828=EDGE_CURVE('',#4901,#4922,#5596,.T.);
#3829=EDGE_CURVE('',#4922,#4897,#418,.F.);
#3830=EDGE_CURVE('',#4896,#4923,#419,.F.);
#3831=EDGE_CURVE('',#4923,#4924,#5597,.T.);
#3832=EDGE_CURVE('',#4924,#4889,#420,.F.);
#3833=EDGE_CURVE('',#4888,#4925,#421,.F.);
#3834=EDGE_CURVE('',#4925,#4926,#5598,.T.);
#3835=EDGE_CURVE('',#4926,#4881,#422,.F.);
#3836=EDGE_CURVE('',#4880,#4927,#423,.F.);
#3837=EDGE_CURVE('',#4927,#4928,#5599,.T.);
#3838=EDGE_CURVE('',#4928,#4873,#424,.F.);
#3839=EDGE_CURVE('',#4872,#4929,#425,.F.);
#3840=EDGE_CURVE('',#4929,#4930,#5600,.T.);
#3841=EDGE_CURVE('',#4930,#4865,#426,.F.);
#3842=EDGE_CURVE('',#4864,#4931,#427,.F.);
#3843=EDGE_CURVE('',#4931,#4932,#5601,.T.);
#3844=EDGE_CURVE('',#4932,#4857,#428,.F.);
#3845=EDGE_CURVE('',#4856,#4933,#429,.F.);
#3846=EDGE_CURVE('',#4933,#4934,#5602,.T.);
#3847=EDGE_CURVE('',#4934,#4849,#430,.F.);
#3848=EDGE_CURVE('',#4848,#4935,#431,.F.);
#3849=EDGE_CURVE('',#4935,#4936,#5603,.T.);
#3850=EDGE_CURVE('',#4936,#4841,#432,.F.);
#3851=EDGE_CURVE('',#4840,#4937,#433,.F.);
#3852=EDGE_CURVE('',#4937,#4938,#5604,.T.);
#3853=EDGE_CURVE('',#4938,#4833,#434,.F.);
#3854=EDGE_CURVE('',#4832,#4939,#435,.F.);
#3855=EDGE_CURVE('',#4939,#4940,#5605,.T.);
#3856=EDGE_CURVE('',#4940,#4825,#436,.F.);
#3857=EDGE_CURVE('',#4941,#4941,#5606,.F.);
#3858=EDGE_CURVE('',#4747,#4750,#5607,.T.);
#3859=EDGE_CURVE('',#4921,#4750,#437,.T.);
#3860=EDGE_CURVE('',#4755,#4920,#438,.T.);
#3861=EDGE_CURVE('',#4755,#4758,#5608,.T.);
#3862=EDGE_CURVE('',#4919,#4758,#439,.T.);
#3863=EDGE_CURVE('',#4763,#4918,#440,.T.);
#3864=EDGE_CURVE('',#4763,#4766,#5609,.T.);
#3865=EDGE_CURVE('',#4917,#4766,#441,.T.);
#3866=EDGE_CURVE('',#4771,#4916,#442,.T.);
#3867=EDGE_CURVE('',#4771,#4774,#5610,.T.);
#3868=EDGE_CURVE('',#4915,#4774,#443,.T.);
#3869=EDGE_CURVE('',#4779,#4914,#444,.T.);
#3870=EDGE_CURVE('',#4779,#4782,#5611,.T.);
#3871=EDGE_CURVE('',#4913,#4782,#445,.T.);
#3872=EDGE_CURVE('',#4787,#4912,#446,.T.);
#3873=EDGE_CURVE('',#4787,#4790,#5612,.T.);
#3874=EDGE_CURVE('',#4911,#4790,#447,.T.);
#3875=EDGE_CURVE('',#4795,#4910,#448,.T.);
#3876=EDGE_CURVE('',#4795,#4798,#5613,.T.);
#3877=EDGE_CURVE('',#4909,#4798,#449,.T.);
#3878=EDGE_CURVE('',#4803,#4908,#450,.T.);
#3879=EDGE_CURVE('',#4803,#4806,#5614,.T.);
#3880=EDGE_CURVE('',#4907,#4806,#451,.T.);
#3881=EDGE_CURVE('',#4811,#4906,#452,.T.);
#3882=EDGE_CURVE('',#4811,#4814,#5615,.T.);
#3883=EDGE_CURVE('',#4905,#4814,#453,.T.);
#3884=EDGE_CURVE('',#4819,#4904,#454,.T.);
#3885=EDGE_CURVE('',#4819,#4822,#5616,.T.);
#3886=EDGE_CURVE('',#4903,#4822,#455,.T.);
#3887=EDGE_CURVE('',#4827,#4940,#456,.T.);
#3888=EDGE_CURVE('',#4827,#4830,#5617,.T.);
#3889=EDGE_CURVE('',#4939,#4830,#457,.T.);
#3890=EDGE_CURVE('',#4835,#4938,#458,.T.);
#3891=EDGE_CURVE('',#4835,#4838,#5618,.T.);
#3892=EDGE_CURVE('',#4937,#4838,#459,.T.);
#3893=EDGE_CURVE('',#4843,#4936,#460,.T.);
#3894=EDGE_CURVE('',#4843,#4846,#5619,.T.);
#3895=EDGE_CURVE('',#4935,#4846,#461,.T.);
#3896=EDGE_CURVE('',#4851,#4934,#462,.T.);
#3897=EDGE_CURVE('',#4851,#4854,#5620,.T.);
#3898=EDGE_CURVE('',#4933,#4854,#463,.T.);
#3899=EDGE_CURVE('',#4859,#4932,#464,.T.);
#3900=EDGE_CURVE('',#4859,#4862,#5621,.T.);
#3901=EDGE_CURVE('',#4931,#4862,#465,.T.);
#3902=EDGE_CURVE('',#4867,#4930,#466,.T.);
#3903=EDGE_CURVE('',#4867,#4870,#5622,.T.);
#3904=EDGE_CURVE('',#4929,#4870,#467,.T.);
#3905=EDGE_CURVE('',#4875,#4928,#468,.T.);
#3906=EDGE_CURVE('',#4875,#4878,#5623,.T.);
#3907=EDGE_CURVE('',#4927,#4878,#469,.T.);
#3908=EDGE_CURVE('',#4883,#4926,#470,.T.);
#3909=EDGE_CURVE('',#4883,#4886,#5624,.T.);
#3910=EDGE_CURVE('',#4925,#4886,#471,.T.);
#3911=EDGE_CURVE('',#4891,#4924,#472,.T.);
#3912=EDGE_CURVE('',#4891,#4894,#5625,.T.);
#3913=EDGE_CURVE('',#4923,#4894,#473,.T.);
#3914=EDGE_CURVE('',#4899,#4922,#474,.T.);
#3915=EDGE_CURVE('',#4942,#4942,#5626,.T.);
#3916=EDGE_CURVE('',#4943,#4943,#5627,.T.);
#3917=EDGE_CURVE('',#4944,#4944,#5628,.F.);
#4655=VERTEX_POINT('',#11101);
#4656=VERTEX_POINT('',#11103);
#4657=VERTEX_POINT('',#11106);
#4658=VERTEX_POINT('',#11109);
#4659=VERTEX_POINT('',#11112);
#4660=VERTEX_POINT('',#11113);
#4661=VERTEX_POINT('',#11118);
#4662=VERTEX_POINT('',#11120);
#4663=VERTEX_POINT('',#11125);
#4664=VERTEX_POINT('',#11127);
#4665=VERTEX_POINT('',#11132);
#4666=VERTEX_POINT('',#11134);
#4667=VERTEX_POINT('',#11139);
#4668=VERTEX_POINT('',#11141);
#4669=VERTEX_POINT('',#11146);
#4670=VERTEX_POINT('',#11148);
#4671=VERTEX_POINT('',#11153);
#4672=VERTEX_POINT('',#11155);
#4673=VERTEX_POINT('',#11160);
#4674=VERTEX_POINT('',#11162);
#4675=VERTEX_POINT('',#11167);
#4676=VERTEX_POINT('',#11169);
#4677=VERTEX_POINT('',#11174);
#4678=VERTEX_POINT('',#11176);
#4679=VERTEX_POINT('',#11181);
#4680=VERTEX_POINT('',#11183);
#4681=VERTEX_POINT('',#11188);
#4682=VERTEX_POINT('',#11190);
#4683=VERTEX_POINT('',#11195);
#4684=VERTEX_POINT('',#11197);
#4685=VERTEX_POINT('',#11202);
#4686=VERTEX_POINT('',#11204);
#4687=VERTEX_POINT('',#11209);
#4688=VERTEX_POINT('',#11211);
#4689=VERTEX_POINT('',#11216);
#4690=VERTEX_POINT('',#11218);
#4691=VERTEX_POINT('',#11223);
#4692=VERTEX_POINT('',#11225);
#4693=VERTEX_POINT('',#11230);
#4694=VERTEX_POINT('',#11232);
#4695=VERTEX_POINT('',#11237);
#4696=VERTEX_POINT('',#11239);
#4697=VERTEX_POINT('',#11244);
#4698=VERTEX_POINT('',#11246);
#4699=VERTEX_POINT('',#11251);
#4700=VERTEX_POINT('',#11253);
#4701=VERTEX_POINT('',#11258);
#4702=VERTEX_POINT('',#11260);
#4703=VERTEX_POINT('',#11265);
#4704=VERTEX_POINT('',#11267);
#4705=VERTEX_POINT('',#11272);
#4706=VERTEX_POINT('',#11274);
#4707=VERTEX_POINT('',#11279);
#4708=VERTEX_POINT('',#11281);
#4709=VERTEX_POINT('',#11286);
#4710=VERTEX_POINT('',#11288);
#4711=VERTEX_POINT('',#11293);
#4712=VERTEX_POINT('',#11295);
#4713=VERTEX_POINT('',#11300);
#4714=VERTEX_POINT('',#11302);
#4715=VERTEX_POINT('',#11307);
#4716=VERTEX_POINT('',#11309);
#4717=VERTEX_POINT('',#11314);
#4718=VERTEX_POINT('',#11316);
#4719=VERTEX_POINT('',#11321);
#4720=VERTEX_POINT('',#11323);
#4721=VERTEX_POINT('',#11328);
#4722=VERTEX_POINT('',#11330);
#4723=VERTEX_POINT('',#11335);
#4724=VERTEX_POINT('',#11337);
#4725=VERTEX_POINT('',#11342);
#4726=VERTEX_POINT('',#11344);
#4727=VERTEX_POINT('',#11349);
#4728=VERTEX_POINT('',#11351);
#4729=VERTEX_POINT('',#11356);
#4730=VERTEX_POINT('',#11358);
#4731=VERTEX_POINT('',#11363);
#4732=VERTEX_POINT('',#11365);
#4733=VERTEX_POINT('',#11370);
#4734=VERTEX_POINT('',#11372);
#4735=VERTEX_POINT('',#11377);
#4736=VERTEX_POINT('',#11379);
#4737=VERTEX_POINT('',#11384);
#4738=VERTEX_POINT('',#11386);
#4739=VERTEX_POINT('',#11393);
#4740=VERTEX_POINT('',#11399);
#4741=VERTEX_POINT('',#11401);
#4742=VERTEX_POINT('',#11411);
#4743=VERTEX_POINT('',#11416);
#4744=VERTEX_POINT('',#11423);
#4745=VERTEX_POINT('',#11424);
#4746=VERTEX_POINT('',#11429);
#4747=VERTEX_POINT('',#11443);
#4748=VERTEX_POINT('',#11448);
#4749=VERTEX_POINT('',#11455);
#4750=VERTEX_POINT('',#11465);
#4751=VERTEX_POINT('',#11470);
#4752=VERTEX_POINT('',#11480);
#4753=VERTEX_POINT('',#11482);
#4754=VERTEX_POINT('',#11487);
#4755=VERTEX_POINT('',#11497);
#4756=VERTEX_POINT('',#11502);
#4757=VERTEX_POINT('',#11509);
#4758=VERTEX_POINT('',#11519);
#4759=VERTEX_POINT('',#11524);
#4760=VERTEX_POINT('',#11534);
#4761=VERTEX_POINT('',#11536);
#4762=VERTEX_POINT('',#11541);
#4763=VERTEX_POINT('',#11551);
#4764=VERTEX_POINT('',#11556);
#4765=VERTEX_POINT('',#11563);
#4766=VERTEX_POINT('',#11573);
#4767=VERTEX_POINT('',#11578);
#4768=VERTEX_POINT('',#11588);
#4769=VERTEX_POINT('',#11590);
#4770=VERTEX_POINT('',#11595);
#4771=VERTEX_POINT('',#11605);
#4772=VERTEX_POINT('',#11610);
#4773=VERTEX_POINT('',#11617);
#4774=VERTEX_POINT('',#11627);
#4775=VERTEX_POINT('',#11632);
#4776=VERTEX_POINT('',#11642);
#4777=VERTEX_POINT('',#11644);
#4778=VERTEX_POINT('',#11649);
#4779=VERTEX_POINT('',#11659);
#4780=VERTEX_POINT('',#11664);
#4781=VERTEX_POINT('',#11671);
#4782=VERTEX_POINT('',#11681);
#4783=VERTEX_POINT('',#11686);
#4784=VERTEX_POINT('',#11696);
#4785=VERTEX_POINT('',#11698);
#4786=VERTEX_POINT('',#11703);
#4787=VERTEX_POINT('',#11713);
#4788=VERTEX_POINT('',#11718);
#4789=VERTEX_POINT('',#11725);
#4790=VERTEX_POINT('',#11735);
#4791=VERTEX_POINT('',#11740);
#4792=VERTEX_POINT('',#11750);
#4793=VERTEX_POINT('',#11752);
#4794=VERTEX_POINT('',#11757);
#4795=VERTEX_POINT('',#11767);
#4796=VERTEX_POINT('',#11772);
#4797=VERTEX_POINT('',#11779);
#4798=VERTEX_POINT('',#11789);
#4799=VERTEX_POINT('',#11794);
#4800=VERTEX_POINT('',#11804);
#4801=VERTEX_POINT('',#11806);
#4802=VERTEX_POINT('',#11811);
#4803=VERTEX_POINT('',#11821);
#4804=VERTEX_POINT('',#11826);
#4805=VERTEX_POINT('',#11833);
#4806=VERTEX_POINT('',#11843);
#4807=VERTEX_POINT('',#11848);
#4808=VERTEX_POINT('',#11858);
#4809=VERTEX_POINT('',#11860);
#4810=VERTEX_POINT('',#11865);
#4811=VERTEX_POINT('',#11875);
#4812=VERTEX_POINT('',#11880);
#4813=VERTEX_POINT('',#11887);
#4814=VERTEX_POINT('',#11897);
#4815=VERTEX_POINT('',#11902);
#4816=VERTEX_POINT('',#11912);
#4817=VERTEX_POINT('',#11914);
#4818=VERTEX_POINT('',#11919);
#4819=VERTEX_POINT('',#11929);
#4820=VERTEX_POINT('',#11934);
#4821=VERTEX_POINT('',#11941);
#4822=VERTEX_POINT('',#11951);
#4823=VERTEX_POINT('',#11956);
#4824=VERTEX_POINT('',#11966);
#4825=VERTEX_POINT('',#11968);
#4826=VERTEX_POINT('',#11973);
#4827=VERTEX_POINT('',#11983);
#4828=VERTEX_POINT('',#11988);
#4829=VERTEX_POINT('',#11995);
#4830=VERTEX_POINT('',#12005);
#4831=VERTEX_POINT('',#12010);
#4832=VERTEX_POINT('',#12020);
#4833=VERTEX_POINT('',#12022);
#4834=VERTEX_POINT('',#12027);
#4835=VERTEX_POINT('',#12037);
#4836=VERTEX_POINT('',#12042);
#4837=VERTEX_POINT('',#12049);
#4838=VERTEX_POINT('',#12059);
#4839=VERTEX_POINT('',#12064);
#4840=VERTEX_POINT('',#12074);
#4841=VERTEX_POINT('',#12076);
#4842=VERTEX_POINT('',#12081);
#4843=VERTEX_POINT('',#12091);
#4844=VERTEX_POINT('',#12096);
#4845=VERTEX_POINT('',#12103);
#4846=VERTEX_POINT('',#12113);
#4847=VERTEX_POINT('',#12118);
#4848=VERTEX_POINT('',#12128);
#4849=VERTEX_POINT('',#12130);
#4850=VERTEX_POINT('',#12135);
#4851=VERTEX_POINT('',#12145);
#4852=VERTEX_POINT('',#12150);
#4853=VERTEX_POINT('',#12157);
#4854=VERTEX_POINT('',#12167);
#4855=VERTEX_POINT('',#12172);
#4856=VERTEX_POINT('',#12182);
#4857=VERTEX_POINT('',#12184);
#4858=VERTEX_POINT('',#12189);
#4859=VERTEX_POINT('',#12199);
#4860=VERTEX_POINT('',#12204);
#4861=VERTEX_POINT('',#12211);
#4862=VERTEX_POINT('',#12221);
#4863=VERTEX_POINT('',#12226);
#4864=VERTEX_POINT('',#12236);
#4865=VERTEX_POINT('',#12238);
#4866=VERTEX_POINT('',#12243);
#4867=VERTEX_POINT('',#12253);
#4868=VERTEX_POINT('',#12258);
#4869=VERTEX_POINT('',#12265);
#4870=VERTEX_POINT('',#12275);
#4871=VERTEX_POINT('',#12280);
#4872=VERTEX_POINT('',#12290);
#4873=VERTEX_POINT('',#12292);
#4874=VERTEX_POINT('',#12297);
#4875=VERTEX_POINT('',#12307);
#4876=VERTEX_POINT('',#12312);
#4877=VERTEX_POINT('',#12319);
#4878=VERTEX_POINT('',#12329);
#4879=VERTEX_POINT('',#12334);
#4880=VERTEX_POINT('',#12344);
#4881=VERTEX_POINT('',#12346);
#4882=VERTEX_POINT('',#12351);
#4883=VERTEX_POINT('',#12361);
#4884=VERTEX_POINT('',#12366);
#4885=VERTEX_POINT('',#12373);
#4886=VERTEX_POINT('',#12383);
#4887=VERTEX_POINT('',#12388);
#4888=VERTEX_POINT('',#12398);
#4889=VERTEX_POINT('',#12400);
#4890=VERTEX_POINT('',#12405);
#4891=VERTEX_POINT('',#12415);
#4892=VERTEX_POINT('',#12420);
#4893=VERTEX_POINT('',#12427);
#4894=VERTEX_POINT('',#12437);
#4895=VERTEX_POINT('',#12442);
#4896=VERTEX_POINT('',#12452);
#4897=VERTEX_POINT('',#12454);
#4898=VERTEX_POINT('',#12459);
#4899=VERTEX_POINT('',#12469);
#4900=VERTEX_POINT('',#12476);
#4901=VERTEX_POINT('',#12484);
#4902=VERTEX_POINT('',#12494);
#4903=VERTEX_POINT('',#12504);
#4904=VERTEX_POINT('',#12506);
#4905=VERTEX_POINT('',#12515);
#4906=VERTEX_POINT('',#12517);
#4907=VERTEX_POINT('',#12526);
#4908=VERTEX_POINT('',#12528);
#4909=VERTEX_POINT('',#12537);
#4910=VERTEX_POINT('',#12539);
#4911=VERTEX_POINT('',#12548);
#4912=VERTEX_POINT('',#12550);
#4913=VERTEX_POINT('',#12559);
#4914=VERTEX_POINT('',#12561);
#4915=VERTEX_POINT('',#12570);
#4916=VERTEX_POINT('',#12572);
#4917=VERTEX_POINT('',#12581);
#4918=VERTEX_POINT('',#12583);
#4919=VERTEX_POINT('',#12592);
#4920=VERTEX_POINT('',#12594);
#4921=VERTEX_POINT('',#12603);
#4922=VERTEX_POINT('',#12606);
#4923=VERTEX_POINT('',#12615);
#4924=VERTEX_POINT('',#12617);
#4925=VERTEX_POINT('',#12626);
#4926=VERTEX_POINT('',#12628);
#4927=VERTEX_POINT('',#12637);
#4928=VERTEX_POINT('',#12639);
#4929=VERTEX_POINT('',#12648);
#4930=VERTEX_POINT('',#12650);
#4931=VERTEX_POINT('',#12659);
#4932=VERTEX_POINT('',#12661);
#4933=VERTEX_POINT('',#12670);
#4934=VERTEX_POINT('',#12672);
#4935=VERTEX_POINT('',#12681);
#4936=VERTEX_POINT('',#12683);
#4937=VERTEX_POINT('',#12692);
#4938=VERTEX_POINT('',#12694);
#4939=VERTEX_POINT('',#12703);
#4940=VERTEX_POINT('',#12705);
#4941=VERTEX_POINT('',#12711);
#4942=VERTEX_POINT('',#12942);
#4943=VERTEX_POINT('',#12947);
#4944=VERTEX_POINT('',#12968);
#5499=CIRCLE('',#8241,0.0115);
#5500=CIRCLE('',#8242,0.0115);
#5501=CIRCLE('',#8244,0.0125);
#5502=CIRCLE('',#8246,0.016);
#5503=CIRCLE('',#8248,0.0125);
#5504=CIRCLE('',#8249,0.0125);
#5505=CIRCLE('',#8250,0.0125);
#5506=CIRCLE('',#8251,0.0125);
#5507=CIRCLE('',#8252,0.0125);
#5508=CIRCLE('',#8253,0.0125);
#5509=CIRCLE('',#8254,0.0125);
#5510=CIRCLE('',#8255,0.0125);
#5511=CIRCLE('',#8256,0.0125);
#5512=CIRCLE('',#8257,0.0125);
#5513=CIRCLE('',#8258,0.0125);
#5514=CIRCLE('',#8259,0.0125);
#5515=CIRCLE('',#8260,0.0125);
#5516=CIRCLE('',#8261,0.0125);
#5517=CIRCLE('',#8262,0.0125);
#5518=CIRCLE('',#8263,0.0125);
#5519=CIRCLE('',#8264,0.0125);
#5520=CIRCLE('',#8265,0.0125);
#5521=CIRCLE('',#8266,0.0125);
#5522=CIRCLE('',#8267,0.0125);
#5523=CIRCLE('',#8268,0.0125);
#5524=CIRCLE('',#8269,0.0125);
#5525=CIRCLE('',#8270,0.0125);
#5526=CIRCLE('',#8271,0.0125);
#5527=CIRCLE('',#8272,0.0125);
#5528=CIRCLE('',#8273,0.0125);
#5529=CIRCLE('',#8274,0.0125);
#5530=CIRCLE('',#8275,0.0125);
#5531=CIRCLE('',#8276,0.0125);
#5532=CIRCLE('',#8277,0.0125);
#5533=CIRCLE('',#8278,0.0125);
#5534=CIRCLE('',#8279,0.0125);
#5535=CIRCLE('',#8280,0.0125);
#5536=CIRCLE('',#8281,0.0125);
#5537=CIRCLE('',#8282,0.0125);
#5538=CIRCLE('',#8283,0.0125);
#5539=CIRCLE('',#8284,0.0125);
#5540=CIRCLE('',#8285,0.0125);
#5541=CIRCLE('',#8286,0.0125);
#5542=CIRCLE('',#8287,0.0125);
#5543=CIRCLE('',#8289,0.016);
#5544=CIRCLE('',#8291,0.013);
#5545=CIRCLE('',#8294,0.0175);
#5546=CIRCLE('',#8297,0.013);
#5547=CIRCLE('',#8300,0.0175);
#5548=CIRCLE('',#8303,0.013);
#5549=CIRCLE('',#8306,0.0175);
#5550=CIRCLE('',#8309,0.013);
#5551=CIRCLE('',#8312,0.0175);
#5552=CIRCLE('',#8315,0.013);
#5553=CIRCLE('',#8318,0.0175);
#5554=CIRCLE('',#8321,0.013);
#5555=CIRCLE('',#8324,0.0175);
#5556=CIRCLE('',#8327,0.013);
#5557=CIRCLE('',#8330,0.0175);
#5558=CIRCLE('',#8333,0.013);
#5559=CIRCLE('',#8336,0.0175);
#5560=CIRCLE('',#8339,0.013);
#5561=CIRCLE('',#8342,0.0175);
#5562=CIRCLE('',#8345,0.013);
#5563=CIRCLE('',#8348,0.0175);
#5564=CIRCLE('',#8351,0.013);
#5565=CIRCLE('',#8354,0.0175);
#5566=CIRCLE('',#8357,0.013);
#5567=CIRCLE('',#8360,0.0175);
#5568=CIRCLE('',#8363,0.013);
#5569=CIRCLE('',#8366,0.0175);
#5570=CIRCLE('',#8369,0.013);
#5571=CIRCLE('',#8372,0.0175);
#5572=CIRCLE('',#8375,0.013);
#5573=CIRCLE('',#8378,0.0175);
#5574=CIRCLE('',#8381,0.013);
#5575=CIRCLE('',#8384,0.0175);
#5576=CIRCLE('',#8387,0.013);
#5577=CIRCLE('',#8390,0.0175);
#5578=CIRCLE('',#8393,0.013);
#5579=CIRCLE('',#8396,0.0175);
#5580=CIRCLE('',#8399,0.013);
#5581=CIRCLE('',#8402,0.0175);
#5582=CIRCLE('',#8405,0.013);
#5583=CIRCLE('',#8408,0.0175);
#5584=CIRCLE('',#8411,0.0175);
#5585=CIRCLE('',#8413,0.013);
#5586=CIRCLE('',#8417,0.0175);
#5587=CIRCLE('',#8418,0.0175);
#5588=CIRCLE('',#8419,0.0175);
#5589=CIRCLE('',#8420,0.0175);
#5590=CIRCLE('',#8421,0.0175);
#5591=CIRCLE('',#8422,0.0175);
#5592=CIRCLE('',#8423,0.0175);
#5593=CIRCLE('',#8424,0.0175);
#5594=CIRCLE('',#8425,0.0175);
#5595=CIRCLE('',#8426,0.0175);
#5596=CIRCLE('',#8427,0.0175);
#5597=CIRCLE('',#8428,0.0175);
#5598=CIRCLE('',#8429,0.0175);
#5599=CIRCLE('',#8430,0.0175);
#5600=CIRCLE('',#8431,0.0175);
#5601=CIRCLE('',#8432,0.0175);
#5602=CIRCLE('',#8433,0.0175);
#5603=CIRCLE('',#8434,0.0175);
#5604=CIRCLE('',#8435,0.0175);
#5605=CIRCLE('',#8436,0.0175);
#5606=CIRCLE('',#8437,0.0175);
#5607=CIRCLE('',#8439,0.013);
#5608=CIRCLE('',#8443,0.013);
#5609=CIRCLE('',#8447,0.013);
#5610=CIRCLE('',#8451,0.013);
#5611=CIRCLE('',#8455,0.013);
#5612=CIRCLE('',#8459,0.013);
#5613=CIRCLE('',#8463,0.013);
#5614=CIRCLE('',#8467,0.013);
#5615=CIRCLE('',#8471,0.013);
#5616=CIRCLE('',#8475,0.013);
#5617=CIRCLE('',#8479,0.013);
#5618=CIRCLE('',#8483,0.013);
#5619=CIRCLE('',#8487,0.013);
#5620=CIRCLE('',#8491,0.013);
#5621=CIRCLE('',#8495,0.013);
#5622=CIRCLE('',#8499,0.013);
#5623=CIRCLE('',#8503,0.013);
#5624=CIRCLE('',#8507,0.013);
#5625=CIRCLE('',#8511,0.013);
#5626=CIRCLE('',#8515,0.0175);
#5627=CIRCLE('',#8519,0.0165);
#5628=CIRCLE('',#8539,0.0165);
#5953=EDGE_LOOP('',(#1094));
#5954=EDGE_LOOP('',(#1095));
#5955=EDGE_LOOP('',(#1096));
#5956=EDGE_LOOP('',(#1097));
#5957=EDGE_LOOP('',(#1098));
#5958=EDGE_LOOP('',(#1099));
#5959=EDGE_LOOP('',(#1100));
#5960=EDGE_LOOP('',(#1101,#1102,#1103,#1104,#1105,#1106,#1107,#1108,#1109,
#1110,#1111,#1112,#1113,#1114,#1115,#1116,#1117,#1118,#1119,#1120,#1121,
#1122,#1123,#1124,#1125,#1126,#1127,#1128,#1129,#1130,#1131,#1132,#1133,
#1134,#1135,#1136,#1137,#1138,#1139,#1140,#1141,#1142,#1143,#1144,#1145,
#1146,#1147,#1148,#1149,#1150,#1151,#1152,#1153,#1154,#1155,#1156,#1157,
#1158,#1159,#1160,#1161,#1162,#1163,#1164,#1165,#1166,#1167,#1168,#1169,
#1170,#1171,#1172,#1173,#1174,#1175,#1176,#1177,#1178,#1179,#1180));
#5961=EDGE_LOOP('',(#1181));
#5962=EDGE_LOOP('',(#1182));
#5963=EDGE_LOOP('',(#1183,#1184,#1185,#1186));
#5964=EDGE_LOOP('',(#1187,#1188,#1189,#1190,#1191));
#5965=EDGE_LOOP('',(#1192,#1193,#1194,#1195,#1196,#1197));
#5966=EDGE_LOOP('',(#1198,#1199,#1200,#1201,#1202));
#5967=EDGE_LOOP('',(#1203,#1204,#1205,#1206));
#5968=EDGE_LOOP('',(#1207,#1208,#1209,#1210,#1211));
#5969=EDGE_LOOP('',(#1212,#1213,#1214,#1215,#1216,#1217));
#5970=EDGE_LOOP('',(#1218,#1219,#1220,#1221,#1222));
#5971=EDGE_LOOP('',(#1223,#1224,#1225,#1226));
#5972=EDGE_LOOP('',(#1227,#1228,#1229,#1230,#1231));
#5973=EDGE_LOOP('',(#1232,#1233,#1234,#1235,#1236,#1237));
#5974=EDGE_LOOP('',(#1238,#1239,#1240,#1241,#1242));
#5975=EDGE_LOOP('',(#1243,#1244,#1245,#1246));
#5976=EDGE_LOOP('',(#1247,#1248,#1249,#1250,#1251));
#5977=EDGE_LOOP('',(#1252,#1253,#1254,#1255,#1256,#1257));
#5978=EDGE_LOOP('',(#1258,#1259,#1260,#1261,#1262));
#5979=EDGE_LOOP('',(#1263,#1264,#1265,#1266));
#5980=EDGE_LOOP('',(#1267,#1268,#1269,#1270,#1271));
#5981=EDGE_LOOP('',(#1272,#1273,#1274,#1275,#1276,#1277));
#5982=EDGE_LOOP('',(#1278,#1279,#1280,#1281,#1282));
#5983=EDGE_LOOP('',(#1283,#1284,#1285,#1286));
#5984=EDGE_LOOP('',(#1287,#1288,#1289,#1290,#1291));
#5985=EDGE_LOOP('',(#1292,#1293,#1294,#1295,#1296,#1297));
#5986=EDGE_LOOP('',(#1298,#1299,#1300,#1301,#1302));
#5987=EDGE_LOOP('',(#1303,#1304,#1305,#1306));
#5988=EDGE_LOOP('',(#1307,#1308,#1309,#1310,#1311));
#5989=EDGE_LOOP('',(#1312,#1313,#1314,#1315,#1316,#1317));
#5990=EDGE_LOOP('',(#1318,#1319,#1320,#1321,#1322));
#5991=EDGE_LOOP('',(#1323,#1324,#1325,#1326));
#5992=EDGE_LOOP('',(#1327,#1328,#1329,#1330,#1331));
#5993=EDGE_LOOP('',(#1332,#1333,#1334,#1335,#1336,#1337));
#5994=EDGE_LOOP('',(#1338,#1339,#1340,#1341,#1342));
#5995=EDGE_LOOP('',(#1343,#1344,#1345,#1346));
#5996=EDGE_LOOP('',(#1347,#1348,#1349,#1350,#1351));
#5997=EDGE_LOOP('',(#1352,#1353,#1354,#1355,#1356,#1357));
#5998=EDGE_LOOP('',(#1358,#1359,#1360,#1361,#1362));
#5999=EDGE_LOOP('',(#1363,#1364,#1365,#1366));
#6000=EDGE_LOOP('',(#1367,#1368,#1369,#1370,#1371));
#6001=EDGE_LOOP('',(#1372,#1373,#1374,#1375,#1376,#1377));
#6002=EDGE_LOOP('',(#1378,#1379,#1380,#1381,#1382));
#6003=EDGE_LOOP('',(#1383,#1384,#1385,#1386));
#6004=EDGE_LOOP('',(#1387,#1388,#1389,#1390,#1391));
#6005=EDGE_LOOP('',(#1392,#1393,#1394,#1395,#1396,#1397));
#6006=EDGE_LOOP('',(#1398,#1399,#1400,#1401,#1402));
#6007=EDGE_LOOP('',(#1403,#1404,#1405,#1406));
#6008=EDGE_LOOP('',(#1407,#1408,#1409,#1410,#1411));
#6009=EDGE_LOOP('',(#1412,#1413,#1414,#1415,#1416,#1417));
#6010=EDGE_LOOP('',(#1418,#1419,#1420,#1421,#1422));
#6011=EDGE_LOOP('',(#1423,#1424,#1425,#1426));
#6012=EDGE_LOOP('',(#1427,#1428,#1429,#1430,#1431));
#6013=EDGE_LOOP('',(#1432,#1433,#1434,#1435,#1436,#1437));
#6014=EDGE_LOOP('',(#1438,#1439,#1440,#1441,#1442));
#6015=EDGE_LOOP('',(#1443,#1444,#1445,#1446));
#6016=EDGE_LOOP('',(#1447,#1448,#1449,#1450,#1451));
#6017=EDGE_LOOP('',(#1452,#1453,#1454,#1455,#1456,#1457));
#6018=EDGE_LOOP('',(#1458,#1459,#1460,#1461,#1462));
#6019=EDGE_LOOP('',(#1463,#1464,#1465,#1466));
#6020=EDGE_LOOP('',(#1467,#1468,#1469,#1470,#1471));
#6021=EDGE_LOOP('',(#1472,#1473,#1474,#1475,#1476,#1477));
#6022=EDGE_LOOP('',(#1478,#1479,#1480,#1481,#1482));
#6023=EDGE_LOOP('',(#1483,#1484,#1485,#1486));
#6024=EDGE_LOOP('',(#1487,#1488,#1489,#1490,#1491));
#6025=EDGE_LOOP('',(#1492,#1493,#1494,#1495,#1496,#1497));
#6026=EDGE_LOOP('',(#1498,#1499,#1500,#1501,#1502));
#6027=EDGE_LOOP('',(#1503,#1504,#1505,#1506));
#6028=EDGE_LOOP('',(#1507,#1508,#1509,#1510,#1511));
#6029=EDGE_LOOP('',(#1512,#1513,#1514,#1515,#1516,#1517));
#6030=EDGE_LOOP('',(#1518,#1519,#1520,#1521,#1522));
#6031=EDGE_LOOP('',(#1523,#1524,#1525,#1526));
#6032=EDGE_LOOP('',(#1527,#1528,#1529,#1530,#1531));
#6033=EDGE_LOOP('',(#1532,#1533,#1534,#1535,#1536,#1537));
#6034=EDGE_LOOP('',(#1538,#1539,#1540,#1541,#1542));
#6035=EDGE_LOOP('',(#1543,#1544,#1545,#1546));
#6036=EDGE_LOOP('',(#1547,#1548,#1549,#1550,#1551));
#6037=EDGE_LOOP('',(#1552,#1553,#1554,#1555,#1556,#1557));
#6038=EDGE_LOOP('',(#1558,#1559,#1560,#1561,#1562));
#6039=EDGE_LOOP('',(#1563,#1564,#1565,#1566));
#6040=EDGE_LOOP('',(#1567,#1568,#1569,#1570,#1571));
#6041=EDGE_LOOP('',(#1572,#1573,#1574,#1575,#1576,#1577));
#6042=EDGE_LOOP('',(#1578,#1579,#1580,#1581,#1582));
#6043=EDGE_LOOP('',(#1583));
#6044=EDGE_LOOP('',(#1584));
#6045=EDGE_LOOP('',(#1585,#1586,#1587,#1588));
#6046=EDGE_LOOP('',(#1589,#1590,#1591,#1592));
#6047=EDGE_LOOP('',(#1593,#1594,#1595,#1596));
#6048=EDGE_LOOP('',(#1597,#1598,#1599,#1600,#1601,#1602,#1603,#1604,#1605,
#1606,#1607,#1608,#1609,#1610,#1611,#1612,#1613,#1614,#1615,#1616,#1617,
#1618,#1619,#1620,#1621,#1622,#1623,#1624,#1625,#1626,#1627,#1628,#1629,
#1630,#1631,#1632,#1633,#1634,#1635,#1636,#1637,#1638,#1639,#1640,#1641,
#1642,#1643,#1644,#1645,#1646,#1647,#1648,#1649,#1650,#1651,#1652,#1653,
#1654,#1655,#1656,#1657,#1658,#1659,#1660,#1661,#1662,#1663,#1664,#1665,
#1666,#1667,#1668,#1669,#1670,#1671,#1672,#1673,#1674,#1675,#1676));
#6049=EDGE_LOOP('',(#1677));
#6050=EDGE_LOOP('',(#1678,#1679,#1680,#1681));
#6051=EDGE_LOOP('',(#1682,#1683,#1684,#1685));
#6052=EDGE_LOOP('',(#1686,#1687,#1688,#1689));
#6053=EDGE_LOOP('',(#1690,#1691,#1692,#1693));
#6054=EDGE_LOOP('',(#1694,#1695,#1696,#1697));
#6055=EDGE_LOOP('',(#1698,#1699,#1700,#1701));
#6056=EDGE_LOOP('',(#1702,#1703,#1704,#1705));
#6057=EDGE_LOOP('',(#1706,#1707,#1708,#1709));
#6058=EDGE_LOOP('',(#1710,#1711,#1712,#1713));
#6059=EDGE_LOOP('',(#1714,#1715,#1716,#1717));
#6060=EDGE_LOOP('',(#1718,#1719,#1720,#1721));
#6061=EDGE_LOOP('',(#1722,#1723,#1724,#1725));
#6062=EDGE_LOOP('',(#1726,#1727,#1728,#1729));
#6063=EDGE_LOOP('',(#1730,#1731,#1732,#1733));
#6064=EDGE_LOOP('',(#1734,#1735,#1736,#1737));
#6065=EDGE_LOOP('',(#1738,#1739,#1740,#1741));
#6066=EDGE_LOOP('',(#1742,#1743,#1744,#1745));
#6067=EDGE_LOOP('',(#1746,#1747,#1748,#1749));
#6068=EDGE_LOOP('',(#1750,#1751,#1752,#1753));
#6069=EDGE_LOOP('',(#1754,#1755,#1756,#1757));
#6070=EDGE_LOOP('',(#1758,#1759,#1760,#1761));
#6071=EDGE_LOOP('',(#1762,#1763,#1764,#1765));
#6072=EDGE_LOOP('',(#1766,#1767,#1768,#1769));
#6073=EDGE_LOOP('',(#1770,#1771,#1772,#1773));
#6074=EDGE_LOOP('',(#1774,#1775,#1776,#1777));
#6075=EDGE_LOOP('',(#1778,#1779,#1780,#1781));
#6076=EDGE_LOOP('',(#1782,#1783,#1784,#1785));
#6077=EDGE_LOOP('',(#1786,#1787,#1788,#1789));
#6078=EDGE_LOOP('',(#1790,#1791,#1792,#1793));
#6079=EDGE_LOOP('',(#1794,#1795,#1796,#1797));
#6080=EDGE_LOOP('',(#1798,#1799,#1800,#1801));
#6081=EDGE_LOOP('',(#1802,#1803,#1804,#1805));
#6082=EDGE_LOOP('',(#1806,#1807,#1808,#1809));
#6083=EDGE_LOOP('',(#1810,#1811,#1812,#1813));
#6084=EDGE_LOOP('',(#1814,#1815,#1816,#1817));
#6085=EDGE_LOOP('',(#1818,#1819,#1820,#1821));
#6086=EDGE_LOOP('',(#1822,#1823,#1824,#1825));
#6087=EDGE_LOOP('',(#1826,#1827,#1828,#1829));
#6088=EDGE_LOOP('',(#1830,#1831,#1832,#1833));
#6089=EDGE_LOOP('',(#1834,#1835,#1836,#1837));
#6090=EDGE_LOOP('',(#1838,#1839,#1840,#1841));
#6091=EDGE_LOOP('',(#1842,#1843,#1844,#1845));
#6092=EDGE_LOOP('',(#1846,#1847,#1848,#1849));
#6093=EDGE_LOOP('',(#1850,#1851,#1852,#1853));
#6094=EDGE_LOOP('',(#1854,#1855,#1856,#1857));
#6095=EDGE_LOOP('',(#1858,#1859,#1860,#1861));
#6096=EDGE_LOOP('',(#1862,#1863,#1864,#1865));
#6097=EDGE_LOOP('',(#1866,#1867,#1868,#1869));
#6098=EDGE_LOOP('',(#1870,#1871,#1872,#1873));
#6099=EDGE_LOOP('',(#1874,#1875,#1876,#1877));
#6100=EDGE_LOOP('',(#1878,#1879,#1880,#1881));
#6101=EDGE_LOOP('',(#1882,#1883,#1884,#1885));
#6102=EDGE_LOOP('',(#1886,#1887,#1888,#1889));
#6103=EDGE_LOOP('',(#1890,#1891,#1892,#1893));
#6104=EDGE_LOOP('',(#1894,#1895,#1896,#1897));
#6105=EDGE_LOOP('',(#1898,#1899,#1900,#1901));
#6106=EDGE_LOOP('',(#1902,#1903,#1904,#1905));
#6107=EDGE_LOOP('',(#1906));
#6108=EDGE_LOOP('',(#1907));
#6109=EDGE_LOOP('',(#1908,#1909,#1910,#1911));
#6110=EDGE_LOOP('',(#1912,#1913,#1914,#1915));
#6111=EDGE_LOOP('',(#1916));
#6112=EDGE_LOOP('',(#1917));
#6113=EDGE_LOOP('',(#1918,#1919,#1920,#1921));
#6114=EDGE_LOOP('',(#1922,#1923,#1924,#1925));
#6115=EDGE_LOOP('',(#1926,#1927,#1928,#1929));
#6116=EDGE_LOOP('',(#1930,#1931,#1932,#1933));
#6117=EDGE_LOOP('',(#1934,#1935,#1936,#1937));
#6118=EDGE_LOOP('',(#1938,#1939,#1940,#1941));
#6119=EDGE_LOOP('',(#1942,#1943,#1944,#1945));
#6120=EDGE_LOOP('',(#1946,#1947,#1948,#1949));
#6121=EDGE_LOOP('',(#1950,#1951,#1952,#1953));
#6122=EDGE_LOOP('',(#1954,#1955,#1956,#1957));
#6123=EDGE_LOOP('',(#1958,#1959,#1960,#1961));
#6124=EDGE_LOOP('',(#1962,#1963,#1964,#1965));
#6125=EDGE_LOOP('',(#1966,#1967,#1968,#1969));
#6126=EDGE_LOOP('',(#1970,#1971,#1972,#1973));
#6127=EDGE_LOOP('',(#1974,#1975,#1976,#1977));
#6128=EDGE_LOOP('',(#1978,#1979,#1980,#1981));
#6129=EDGE_LOOP('',(#1982,#1983,#1984,#1985));
#6130=EDGE_LOOP('',(#1986,#1987,#1988,#1989));
#6131=EDGE_LOOP('',(#1990));
#6132=EDGE_LOOP('',(#1991));
#6133=EDGE_LOOP('',(#1992));
#6134=EDGE_LOOP('',(#1993));
#6714=FACE_BOUND('',#5953,.T.);
#6715=FACE_BOUND('',#5954,.T.);
#6716=FACE_BOUND('',#5955,.T.);
#6717=FACE_BOUND('',#5956,.T.);
#6718=FACE_BOUND('',#5957,.T.);
#6719=FACE_BOUND('',#5958,.T.);
#6720=FACE_BOUND('',#5959,.T.);
#6721=FACE_BOUND('',#5960,.T.);
#6722=FACE_BOUND('',#5961,.T.);
#6723=FACE_BOUND('',#5962,.T.);
#6724=FACE_BOUND('',#5963,.T.);
#6725=FACE_BOUND('',#5964,.T.);
#6726=FACE_BOUND('',#5965,.T.);
#6727=FACE_BOUND('',#5966,.T.);
#6728=FACE_BOUND('',#5967,.T.);
#6729=FACE_BOUND('',#5968,.T.);
#6730=FACE_BOUND('',#5969,.T.);
#6731=FACE_BOUND('',#5970,.T.);
#6732=FACE_BOUND('',#5971,.T.);
#6733=FACE_BOUND('',#5972,.T.);
#6734=FACE_BOUND('',#5973,.T.);
#6735=FACE_BOUND('',#5974,.T.);
#6736=FACE_BOUND('',#5975,.T.);
#6737=FACE_BOUND('',#5976,.T.);
#6738=FACE_BOUND('',#5977,.T.);
#6739=FACE_BOUND('',#5978,.T.);
#6740=FACE_BOUND('',#5979,.T.);
#6741=FACE_BOUND('',#5980,.T.);
#6742=FACE_BOUND('',#5981,.T.);
#6743=FACE_BOUND('',#5982,.T.);
#6744=FACE_BOUND('',#5983,.T.);
#6745=FACE_BOUND('',#5984,.T.);
#6746=FACE_BOUND('',#5985,.T.);
#6747=FACE_BOUND('',#5986,.T.);
#6748=FACE_BOUND('',#5987,.T.);
#6749=FACE_BOUND('',#5988,.T.);
#6750=FACE_BOUND('',#5989,.T.);
#6751=FACE_BOUND('',#5990,.T.);
#6752=FACE_BOUND('',#5991,.T.);
#6753=FACE_BOUND('',#5992,.T.);
#6754=FACE_BOUND('',#5993,.T.);
#6755=FACE_BOUND('',#5994,.T.);
#6756=FACE_BOUND('',#5995,.T.);
#6757=FACE_BOUND('',#5996,.T.);
#6758=FACE_BOUND('',#5997,.T.);
#6759=FACE_BOUND('',#5998,.T.);
#6760=FACE_BOUND('',#5999,.T.);
#6761=FACE_BOUND('',#6000,.T.);
#6762=FACE_BOUND('',#6001,.T.);
#6763=FACE_BOUND('',#6002,.T.);
#6764=FACE_BOUND('',#6003,.T.);
#6765=FACE_BOUND('',#6004,.T.);
#6766=FACE_BOUND('',#6005,.T.);
#6767=FACE_BOUND('',#6006,.T.);
#6768=FACE_BOUND('',#6007,.T.);
#6769=FACE_BOUND('',#6008,.T.);
#6770=FACE_BOUND('',#6009,.T.);
#6771=FACE_BOUND('',#6010,.T.);
#6772=FACE_BOUND('',#6011,.T.);
#6773=FACE_BOUND('',#6012,.T.);
#6774=FACE_BOUND('',#6013,.T.);
#6775=FACE_BOUND('',#6014,.T.);
#6776=FACE_BOUND('',#6015,.T.);
#6777=FACE_BOUND('',#6016,.T.);
#6778=FACE_BOUND('',#6017,.T.);
#6779=FACE_BOUND('',#6018,.T.);
#6780=FACE_BOUND('',#6019,.T.);
#6781=FACE_BOUND('',#6020,.T.);
#6782=FACE_BOUND('',#6021,.T.);
#6783=FACE_BOUND('',#6022,.T.);
#6784=FACE_BOUND('',#6023,.T.);
#6785=FACE_BOUND('',#6024,.T.);
#6786=FACE_BOUND('',#6025,.T.);
#6787=FACE_BOUND('',#6026,.T.);
#6788=FACE_BOUND('',#6027,.T.);
#6789=FACE_BOUND('',#6028,.T.);
#6790=FACE_BOUND('',#6029,.T.);
#6791=FACE_BOUND('',#6030,.T.);
#6792=FACE_BOUND('',#6031,.T.);
#6793=FACE_BOUND('',#6032,.T.);
#6794=FACE_BOUND('',#6033,.T.);
#6795=FACE_BOUND('',#6034,.T.);
#6796=FACE_BOUND('',#6035,.T.);
#6797=FACE_BOUND('',#6036,.T.);
#6798=FACE_BOUND('',#6037,.T.);
#6799=FACE_BOUND('',#6038,.T.);
#6800=FACE_BOUND('',#6039,.T.);
#6801=FACE_BOUND('',#6040,.T.);
#6802=FACE_BOUND('',#6041,.T.);
#6803=FACE_BOUND('',#6042,.T.);
#6804=FACE_BOUND('',#6043,.T.);
#6805=FACE_BOUND('',#6044,.T.);
#6806=FACE_BOUND('',#6045,.T.);
#6807=FACE_BOUND('',#6046,.T.);
#6808=FACE_BOUND('',#6047,.T.);
#6809=FACE_BOUND('',#6048,.T.);
#6810=FACE_BOUND('',#6049,.T.);
#6811=FACE_BOUND('',#6050,.T.);
#6812=FACE_BOUND('',#6051,.T.);
#6813=FACE_BOUND('',#6052,.T.);
#6814=FACE_BOUND('',#6053,.T.);
#6815=FACE_BOUND('',#6054,.T.);
#6816=FACE_BOUND('',#6055,.T.);
#6817=FACE_BOUND('',#6056,.T.);
#6818=FACE_BOUND('',#6057,.T.);
#6819=FACE_BOUND('',#6058,.T.);
#6820=FACE_BOUND('',#6059,.T.);
#6821=FACE_BOUND('',#6060,.T.);
#6822=FACE_BOUND('',#6061,.T.);
#6823=FACE_BOUND('',#6062,.T.);
#6824=FACE_BOUND('',#6063,.T.);
#6825=FACE_BOUND('',#6064,.T.);
#6826=FACE_BOUND('',#6065,.T.);
#6827=FACE_BOUND('',#6066,.T.);
#6828=FACE_BOUND('',#6067,.T.);
#6829=FACE_BOUND('',#6068,.T.);
#6830=FACE_BOUND('',#6069,.T.);
#6831=FACE_BOUND('',#6070,.T.);
#6832=FACE_BOUND('',#6071,.T.);
#6833=FACE_BOUND('',#6072,.T.);
#6834=FACE_BOUND('',#6073,.T.);
#6835=FACE_BOUND('',#6074,.T.);
#6836=FACE_BOUND('',#6075,.T.);
#6837=FACE_BOUND('',#6076,.T.);
#6838=FACE_BOUND('',#6077,.T.);
#6839=FACE_BOUND('',#6078,.T.);
#6840=FACE_BOUND('',#6079,.T.);
#6841=FACE_BOUND('',#6080,.T.);
#6842=FACE_BOUND('',#6081,.T.);
#6843=FACE_BOUND('',#6082,.T.);
#6844=FACE_BOUND('',#6083,.T.);
#6845=FACE_BOUND('',#6084,.T.);
#6846=FACE_BOUND('',#6085,.T.);
#6847=FACE_BOUND('',#6086,.T.);
#6848=FACE_BOUND('',#6087,.T.);
#6849=FACE_BOUND('',#6088,.T.);
#6850=FACE_BOUND('',#6089,.T.);
#6851=FACE_BOUND('',#6090,.T.);
#6852=FACE_BOUND('',#6091,.T.);
#6853=FACE_BOUND('',#6092,.T.);
#6854=FACE_BOUND('',#6093,.T.);
#6855=FACE_BOUND('',#6094,.T.);
#6856=FACE_BOUND('',#6095,.T.);
#6857=FACE_BOUND('',#6096,.T.);
#6858=FACE_BOUND('',#6097,.T.);
#6859=FACE_BOUND('',#6098,.T.);
#6860=FACE_BOUND('',#6099,.T.);
#6861=FACE_BOUND('',#6100,.T.);
#6862=FACE_BOUND('',#6101,.T.);
#6863=FACE_BOUND('',#6102,.T.);
#6864=FACE_BOUND('',#6103,.T.);
#6865=FACE_BOUND('',#6104,.T.);
#6866=FACE_BOUND('',#6105,.T.);
#6867=FACE_BOUND('',#6106,.T.);
#6868=FACE_BOUND('',#6107,.T.);
#6869=FACE_BOUND('',#6108,.T.);
#6870=FACE_BOUND('',#6109,.T.);
#6871=FACE_BOUND('',#6110,.T.);
#6872=FACE_BOUND('',#6111,.T.);
#6873=FACE_BOUND('',#6112,.T.);
#6874=FACE_BOUND('',#6113,.T.);
#6875=FACE_BOUND('',#6114,.T.);
#6876=FACE_BOUND('',#6115,.T.);
#6877=FACE_BOUND('',#6116,.T.);
#6878=FACE_BOUND('',#6117,.T.);
#6879=FACE_BOUND('',#6118,.T.);
#6880=FACE_BOUND('',#6119,.T.);
#6881=FACE_BOUND('',#6120,.T.);
#6882=FACE_BOUND('',#6121,.T.);
#6883=FACE_BOUND('',#6122,.T.);
#6884=FACE_BOUND('',#6123,.T.);
#6885=FACE_BOUND('',#6124,.T.);
#6886=FACE_BOUND('',#6125,.T.);
#6887=FACE_BOUND('',#6126,.T.);
#6888=FACE_BOUND('',#6127,.T.);
#6889=FACE_BOUND('',#6128,.T.);
#6890=FACE_BOUND('',#6129,.T.);
#6891=FACE_BOUND('',#6130,.T.);
#6892=FACE_BOUND('',#6131,.T.);
#6893=FACE_BOUND('',#6132,.T.);
#6894=FACE_BOUND('',#6133,.T.);
#6895=FACE_BOUND('',#6134,.T.);
#7475=CYLINDRICAL_SURFACE('',#8240,0.0115);
#7476=CYLINDRICAL_SURFACE('',#8247,0.0125);
#7477=CYLINDRICAL_SURFACE('',#8288,0.016);
#7478=CYLINDRICAL_SURFACE('',#8412,0.013);
#7479=CYLINDRICAL_SURFACE('',#8416,0.0175);
#7480=CYLINDRICAL_SURFACE('',#8438,0.013);
#7481=CYLINDRICAL_SURFACE('',#8442,0.013);
#7482=CYLINDRICAL_SURFACE('',#8446,0.013);
#7483=CYLINDRICAL_SURFACE('',#8450,0.013);
#7484=CYLINDRICAL_SURFACE('',#8454,0.013);
#7485=CYLINDRICAL_SURFACE('',#8458,0.013);
#7486=CYLINDRICAL_SURFACE('',#8462,0.013);
#7487=CYLINDRICAL_SURFACE('',#8466,0.013);
#7488=CYLINDRICAL_SURFACE('',#8470,0.013);
#7489=CYLINDRICAL_SURFACE('',#8474,0.013);
#7490=CYLINDRICAL_SURFACE('',#8478,0.013);
#7491=CYLINDRICAL_SURFACE('',#8482,0.013);
#7492=CYLINDRICAL_SURFACE('',#8486,0.013);
#7493=CYLINDRICAL_SURFACE('',#8490,0.013);
#7494=CYLINDRICAL_SURFACE('',#8494,0.013);
#7495=CYLINDRICAL_SURFACE('',#8498,0.013);
#7496=CYLINDRICAL_SURFACE('',#8502,0.013);
#7497=CYLINDRICAL_SURFACE('',#8506,0.013);
#7498=CYLINDRICAL_SURFACE('',#8510,0.013);
#7499=CYLINDRICAL_SURFACE('',#8514,0.0175);
#7500=CYLINDRICAL_SURFACE('',#8540,0.0165);
#7664=ADVANCED_FACE('',(#6714,#6715),#7475,.F.);
#7665=ADVANCED_FACE('',(#6716,#6717),#888,.F.);
#7666=ADVANCED_FACE('',(#6718,#6719),#889,.F.);
#7667=ADVANCED_FACE('',(#6720,#6721),#7476,.T.);
#7668=ADVANCED_FACE('',(#6722,#6723),#7477,.T.);
#7669=ADVANCED_FACE('',(#6724),#890,.T.);
#7670=ADVANCED_FACE('',(#6725),#891,.T.);
#7671=ADVANCED_FACE('',(#6726),#892,.F.);
#7672=ADVANCED_FACE('',(#6727),#893,.T.);
#7673=ADVANCED_FACE('',(#6728),#894,.T.);
#7674=ADVANCED_FACE('',(#6729),#895,.T.);
#7675=ADVANCED_FACE('',(#6730),#896,.F.);
#7676=ADVANCED_FACE('',(#6731),#897,.T.);
#7677=ADVANCED_FACE('',(#6732),#898,.T.);
#7678=ADVANCED_FACE('',(#6733),#899,.T.);
#7679=ADVANCED_FACE('',(#6734),#900,.F.);
#7680=ADVANCED_FACE('',(#6735),#901,.T.);
#7681=ADVANCED_FACE('',(#6736),#902,.T.);
#7682=ADVANCED_FACE('',(#6737),#903,.T.);
#7683=ADVANCED_FACE('',(#6738),#904,.F.);
#7684=ADVANCED_FACE('',(#6739),#905,.T.);
#7685=ADVANCED_FACE('',(#6740),#906,.T.);
#7686=ADVANCED_FACE('',(#6741),#907,.T.);
#7687=ADVANCED_FACE('',(#6742),#908,.F.);
#7688=ADVANCED_FACE('',(#6743),#909,.T.);
#7689=ADVANCED_FACE('',(#6744),#910,.T.);
#7690=ADVANCED_FACE('',(#6745),#911,.T.);
#7691=ADVANCED_FACE('',(#6746),#912,.F.);
#7692=ADVANCED_FACE('',(#6747),#913,.T.);
#7693=ADVANCED_FACE('',(#6748),#914,.T.);
#7694=ADVANCED_FACE('',(#6749),#915,.T.);
#7695=ADVANCED_FACE('',(#6750),#916,.F.);
#7696=ADVANCED_FACE('',(#6751),#917,.T.);
#7697=ADVANCED_FACE('',(#6752),#918,.T.);
#7698=ADVANCED_FACE('',(#6753),#919,.T.);
#7699=ADVANCED_FACE('',(#6754),#920,.F.);
#7700=ADVANCED_FACE('',(#6755),#921,.T.);
#7701=ADVANCED_FACE('',(#6756),#922,.T.);
#7702=ADVANCED_FACE('',(#6757),#923,.T.);
#7703=ADVANCED_FACE('',(#6758),#924,.F.);
#7704=ADVANCED_FACE('',(#6759),#925,.T.);
#7705=ADVANCED_FACE('',(#6760),#926,.T.);
#7706=ADVANCED_FACE('',(#6761),#927,.T.);
#7707=ADVANCED_FACE('',(#6762),#928,.F.);
#7708=ADVANCED_FACE('',(#6763),#929,.T.);
#7709=ADVANCED_FACE('',(#6764),#930,.T.);
#7710=ADVANCED_FACE('',(#6765),#931,.T.);
#7711=ADVANCED_FACE('',(#6766),#932,.F.);
#7712=ADVANCED_FACE('',(#6767),#933,.T.);
#7713=ADVANCED_FACE('',(#6768),#934,.T.);
#7714=ADVANCED_FACE('',(#6769),#935,.T.);
#7715=ADVANCED_FACE('',(#6770),#936,.F.);
#7716=ADVANCED_FACE('',(#6771),#937,.T.);
#7717=ADVANCED_FACE('',(#6772),#938,.T.);
#7718=ADVANCED_FACE('',(#6773),#939,.T.);
#7719=ADVANCED_FACE('',(#6774),#940,.F.);
#7720=ADVANCED_FACE('',(#6775),#941,.T.);
#7721=ADVANCED_FACE('',(#6776),#942,.T.);
#7722=ADVANCED_FACE('',(#6777),#943,.T.);
#7723=ADVANCED_FACE('',(#6778),#944,.F.);
#7724=ADVANCED_FACE('',(#6779),#945,.T.);
#7725=ADVANCED_FACE('',(#6780),#946,.T.);
#7726=ADVANCED_FACE('',(#6781),#947,.T.);
#7727=ADVANCED_FACE('',(#6782),#948,.F.);
#7728=ADVANCED_FACE('',(#6783),#949,.T.);
#7729=ADVANCED_FACE('',(#6784),#950,.T.);
#7730=ADVANCED_FACE('',(#6785),#951,.T.);
#7731=ADVANCED_FACE('',(#6786),#952,.F.);
#7732=ADVANCED_FACE('',(#6787),#953,.T.);
#7733=ADVANCED_FACE('',(#6788),#954,.T.);
#7734=ADVANCED_FACE('',(#6789),#955,.T.);
#7735=ADVANCED_FACE('',(#6790),#956,.F.);
#7736=ADVANCED_FACE('',(#6791),#957,.T.);
#7737=ADVANCED_FACE('',(#6792),#958,.T.);
#7738=ADVANCED_FACE('',(#6793),#959,.T.);
#7739=ADVANCED_FACE('',(#6794),#960,.F.);
#7740=ADVANCED_FACE('',(#6795),#961,.T.);
#7741=ADVANCED_FACE('',(#6796),#962,.T.);
#7742=ADVANCED_FACE('',(#6797),#963,.T.);
#7743=ADVANCED_FACE('',(#6798),#964,.F.);
#7744=ADVANCED_FACE('',(#6799),#965,.T.);
#7745=ADVANCED_FACE('',(#6800),#966,.T.);
#7746=ADVANCED_FACE('',(#6801),#967,.T.);
#7747=ADVANCED_FACE('',(#6802),#968,.F.);
#7748=ADVANCED_FACE('',(#6803),#969,.T.);
#7749=ADVANCED_FACE('',(#6804,#6805),#970,.F.);
#7750=ADVANCED_FACE('',(#6806),#7478,.T.);
#7751=ADVANCED_FACE('',(#6807),#971,.F.);
#7752=ADVANCED_FACE('',(#6808),#972,.F.);
#7753=ADVANCED_FACE('',(#6809,#6810),#7479,.T.);
#7754=ADVANCED_FACE('',(#6811),#7480,.T.);
#7755=ADVANCED_FACE('',(#6812),#973,.F.);
#7756=ADVANCED_FACE('',(#6813),#974,.F.);
#7757=ADVANCED_FACE('',(#6814),#7481,.T.);
#7758=ADVANCED_FACE('',(#6815),#975,.F.);
#7759=ADVANCED_FACE('',(#6816),#976,.F.);
#7760=ADVANCED_FACE('',(#6817),#7482,.T.);
#7761=ADVANCED_FACE('',(#6818),#977,.F.);
#7762=ADVANCED_FACE('',(#6819),#978,.F.);
#7763=ADVANCED_FACE('',(#6820),#7483,.T.);
#7764=ADVANCED_FACE('',(#6821),#979,.F.);
#7765=ADVANCED_FACE('',(#6822),#980,.F.);
#7766=ADVANCED_FACE('',(#6823),#7484,.T.);
#7767=ADVANCED_FACE('',(#6824),#981,.F.);
#7768=ADVANCED_FACE('',(#6825),#982,.F.);
#7769=ADVANCED_FACE('',(#6826),#7485,.T.);
#7770=ADVANCED_FACE('',(#6827),#983,.F.);
#7771=ADVANCED_FACE('',(#6828),#984,.F.);
#7772=ADVANCED_FACE('',(#6829),#7486,.T.);
#7773=ADVANCED_FACE('',(#6830),#985,.F.);
#7774=ADVANCED_FACE('',(#6831),#986,.F.);
#7775=ADVANCED_FACE('',(#6832),#7487,.T.);
#7776=ADVANCED_FACE('',(#6833),#987,.F.);
#7777=ADVANCED_FACE('',(#6834),#988,.F.);
#7778=ADVANCED_FACE('',(#6835),#7488,.T.);
#7779=ADVANCED_FACE('',(#6836),#989,.F.);
#7780=ADVANCED_FACE('',(#6837),#990,.F.);
#7781=ADVANCED_FACE('',(#6838),#7489,.T.);
#7782=ADVANCED_FACE('',(#6839),#991,.F.);
#7783=ADVANCED_FACE('',(#6840),#992,.F.);
#7784=ADVANCED_FACE('',(#6841),#7490,.T.);
#7785=ADVANCED_FACE('',(#6842),#993,.F.);
#7786=ADVANCED_FACE('',(#6843),#994,.F.);
#7787=ADVANCED_FACE('',(#6844),#7491,.T.);
#7788=ADVANCED_FACE('',(#6845),#995,.F.);
#7789=ADVANCED_FACE('',(#6846),#996,.F.);
#7790=ADVANCED_FACE('',(#6847),#7492,.T.);
#7791=ADVANCED_FACE('',(#6848),#997,.F.);
#7792=ADVANCED_FACE('',(#6849),#998,.F.);
#7793=ADVANCED_FACE('',(#6850),#7493,.T.);
#7794=ADVANCED_FACE('',(#6851),#999,.F.);
#7795=ADVANCED_FACE('',(#6852),#1000,.F.);
#7796=ADVANCED_FACE('',(#6853),#7494,.T.);
#7797=ADVANCED_FACE('',(#6854),#1001,.F.);
#7798=ADVANCED_FACE('',(#6855),#1002,.F.);
#7799=ADVANCED_FACE('',(#6856),#7495,.T.);
#7800=ADVANCED_FACE('',(#6857),#1003,.F.);
#7801=ADVANCED_FACE('',(#6858),#1004,.F.);
#7802=ADVANCED_FACE('',(#6859),#7496,.T.);
#7803=ADVANCED_FACE('',(#6860),#1005,.F.);
#7804=ADVANCED_FACE('',(#6861),#1006,.F.);
#7805=ADVANCED_FACE('',(#6862),#7497,.T.);
#7806=ADVANCED_FACE('',(#6863),#1007,.F.);
#7807=ADVANCED_FACE('',(#6864),#1008,.F.);
#7808=ADVANCED_FACE('',(#6865),#7498,.T.);
#7809=ADVANCED_FACE('',(#6866),#1009,.F.);
#7810=ADVANCED_FACE('',(#6867),#1010,.F.);
#7811=ADVANCED_FACE('',(#6868,#6869),#7499,.T.);
#7812=ADVANCED_FACE('',(#6870),#1011,.T.);
#7813=ADVANCED_FACE('',(#6871),#1012,.T.);
#7814=ADVANCED_FACE('',(#6872,#6873),#1013,.F.);
#7815=ADVANCED_FACE('',(#6874),#1014,.T.);
#7816=ADVANCED_FACE('',(#6875),#1015,.T.);
#7817=ADVANCED_FACE('',(#6876),#1016,.T.);
#7818=ADVANCED_FACE('',(#6877),#1017,.T.);
#7819=ADVANCED_FACE('',(#6878),#1018,.T.);
#7820=ADVANCED_FACE('',(#6879),#1019,.T.);
#7821=ADVANCED_FACE('',(#6880),#1020,.T.);
#7822=ADVANCED_FACE('',(#6881),#1021,.T.);
#7823=ADVANCED_FACE('',(#6882),#1022,.T.);
#7824=ADVANCED_FACE('',(#6883),#1023,.T.);
#7825=ADVANCED_FACE('',(#6884),#1024,.T.);
#7826=ADVANCED_FACE('',(#6885),#1025,.T.);
#7827=ADVANCED_FACE('',(#6886),#1026,.T.);
#7828=ADVANCED_FACE('',(#6887),#1027,.T.);
#7829=ADVANCED_FACE('',(#6888),#1028,.T.);
#7830=ADVANCED_FACE('',(#6889),#1029,.T.);
#7831=ADVANCED_FACE('',(#6890),#1030,.T.);
#7832=ADVANCED_FACE('',(#6891),#1031,.T.);
#7833=ADVANCED_FACE('',(#6892,#6893),#1032,.F.);
#7834=ADVANCED_FACE('',(#6894,#6895),#7500,.T.);
#8168=CLOSED_SHELL('',(#7664,#7665,#7666,#7667,#7668,#7669,#7670,#7671,
#7672,#7673,#7674,#7675,#7676,#7677,#7678,#7679,#7680,#7681,#7682,#7683,
#7684,#7685,#7686,#7687,#7688,#7689,#7690,#7691,#7692,#7693,#7694,#7695,
#7696,#7697,#7698,#7699,#7700,#7701,#7702,#7703,#7704,#7705,#7706,#7707,
#7708,#7709,#7710,#7711,#7712,#7713,#7714,#7715,#7716,#7717,#7718,#7719,
#7720,#7721,#7722,#7723,#7724,#7725,#7726,#7727,#7728,#7729,#7730,#7731,
#7732,#7733,#7734,#7735,#7736,#7737,#7738,#7739,#7740,#7741,#7742,#7743,
#7744,#7745,#7746,#7747,#7748,#7749,#7750,#7751,#7752,#7753,#7754,#7755,
#7756,#7757,#7758,#7759,#7760,#7761,#7762,#7763,#7764,#7765,#7766,#7767,
#7768,#7769,#7770,#7771,#7772,#7773,#7774,#7775,#7776,#7777,#7778,#7779,
#7780,#7781,#7782,#7783,#7784,#7785,#7786,#7787,#7788,#7789,#7790,#7791,
#7792,#7793,#7794,#7795,#7796,#7797,#7798,#7799,#7800,#7801,#7802,#7803,
#7804,#7805,#7806,#7807,#7808,#7809,#7810,#7811,#7812,#7813,#7814,#7815,
#7816,#7817,#7818,#7819,#7820,#7821,#7822,#7823,#7824,#7825,#7826,#7827,
#7828,#7829,#7830,#7831,#7832,#7833,#7834));
#8174=STYLED_ITEM('',(#8180),#8219);
#8180=PRESENTATION_STYLE_ASSIGNMENT((#8186));
#8186=SURFACE_STYLE_USAGE(.BOTH.,#8192);
#8192=SURFACE_SIDE_STYLE('',(#8198));
#8198=SURFACE_STYLE_FILL_AREA(#8204);
#8204=FILL_AREA_STYLE('',(#8210));
#8210=FILL_AREA_STYLE_COLOUR('',#8216);
#8216=COLOUR_RGB('', 0.66274510, 0.83137255, 0.94901961);
#8219=MANIFOLD_SOLID_BREP('cassette body__ DE    15749',#8168);
#8226=SHAPE_DEFINITION_REPRESENTATION(#18828,#8233);
#8233=SHAPE_REPRESENTATION('cassette body__ DE    15749',(#8239),#18811);
#8239=AXIS2_PLACEMENT_3D('',#11098,#9192,#9193);
#8240=AXIS2_PLACEMENT_3D('',#11099,#9194,#9195);
#8241=AXIS2_PLACEMENT_3D('',#11100,#9196,#9197);
#8242=AXIS2_PLACEMENT_3D('',#11102,#9198,#9199);
#8243=AXIS2_PLACEMENT_3D('',#11104,#9200,#9201);
#8244=AXIS2_PLACEMENT_3D('',#11105,#9202,#9203);
#8245=AXIS2_PLACEMENT_3D('',#11107,#9204,#9205);
#8246=AXIS2_PLACEMENT_3D('',#11108,#9206,#9207);
#8247=AXIS2_PLACEMENT_3D('',#11110,#9208,#9209);
#8248=AXIS2_PLACEMENT_3D('',#11111,#9210,#9211);
#8249=AXIS2_PLACEMENT_3D('',#11119,#9212,#9213);
#8250=AXIS2_PLACEMENT_3D('',#11126,#9214,#9215);
#8251=AXIS2_PLACEMENT_3D('',#11133,#9216,#9217);
#8252=AXIS2_PLACEMENT_3D('',#11140,#9218,#9219);
#8253=AXIS2_PLACEMENT_3D('',#11147,#9220,#9221);
#8254=AXIS2_PLACEMENT_3D('',#11154,#9222,#9223);
#8255=AXIS2_PLACEMENT_3D('',#11161,#9224,#9225);
#8256=AXIS2_PLACEMENT_3D('',#11168,#9226,#9227);
#8257=AXIS2_PLACEMENT_3D('',#11175,#9228,#9229);
#8258=AXIS2_PLACEMENT_3D('',#11182,#9230,#9231);
#8259=AXIS2_PLACEMENT_3D('',#11189,#9232,#9233);
#8260=AXIS2_PLACEMENT_3D('',#11196,#9234,#9235);
#8261=AXIS2_PLACEMENT_3D('',#11203,#9236,#9237);
#8262=AXIS2_PLACEMENT_3D('',#11210,#9238,#9239);
#8263=AXIS2_PLACEMENT_3D('',#11217,#9240,#9241);
#8264=AXIS2_PLACEMENT_3D('',#11224,#9242,#9243);
#8265=AXIS2_PLACEMENT_3D('',#11231,#9244,#9245);
#8266=AXIS2_PLACEMENT_3D('',#11238,#9246,#9247);
#8267=AXIS2_PLACEMENT_3D('',#11245,#9248,#9249);
#8268=AXIS2_PLACEMENT_3D('',#11252,#9250,#9251);
#8269=AXIS2_PLACEMENT_3D('',#11259,#9252,#9253);
#8270=AXIS2_PLACEMENT_3D('',#11266,#9254,#9255);
#8271=AXIS2_PLACEMENT_3D('',#11273,#9256,#9257);
#8272=AXIS2_PLACEMENT_3D('',#11280,#9258,#9259);
#8273=AXIS2_PLACEMENT_3D('',#11287,#9260,#9261);
#8274=AXIS2_PLACEMENT_3D('',#11294,#9262,#9263);
#8275=AXIS2_PLACEMENT_3D('',#11301,#9264,#9265);
#8276=AXIS2_PLACEMENT_3D('',#11308,#9266,#9267);
#8277=AXIS2_PLACEMENT_3D('',#11315,#9268,#9269);
#8278=AXIS2_PLACEMENT_3D('',#11322,#9270,#9271);
#8279=AXIS2_PLACEMENT_3D('',#11329,#9272,#9273);
#8280=AXIS2_PLACEMENT_3D('',#11336,#9274,#9275);
#8281=AXIS2_PLACEMENT_3D('',#11343,#9276,#9277);
#8282=AXIS2_PLACEMENT_3D('',#11350,#9278,#9279);
#8283=AXIS2_PLACEMENT_3D('',#11357,#9280,#9281);
#8284=AXIS2_PLACEMENT_3D('',#11364,#9282,#9283);
#8285=AXIS2_PLACEMENT_3D('',#11371,#9284,#9285);
#8286=AXIS2_PLACEMENT_3D('',#11378,#9286,#9287);
#8287=AXIS2_PLACEMENT_3D('',#11385,#9288,#9289);
#8288=AXIS2_PLACEMENT_3D('',#11391,#9290,#9291);
#8289=AXIS2_PLACEMENT_3D('',#11392,#9292,#9293);
#8290=AXIS2_PLACEMENT_3D('',#11394,#9294,#9295);
#8291=AXIS2_PLACEMENT_3D('',#11400,#9296,#9297);
#8292=AXIS2_PLACEMENT_3D('',#11406,#9298,#9299);
#8293=AXIS2_PLACEMENT_3D('',#11421,#9300,#9301);
#8294=AXIS2_PLACEMENT_3D('',#11422,#9302,#9303);
#8295=AXIS2_PLACEMENT_3D('',#11438,#9304,#9305);
#8296=AXIS2_PLACEMENT_3D('',#11453,#9306,#9307);
#8297=AXIS2_PLACEMENT_3D('',#11454,#9308,#9309);
#8298=AXIS2_PLACEMENT_3D('',#11460,#9310,#9311);
#8299=AXIS2_PLACEMENT_3D('',#11475,#9312,#9313);
#8300=AXIS2_PLACEMENT_3D('',#11481,#9314,#9315);
#8301=AXIS2_PLACEMENT_3D('',#11492,#9316,#9317);
#8302=AXIS2_PLACEMENT_3D('',#11507,#9318,#9319);
#8303=AXIS2_PLACEMENT_3D('',#11508,#9320,#9321);
#8304=AXIS2_PLACEMENT_3D('',#11514,#9322,#9323);
#8305=AXIS2_PLACEMENT_3D('',#11529,#9324,#9325);
#8306=AXIS2_PLACEMENT_3D('',#11535,#9326,#9327);
#8307=AXIS2_PLACEMENT_3D('',#11546,#9328,#9329);
#8308=AXIS2_PLACEMENT_3D('',#11561,#9330,#9331);
#8309=AXIS2_PLACEMENT_3D('',#11562,#9332,#9333);
#8310=AXIS2_PLACEMENT_3D('',#11568,#9334,#9335);
#8311=AXIS2_PLACEMENT_3D('',#11583,#9336,#9337);
#8312=AXIS2_PLACEMENT_3D('',#11589,#9338,#9339);
#8313=AXIS2_PLACEMENT_3D('',#11600,#9340,#9341);
#8314=AXIS2_PLACEMENT_3D('',#11615,#9342,#9343);
#8315=AXIS2_PLACEMENT_3D('',#11616,#9344,#9345);
#8316=AXIS2_PLACEMENT_3D('',#11622,#9346,#9347);
#8317=AXIS2_PLACEMENT_3D('',#11637,#9348,#9349);
#8318=AXIS2_PLACEMENT_3D('',#11643,#9350,#9351);
#8319=AXIS2_PLACEMENT_3D('',#11654,#9352,#9353);
#8320=AXIS2_PLACEMENT_3D('',#11669,#9354,#9355);
#8321=AXIS2_PLACEMENT_3D('',#11670,#9356,#9357);
#8322=AXIS2_PLACEMENT_3D('',#11676,#9358,#9359);
#8323=AXIS2_PLACEMENT_3D('',#11691,#9360,#9361);
#8324=AXIS2_PLACEMENT_3D('',#11697,#9362,#9363);
#8325=AXIS2_PLACEMENT_3D('',#11708,#9364,#9365);
#8326=AXIS2_PLACEMENT_3D('',#11723,#9366,#9367);
#8327=AXIS2_PLACEMENT_3D('',#11724,#9368,#9369);
#8328=AXIS2_PLACEMENT_3D('',#11730,#9370,#9371);
#8329=AXIS2_PLACEMENT_3D('',#11745,#9372,#9373);
#8330=AXIS2_PLACEMENT_3D('',#11751,#9374,#9375);
#8331=AXIS2_PLACEMENT_3D('',#11762,#9376,#9377);
#8332=AXIS2_PLACEMENT_3D('',#11777,#9378,#9379);
#8333=AXIS2_PLACEMENT_3D('',#11778,#9380,#9381);
#8334=AXIS2_PLACEMENT_3D('',#11784,#9382,#9383);
#8335=AXIS2_PLACEMENT_3D('',#11799,#9384,#9385);
#8336=AXIS2_PLACEMENT_3D('',#11805,#9386,#9387);
#8337=AXIS2_PLACEMENT_3D('',#11816,#9388,#9389);
#8338=AXIS2_PLACEMENT_3D('',#11831,#9390,#9391);
#8339=AXIS2_PLACEMENT_3D('',#11832,#9392,#9393);
#8340=AXIS2_PLACEMENT_3D('',#11838,#9394,#9395);
#8341=AXIS2_PLACEMENT_3D('',#11853,#9396,#9397);
#8342=AXIS2_PLACEMENT_3D('',#11859,#9398,#9399);
#8343=AXIS2_PLACEMENT_3D('',#11870,#9400,#9401);
#8344=AXIS2_PLACEMENT_3D('',#11885,#9402,#9403);
#8345=AXIS2_PLACEMENT_3D('',#11886,#9404,#9405);
#8346=AXIS2_PLACEMENT_3D('',#11892,#9406,#9407);
#8347=AXIS2_PLACEMENT_3D('',#11907,#9408,#9409);
#8348=AXIS2_PLACEMENT_3D('',#11913,#9410,#9411);
#8349=AXIS2_PLACEMENT_3D('',#11924,#9412,#9413);
#8350=AXIS2_PLACEMENT_3D('',#11939,#9414,#9415);
#8351=AXIS2_PLACEMENT_3D('',#11940,#9416,#9417);
#8352=AXIS2_PLACEMENT_3D('',#11946,#9418,#9419);
#8353=AXIS2_PLACEMENT_3D('',#11961,#9420,#9421);
#8354=AXIS2_PLACEMENT_3D('',#11967,#9422,#9423);
#8355=AXIS2_PLACEMENT_3D('',#11978,#9424,#9425);
#8356=AXIS2_PLACEMENT_3D('',#11993,#9426,#9427);
#8357=AXIS2_PLACEMENT_3D('',#11994,#9428,#9429);
#8358=AXIS2_PLACEMENT_3D('',#12000,#9430,#9431);
#8359=AXIS2_PLACEMENT_3D('',#12015,#9432,#9433);
#8360=AXIS2_PLACEMENT_3D('',#12021,#9434,#9435);
#8361=AXIS2_PLACEMENT_3D('',#12032,#9436,#9437);
#8362=AXIS2_PLACEMENT_3D('',#12047,#9438,#9439);
#8363=AXIS2_PLACEMENT_3D('',#12048,#9440,#9441);
#8364=AXIS2_PLACEMENT_3D('',#12054,#9442,#9443);
#8365=AXIS2_PLACEMENT_3D('',#12069,#9444,#9445);
#8366=AXIS2_PLACEMENT_3D('',#12075,#9446,#9447);
#8367=AXIS2_PLACEMENT_3D('',#12086,#9448,#9449);
#8368=AXIS2_PLACEMENT_3D('',#12101,#9450,#9451);
#8369=AXIS2_PLACEMENT_3D('',#12102,#9452,#9453);
#8370=AXIS2_PLACEMENT_3D('',#12108,#9454,#9455);
#8371=AXIS2_PLACEMENT_3D('',#12123,#9456,#9457);
#8372=AXIS2_PLACEMENT_3D('',#12129,#9458,#9459);
#8373=AXIS2_PLACEMENT_3D('',#12140,#9460,#9461);
#8374=AXIS2_PLACEMENT_3D('',#12155,#9462,#9463);
#8375=AXIS2_PLACEMENT_3D('',#12156,#9464,#9465);
#8376=AXIS2_PLACEMENT_3D('',#12162,#9466,#9467);
#8377=AXIS2_PLACEMENT_3D('',#12177,#9468,#9469);
#8378=AXIS2_PLACEMENT_3D('',#12183,#9470,#9471);
#8379=AXIS2_PLACEMENT_3D('',#12194,#9472,#9473);
#8380=AXIS2_PLACEMENT_3D('',#12209,#9474,#9475);
#8381=AXIS2_PLACEMENT_3D('',#12210,#9476,#9477);
#8382=AXIS2_PLACEMENT_3D('',#12216,#9478,#9479);
#8383=AXIS2_PLACEMENT_3D('',#12231,#9480,#9481);
#8384=AXIS2_PLACEMENT_3D('',#12237,#9482,#9483);
#8385=AXIS2_PLACEMENT_3D('',#12248,#9484,#9485);
#8386=AXIS2_PLACEMENT_3D('',#12263,#9486,#9487);
#8387=AXIS2_PLACEMENT_3D('',#12264,#9488,#9489);
#8388=AXIS2_PLACEMENT_3D('',#12270,#9490,#9491);
#8389=AXIS2_PLACEMENT_3D('',#12285,#9492,#9493);
#8390=AXIS2_PLACEMENT_3D('',#12291,#9494,#9495);
#8391=AXIS2_PLACEMENT_3D('',#12302,#9496,#9497);
#8392=AXIS2_PLACEMENT_3D('',#12317,#9498,#9499);
#8393=AXIS2_PLACEMENT_3D('',#12318,#9500,#9501);
#8394=AXIS2_PLACEMENT_3D('',#12324,#9502,#9503);
#8395=AXIS2_PLACEMENT_3D('',#12339,#9504,#9505);
#8396=AXIS2_PLACEMENT_3D('',#12345,#9506,#9507);
#8397=AXIS2_PLACEMENT_3D('',#12356,#9508,#9509);
#8398=AXIS2_PLACEMENT_3D('',#12371,#9510,#9511);
#8399=AXIS2_PLACEMENT_3D('',#12372,#9512,#9513);
#8400=AXIS2_PLACEMENT_3D('',#12378,#9514,#9515);
#8401=AXIS2_PLACEMENT_3D('',#12393,#9516,#9517);
#8402=AXIS2_PLACEMENT_3D('',#12399,#9518,#9519);
#8403=AXIS2_PLACEMENT_3D('',#12410,#9520,#9521);
#8404=AXIS2_PLACEMENT_3D('',#12425,#9522,#9523);
#8405=AXIS2_PLACEMENT_3D('',#12426,#9524,#9525);
#8406=AXIS2_PLACEMENT_3D('',#12432,#9526,#9527);
#8407=AXIS2_PLACEMENT_3D('',#12447,#9528,#9529);
#8408=AXIS2_PLACEMENT_3D('',#12453,#9530,#9531);
#8409=AXIS2_PLACEMENT_3D('',#12464,#9532,#9533);
#8410=AXIS2_PLACEMENT_3D('',#12474,#9534,#9535);
#8411=AXIS2_PLACEMENT_3D('',#12475,#9536,#9537);
#8412=AXIS2_PLACEMENT_3D('',#12477,#9538,#9539);
#8413=AXIS2_PLACEMENT_3D('',#12478,#9540,#9541);
#8414=AXIS2_PLACEMENT_3D('',#12479,#9542,#9543);
#8415=AXIS2_PLACEMENT_3D('',#12489,#9544,#9545);
#8416=AXIS2_PLACEMENT_3D('',#12499,#9546,#9547);
#8417=AXIS2_PLACEMENT_3D('',#12505,#9548,#9549);
#8418=AXIS2_PLACEMENT_3D('',#12516,#9550,#9551);
#8419=AXIS2_PLACEMENT_3D('',#12527,#9552,#9553);
#8420=AXIS2_PLACEMENT_3D('',#12538,#9554,#9555);
#8421=AXIS2_PLACEMENT_3D('',#12549,#9556,#9557);
#8422=AXIS2_PLACEMENT_3D('',#12560,#9558,#9559);
#8423=AXIS2_PLACEMENT_3D('',#12571,#9560,#9561);
#8424=AXIS2_PLACEMENT_3D('',#12582,#9562,#9563);
#8425=AXIS2_PLACEMENT_3D('',#12593,#9564,#9565);
#8426=AXIS2_PLACEMENT_3D('',#12604,#9566,#9567);
#8427=AXIS2_PLACEMENT_3D('',#12605,#9568,#9569);
#8428=AXIS2_PLACEMENT_3D('',#12616,#9570,#9571);
#8429=AXIS2_PLACEMENT_3D('',#12627,#9572,#9573);
#8430=AXIS2_PLACEMENT_3D('',#12638,#9574,#9575);
#8431=AXIS2_PLACEMENT_3D('',#12649,#9576,#9577);
#8432=AXIS2_PLACEMENT_3D('',#12660,#9578,#9579);
#8433=AXIS2_PLACEMENT_3D('',#12671,#9580,#9581);
#8434=AXIS2_PLACEMENT_3D('',#12682,#9582,#9583);
#8435=AXIS2_PLACEMENT_3D('',#12693,#9584,#9585);
#8436=AXIS2_PLACEMENT_3D('',#12704,#9586,#9587);
#8437=AXIS2_PLACEMENT_3D('',#12710,#9588,#9589);
#8438=AXIS2_PLACEMENT_3D('',#12712,#9590,#9591);
#8439=AXIS2_PLACEMENT_3D('',#12713,#9592,#9593);
#8440=AXIS2_PLACEMENT_3D('',#12714,#9594,#9595);
#8441=AXIS2_PLACEMENT_3D('',#12719,#9596,#9597);
#8442=AXIS2_PLACEMENT_3D('',#12724,#9598,#9599);
#8443=AXIS2_PLACEMENT_3D('',#12725,#9600,#9601);
#8444=AXIS2_PLACEMENT_3D('',#12726,#9602,#9603);
#8445=AXIS2_PLACEMENT_3D('',#12731,#9604,#9605);
#8446=AXIS2_PLACEMENT_3D('',#12736,#9606,#9607);
#8447=AXIS2_PLACEMENT_3D('',#12737,#9608,#9609);
#8448=AXIS2_PLACEMENT_3D('',#12738,#9610,#9611);
#8449=AXIS2_PLACEMENT_3D('',#12743,#9612,#9613);
#8450=AXIS2_PLACEMENT_3D('',#12748,#9614,#9615);
#8451=AXIS2_PLACEMENT_3D('',#12749,#9616,#9617);
#8452=AXIS2_PLACEMENT_3D('',#12750,#9618,#9619);
#8453=AXIS2_PLACEMENT_3D('',#12755,#9620,#9621);
#8454=AXIS2_PLACEMENT_3D('',#12760,#9622,#9623);
#8455=AXIS2_PLACEMENT_3D('',#12761,#9624,#9625);
#8456=AXIS2_PLACEMENT_3D('',#12762,#9626,#9627);
#8457=AXIS2_PLACEMENT_3D('',#12767,#9628,#9629);
#8458=AXIS2_PLACEMENT_3D('',#12772,#9630,#9631);
#8459=AXIS2_PLACEMENT_3D('',#12773,#9632,#9633);
#8460=AXIS2_PLACEMENT_3D('',#12774,#9634,#9635);
#8461=AXIS2_PLACEMENT_3D('',#12779,#9636,#9637);
#8462=AXIS2_PLACEMENT_3D('',#12784,#9638,#9639);
#8463=AXIS2_PLACEMENT_3D('',#12785,#9640,#9641);
#8464=AXIS2_PLACEMENT_3D('',#12786,#9642,#9643);
#8465=AXIS2_PLACEMENT_3D('',#12791,#9644,#9645);
#8466=AXIS2_PLACEMENT_3D('',#12796,#9646,#9647);
#8467=AXIS2_PLACEMENT_3D('',#12797,#9648,#9649);
#8468=AXIS2_PLACEMENT_3D('',#12798,#9650,#9651);
#8469=AXIS2_PLACEMENT_3D('',#12803,#9652,#9653);
#8470=AXIS2_PLACEMENT_3D('',#12808,#9654,#9655);
#8471=AXIS2_PLACEMENT_3D('',#12809,#9656,#9657);
#8472=AXIS2_PLACEMENT_3D('',#12810,#9658,#9659);
#8473=AXIS2_PLACEMENT_3D('',#12815,#9660,#9661);
#8474=AXIS2_PLACEMENT_3D('',#12820,#9662,#9663);
#8475=AXIS2_PLACEMENT_3D('',#12821,#9664,#9665);
#8476=AXIS2_PLACEMENT_3D('',#12822,#9666,#9667);
#8477=AXIS2_PLACEMENT_3D('',#12827,#9668,#9669);
#8478=AXIS2_PLACEMENT_3D('',#12832,#9670,#9671);
#8479=AXIS2_PLACEMENT_3D('',#12833,#9672,#9673);
#8480=AXIS2_PLACEMENT_3D('',#12834,#9674,#9675);
#8481=AXIS2_PLACEMENT_3D('',#12839,#9676,#9677);
#8482=AXIS2_PLACEMENT_3D('',#12844,#9678,#9679);
#8483=AXIS2_PLACEMENT_3D('',#12845,#9680,#9681);
#8484=AXIS2_PLACEMENT_3D('',#12846,#9682,#9683);
#8485=AXIS2_PLACEMENT_3D('',#12851,#9684,#9685);
#8486=AXIS2_PLACEMENT_3D('',#12856,#9686,#9687);
#8487=AXIS2_PLACEMENT_3D('',#12857,#9688,#9689);
#8488=AXIS2_PLACEMENT_3D('',#12858,#9690,#9691);
#8489=AXIS2_PLACEMENT_3D('',#12863,#9692,#9693);
#8490=AXIS2_PLACEMENT_3D('',#12868,#9694,#9695);
#8491=AXIS2_PLACEMENT_3D('',#12869,#9696,#9697);
#8492=AXIS2_PLACEMENT_3D('',#12870,#9698,#9699);
#8493=AXIS2_PLACEMENT_3D('',#12875,#9700,#9701);
#8494=AXIS2_PLACEMENT_3D('',#12880,#9702,#9703);
#8495=AXIS2_PLACEMENT_3D('',#12881,#9704,#9705);
#8496=AXIS2_PLACEMENT_3D('',#12882,#9706,#9707);
#8497=AXIS2_PLACEMENT_3D('',#12887,#9708,#9709);
#8498=AXIS2_PLACEMENT_3D('',#12892,#9710,#9711);
#8499=AXIS2_PLACEMENT_3D('',#12893,#9712,#9713);
#8500=AXIS2_PLACEMENT_3D('',#12894,#9714,#9715);
#8501=AXIS2_PLACEMENT_3D('',#12899,#9716,#9717);
#8502=AXIS2_PLACEMENT_3D('',#12904,#9718,#9719);
#8503=AXIS2_PLACEMENT_3D('',#12905,#9720,#9721);
#8504=AXIS2_PLACEMENT_3D('',#12906,#9722,#9723);
#8505=AXIS2_PLACEMENT_3D('',#12911,#9724,#9725);
#8506=AXIS2_PLACEMENT_3D('',#12916,#9726,#9727);
#8507=AXIS2_PLACEMENT_3D('',#12917,#9728,#9729);
#8508=AXIS2_PLACEMENT_3D('',#12918,#9730,#9731);
#8509=AXIS2_PLACEMENT_3D('',#12923,#9732,#9733);
#8510=AXIS2_PLACEMENT_3D('',#12928,#9734,#9735);
#8511=AXIS2_PLACEMENT_3D('',#12929,#9736,#9737);
#8512=AXIS2_PLACEMENT_3D('',#12930,#9738,#9739);
#8513=AXIS2_PLACEMENT_3D('',#12935,#9740,#9741);
#8514=AXIS2_PLACEMENT_3D('',#12940,#9742,#9743);
#8515=AXIS2_PLACEMENT_3D('',#12941,#9744,#9745);
#8516=AXIS2_PLACEMENT_3D('',#12943,#9746,#9747);
#8517=AXIS2_PLACEMENT_3D('',#12944,#9748,#9749);
#8518=AXIS2_PLACEMENT_3D('',#12945,#9750,#9751);
#8519=AXIS2_PLACEMENT_3D('',#12946,#9752,#9753);
#8520=AXIS2_PLACEMENT_3D('',#12948,#9754,#9755);
#8521=AXIS2_PLACEMENT_3D('',#12949,#9756,#9757);
#8522=AXIS2_PLACEMENT_3D('',#12950,#9758,#9759);
#8523=AXIS2_PLACEMENT_3D('',#12951,#9760,#9761);
#8524=AXIS2_PLACEMENT_3D('',#12952,#9762,#9763);
#8525=AXIS2_PLACEMENT_3D('',#12953,#9764,#9765);
#8526=AXIS2_PLACEMENT_3D('',#12954,#9766,#9767);
#8527=AXIS2_PLACEMENT_3D('',#12955,#9768,#9769);
#8528=AXIS2_PLACEMENT_3D('',#12956,#9770,#9771);
#8529=AXIS2_PLACEMENT_3D('',#12957,#9772,#9773);
#8530=AXIS2_PLACEMENT_3D('',#12958,#9774,#9775);
#8531=AXIS2_PLACEMENT_3D('',#12959,#9776,#9777);
#8532=AXIS2_PLACEMENT_3D('',#12960,#9778,#9779);
#8533=AXIS2_PLACEMENT_3D('',#12961,#9780,#9781);
#8534=AXIS2_PLACEMENT_3D('',#12962,#9782,#9783);
#8535=AXIS2_PLACEMENT_3D('',#12963,#9784,#9785);
#8536=AXIS2_PLACEMENT_3D('',#12964,#9786,#9787);
#8537=AXIS2_PLACEMENT_3D('',#12965,#9788,#9789);
#8538=AXIS2_PLACEMENT_3D('',#12966,#9790,#9791);
#8539=AXIS2_PLACEMENT_3D('',#12967,#9792,#9793);
#8540=AXIS2_PLACEMENT_3D('',#12969,#9794,#9795);
#9192=DIRECTION('',(0.,0.,1.));
#9193=DIRECTION('',(1.,0.,0.));
#9194=DIRECTION('',(1.,0.,0.));
#9195=DIRECTION('',(0.,0.,-1.));
#9196=DIRECTION('',(1.,0.,0.));
#9197=DIRECTION('',(0.,0.,-1.));
#9198=DIRECTION('',(1.,0.,0.));
#9199=DIRECTION('',(0.,0.,-1.));
#9200=DIRECTION('',(-1.,0.,0.));
#9201=DIRECTION('',(0.,0.,1.));
#9202=DIRECTION('',(-1.,0.,0.));
#9203=DIRECTION('',(0.,0.,1.));
#9204=DIRECTION('',(1.,-2.13742714109856E-17,-3.00478887951711E-17));
#9205=DIRECTION('',(-3.00478887951711E-17,0.,-1.));
#9206=DIRECTION('',(-1.,0.,0.));
#9207=DIRECTION('',(0.,0.,1.));
#9208=DIRECTION('',(-1.,0.,0.));
#9209=DIRECTION('',(0.,0.,1.));
#9210=DIRECTION('',(-1.,0.,0.));
#9211=DIRECTION('',(0.,0.,1.));
#9212=DIRECTION('',(-1.,0.,0.));
#9213=DIRECTION('',(0.,0.,1.));
#9214=DIRECTION('',(-1.,0.,0.));
#9215=DIRECTION('',(0.,0.,1.));
#9216=DIRECTION('',(-1.,0.,0.));
#9217=DIRECTION('',(0.,0.,1.));
#9218=DIRECTION('',(-1.,0.,0.));
#9219=DIRECTION('',(0.,0.,1.));
#9220=DIRECTION('',(-1.,0.,0.));
#9221=DIRECTION('',(0.,0.,1.));
#9222=DIRECTION('',(-1.,0.,0.));
#9223=DIRECTION('',(0.,0.,1.));
#9224=DIRECTION('',(-1.,0.,0.));
#9225=DIRECTION('',(0.,0.,1.));
#9226=DIRECTION('',(-1.,0.,0.));
#9227=DIRECTION('',(0.,0.,1.));
#9228=DIRECTION('',(-1.,0.,0.));
#9229=DIRECTION('',(0.,0.,1.));
#9230=DIRECTION('',(-1.,0.,0.));
#9231=DIRECTION('',(0.,0.,1.));
#9232=DIRECTION('',(-1.,0.,0.));
#9233=DIRECTION('',(0.,0.,1.));
#9234=DIRECTION('',(-1.,0.,0.));
#9235=DIRECTION('',(0.,0.,1.));
#9236=DIRECTION('',(-1.,0.,0.));
#9237=DIRECTION('',(0.,0.,1.));
#9238=DIRECTION('',(-1.,0.,0.));
#9239=DIRECTION('',(0.,0.,1.));
#9240=DIRECTION('',(-1.,0.,0.));
#9241=DIRECTION('',(0.,0.,1.));
#9242=DIRECTION('',(-1.,0.,0.));
#9243=DIRECTION('',(0.,0.,1.));
#9244=DIRECTION('',(-1.,0.,0.));
#9245=DIRECTION('',(0.,0.,1.));
#9246=DIRECTION('',(-1.,0.,0.));
#9247=DIRECTION('',(0.,0.,1.));
#9248=DIRECTION('',(-1.,0.,0.));
#9249=DIRECTION('',(0.,0.,1.));
#9250=DIRECTION('',(-1.,0.,0.));
#9251=DIRECTION('',(0.,0.,1.));
#9252=DIRECTION('',(-1.,0.,0.));
#9253=DIRECTION('',(0.,0.,1.));
#9254=DIRECTION('',(-1.,0.,0.));
#9255=DIRECTION('',(0.,0.,1.));
#9256=DIRECTION('',(-1.,0.,0.));
#9257=DIRECTION('',(0.,0.,1.));
#9258=DIRECTION('',(-1.,0.,0.));
#9259=DIRECTION('',(0.,0.,1.));
#9260=DIRECTION('',(-1.,0.,0.));
#9261=DIRECTION('',(0.,0.,1.));
#9262=DIRECTION('',(-1.,0.,0.));
#9263=DIRECTION('',(0.,0.,1.));
#9264=DIRECTION('',(-1.,0.,0.));
#9265=DIRECTION('',(0.,0.,1.));
#9266=DIRECTION('',(-1.,0.,0.));
#9267=DIRECTION('',(0.,0.,1.));
#9268=DIRECTION('',(-1.,0.,0.));
#9269=DIRECTION('',(0.,0.,1.));
#9270=DIRECTION('',(-1.,0.,0.));
#9271=DIRECTION('',(0.,0.,1.));
#9272=DIRECTION('',(-1.,0.,0.));
#9273=DIRECTION('',(0.,0.,1.));
#9274=DIRECTION('',(-1.,0.,0.));
#9275=DIRECTION('',(0.,0.,1.));
#9276=DIRECTION('',(-1.,0.,0.));
#9277=DIRECTION('',(0.,0.,1.));
#9278=DIRECTION('',(-1.,0.,0.));
#9279=DIRECTION('',(0.,0.,1.));
#9280=DIRECTION('',(-1.,0.,0.));
#9281=DIRECTION('',(0.,0.,1.));
#9282=DIRECTION('',(-1.,0.,0.));
#9283=DIRECTION('',(0.,0.,1.));
#9284=DIRECTION('',(-1.,0.,0.));
#9285=DIRECTION('',(0.,0.,1.));
#9286=DIRECTION('',(-1.,0.,0.));
#9287=DIRECTION('',(0.,0.,1.));
#9288=DIRECTION('',(-1.,0.,0.));
#9289=DIRECTION('',(0.,0.,1.));
#9290=DIRECTION('',(-1.,0.,0.));
#9291=DIRECTION('',(0.,0.,1.));
#9292=DIRECTION('',(-1.,0.,0.));
#9293=DIRECTION('',(0.,0.,1.));
#9294=DIRECTION('',(1.,0.,0.));
#9295=DIRECTION('',(0.,0.,-1.));
#9296=DIRECTION('',(1.,0.,0.));
#9297=DIRECTION('',(0.,0.,-1.));
#9298=DIRECTION('',(0.,0.,1.));
#9299=DIRECTION('',(1.,0.,0.));
#9300=DIRECTION('',(-1.,0.,0.));
#9301=DIRECTION('',(0.,0.,1.));
#9302=DIRECTION('',(-1.,0.,0.));
#9303=DIRECTION('',(0.,0.,1.));
#9304=DIRECTION('',(1.76366925757084E-19,0.309016994741914,-0.951056516175919));
#9305=DIRECTION('',(0.,0.951056516175919,0.309016994741914));
#9306=DIRECTION('',(1.,5.11915082809089E-15,2.61659684133968E-15));
#9307=DIRECTION('',(-5.11915082809089E-15,1.,0.));
#9308=DIRECTION('',(1.,0.,0.));
#9309=DIRECTION('',(0.,0.,-1.));
#9310=DIRECTION('',(4.91605234155644E-18,-0.30901699293847,0.951056516761893));
#9311=DIRECTION('',(0.,-0.951056516761893,-0.30901699293847));
#9312=DIRECTION('',(-1.,0.,0.));
#9313=DIRECTION('',(0.,0.,1.));
#9314=DIRECTION('',(-1.,0.,0.));
#9315=DIRECTION('',(0.,0.,1.));
#9316=DIRECTION('',(2.10154074524954E-18,0.587785252825749,-0.8090169939875));
#9317=DIRECTION('',(0.,0.8090169939875,0.587785252825749));
#9318=DIRECTION('',(1.,3.54488757105866E-15,2.81393787529885E-15));
#9319=DIRECTION('',(-3.54488757105866E-15,1.,0.));
#9320=DIRECTION('',(1.,0.,0.));
#9321=DIRECTION('',(0.,0.,-1.));
#9322=DIRECTION('',(2.58121594927379E-20,-0.58778525152076,0.80901699493563));
#9323=DIRECTION('',(0.,-0.80901699493563,-0.58778525152076));
#9324=DIRECTION('',(-1.,0.,0.));
#9325=DIRECTION('',(0.,0.,1.));
#9326=DIRECTION('',(-1.,0.,0.));
#9327=DIRECTION('',(0.,0.,1.));
#9328=DIRECTION('',(-9.01993783845845E-19,0.809016994935629,-0.587785251520761));
#9329=DIRECTION('',(0.,0.587785251520761,0.809016994935629));
#9330=DIRECTION('',(1.,2.93053751101568E-15,3.40384429899751E-15));
#9331=DIRECTION('',(3.40384429899751E-15,0.,-1.));
#9332=DIRECTION('',(1.,0.,0.));
#9333=DIRECTION('',(0.,0.,-1.));
#9334=DIRECTION('',(4.61321756981649E-18,-0.8090169939875,0.587785252825748));
#9335=DIRECTION('',(0.,-0.587785252825748,-0.8090169939875));
#9336=DIRECTION('',(-1.,0.,0.));
#9337=DIRECTION('',(0.,0.,1.));
#9338=DIRECTION('',(-1.,0.,0.));
#9339=DIRECTION('',(0.,0.,1.));
#9340=DIRECTION('',(5.97474930064793E-18,0.951056516761894,-0.30901699293847));
#9341=DIRECTION('',(0.,0.30901699293847,0.951056516761894));
#9342=DIRECTION('',(1.,2.72501936239058E-15,4.91547108693002E-15));
#9343=DIRECTION('',(4.91547108693002E-15,0.,-1.));
#9344=DIRECTION('',(1.,0.,0.));
#9345=DIRECTION('',(0.,0.,-1.));
#9346=DIRECTION('',(-1.90367459747866E-18,-0.951056516175919,0.309016994741914));
#9347=DIRECTION('',(0.,-0.309016994741914,-0.951056516175919));
#9348=DIRECTION('',(-1.,0.,0.));
#9349=DIRECTION('',(0.,0.,1.));
#9350=DIRECTION('',(-1.,0.,0.));
#9351=DIRECTION('',(0.,0.,1.));
#9352=DIRECTION('',(0.,1.,0.));
#9353=DIRECTION('',(0.,0.,1.));
#9354=DIRECTION('',(1.,0.,0.));
#9355=DIRECTION('',(0.,0.,-1.));
#9356=DIRECTION('',(1.,0.,0.));
#9357=DIRECTION('',(0.,0.,-1.));
#9358=DIRECTION('',(0.,-1.,0.));
#9359=DIRECTION('',(0.,0.,-1.));
#9360=DIRECTION('',(-1.,0.,0.));
#9361=DIRECTION('',(0.,0.,1.));
#9362=DIRECTION('',(-1.,0.,0.));
#9363=DIRECTION('',(0.,0.,1.));
#9364=DIRECTION('',(1.76366925757084E-19,0.951056516175919,0.309016994741914));
#9365=DIRECTION('',(0.,-0.309016994741914,0.951056516175919));
#9366=DIRECTION('',(1.,2.72501936239123E-15,4.91547108693002E-15));
#9367=DIRECTION('',(4.91547108693002E-15,0.,-1.));
#9368=DIRECTION('',(1.,0.,0.));
#9369=DIRECTION('',(0.,0.,-1.));
#9370=DIRECTION('',(4.91605234155644E-18,-0.951056516761893,-0.30901699293847));
#9371=DIRECTION('',(0.,0.30901699293847,-0.951056516761893));
#9372=DIRECTION('',(-1.,0.,0.));
#9373=DIRECTION('',(0.,0.,1.));
#9374=DIRECTION('',(-1.,0.,0.));
#9375=DIRECTION('',(0.,0.,1.));
#9376=DIRECTION('',(2.10154074524954E-18,0.8090169939875,0.587785252825749));
#9377=DIRECTION('',(0.,-0.587785252825749,0.8090169939875));
#9378=DIRECTION('',(1.,2.93053751101741E-15,3.40384429899751E-15));
#9379=DIRECTION('',(3.40384429899751E-15,0.,-1.));
#9380=DIRECTION('',(1.,0.,0.));
#9381=DIRECTION('',(0.,0.,-1.));
#9382=DIRECTION('',(2.58121594927379E-20,-0.80901699493563,-0.58778525152076));
#9383=DIRECTION('',(0.,0.58778525152076,-0.80901699493563));
#9384=DIRECTION('',(-1.,0.,0.));
#9385=DIRECTION('',(0.,0.,1.));
#9386=DIRECTION('',(-1.,0.,0.));
#9387=DIRECTION('',(0.,0.,1.));
#9388=DIRECTION('',(-9.01993783845845E-19,0.587785251520761,0.809016994935629));
#9389=DIRECTION('',(0.,-0.809016994935629,0.587785251520761));
#9390=DIRECTION('',(1.,3.54488757106004E-15,2.81393787529885E-15));
#9391=DIRECTION('',(-3.54488757106004E-15,1.,0.));
#9392=DIRECTION('',(1.,0.,0.));
#9393=DIRECTION('',(0.,0.,-1.));
#9394=DIRECTION('',(4.61321756981649E-18,-0.587785252825748,-0.8090169939875));
#9395=DIRECTION('',(0.,0.8090169939875,-0.587785252825748));
#9396=DIRECTION('',(-1.,0.,0.));
#9397=DIRECTION('',(0.,0.,1.));
#9398=DIRECTION('',(-1.,0.,0.));
#9399=DIRECTION('',(0.,0.,1.));
#9400=DIRECTION('',(5.97474930064793E-18,0.30901699293847,0.951056516761894));
#9401=DIRECTION('',(0.,-0.951056516761894,0.30901699293847));
#9402=DIRECTION('',(1.,5.11915082809161E-15,2.61659684133968E-15));
#9403=DIRECTION('',(-5.11915082809161E-15,1.,0.));
#9404=DIRECTION('',(1.,0.,0.));
#9405=DIRECTION('',(0.,0.,-1.));
#9406=DIRECTION('',(-1.90367459747866E-18,-0.309016994741914,-0.951056516175919));
#9407=DIRECTION('',(0.,0.951056516175919,-0.309016994741914));
#9408=DIRECTION('',(-1.,0.,0.));
#9409=DIRECTION('',(0.,0.,1.));
#9410=DIRECTION('',(-1.,0.,0.));
#9411=DIRECTION('',(0.,0.,1.));
#9412=DIRECTION('',(0.,0.,1.));
#9413=DIRECTION('',(1.,0.,0.));
#9414=DIRECTION('',(1.,0.,0.));
#9415=DIRECTION('',(0.,0.,-1.));
#9416=DIRECTION('',(1.,0.,0.));
#9417=DIRECTION('',(0.,0.,-1.));
#9418=DIRECTION('',(0.,0.,-1.));
#9419=DIRECTION('',(-1.,0.,0.));
#9420=DIRECTION('',(-1.,0.,0.));
#9421=DIRECTION('',(0.,0.,1.));
#9422=DIRECTION('',(-1.,0.,0.));
#9423=DIRECTION('',(0.,0.,1.));
#9424=DIRECTION('',(1.76366925757084E-19,-0.309016994741914,0.951056516175919));
#9425=DIRECTION('',(0.,-0.951056516175919,-0.309016994741914));
#9426=DIRECTION('',(1.,5.11915082809161E-15,2.61659684133999E-15));
#9427=DIRECTION('',(-5.11915082809161E-15,1.,0.));
#9428=DIRECTION('',(1.,0.,0.));
#9429=DIRECTION('',(0.,0.,-1.));
#9430=DIRECTION('',(4.91605234155644E-18,0.30901699293847,-0.951056516761893));
#9431=DIRECTION('',(0.,0.951056516761893,0.30901699293847));
#9432=DIRECTION('',(-1.,0.,0.));
#9433=DIRECTION('',(0.,0.,1.));
#9434=DIRECTION('',(-1.,0.,0.));
#9435=DIRECTION('',(0.,0.,1.));
#9436=DIRECTION('',(2.10154074524954E-18,-0.587785252825749,0.8090169939875));
#9437=DIRECTION('',(0.,-0.8090169939875,-0.587785252825749));
#9438=DIRECTION('',(1.,3.54488757106004E-15,2.81393787529969E-15));
#9439=DIRECTION('',(-3.54488757106004E-15,1.,0.));
#9440=DIRECTION('',(1.,0.,0.));
#9441=DIRECTION('',(0.,0.,-1.));
#9442=DIRECTION('',(2.58121594927379E-20,0.58778525152076,-0.80901699493563));
#9443=DIRECTION('',(0.,0.80901699493563,0.58778525152076));
#9444=DIRECTION('',(-1.,0.,0.));
#9445=DIRECTION('',(0.,0.,1.));
#9446=DIRECTION('',(-1.,0.,0.));
#9447=DIRECTION('',(0.,0.,1.));
#9448=DIRECTION('',(-9.01993783845845E-19,-0.809016994935629,0.587785251520761));
#9449=DIRECTION('',(0.,-0.587785251520761,-0.809016994935629));
#9450=DIRECTION('',(1.,2.93053751101741E-15,3.4038442990036E-15));
#9451=DIRECTION('',(3.4038442990036E-15,0.,-1.));
#9452=DIRECTION('',(1.,0.,0.));
#9453=DIRECTION('',(0.,0.,-1.));
#9454=DIRECTION('',(4.61321756981649E-18,0.8090169939875,-0.587785252825748));
#9455=DIRECTION('',(0.,0.587785252825748,0.8090169939875));
#9456=DIRECTION('',(-1.,0.,0.));
#9457=DIRECTION('',(0.,0.,1.));
#9458=DIRECTION('',(-1.,0.,0.));
#9459=DIRECTION('',(0.,0.,1.));
#9460=DIRECTION('',(5.97474930064793E-18,-0.951056516761894,0.30901699293847));
#9461=DIRECTION('',(0.,-0.30901699293847,-0.951056516761894));
#9462=DIRECTION('',(1.,2.72501936239123E-15,4.91547108691513E-15));
#9463=DIRECTION('',(4.91547108691513E-15,0.,-1.));
#9464=DIRECTION('',(1.,0.,0.));
#9465=DIRECTION('',(0.,0.,-1.));
#9466=DIRECTION('',(-1.90367459747866E-18,0.951056516175919,-0.309016994741914));
#9467=DIRECTION('',(0.,0.309016994741914,0.951056516175919));
#9468=DIRECTION('',(-1.,0.,0.));
#9469=DIRECTION('',(0.,0.,1.));
#9470=DIRECTION('',(-1.,0.,0.));
#9471=DIRECTION('',(0.,0.,1.));
#9472=DIRECTION('',(0.,-1.,0.));
#9473=DIRECTION('',(0.,0.,-1.));
#9474=DIRECTION('',(1.,0.,0.));
#9475=DIRECTION('',(0.,0.,-1.));
#9476=DIRECTION('',(1.,0.,0.));
#9477=DIRECTION('',(0.,0.,-1.));
#9478=DIRECTION('',(0.,1.,0.));
#9479=DIRECTION('',(0.,0.,1.));
#9480=DIRECTION('',(-1.,0.,0.));
#9481=DIRECTION('',(0.,0.,1.));
#9482=DIRECTION('',(-1.,0.,0.));
#9483=DIRECTION('',(0.,0.,1.));
#9484=DIRECTION('',(1.76366925757084E-19,-0.951056516175919,-0.309016994741914));
#9485=DIRECTION('',(0.,0.309016994741914,-0.951056516175919));
#9486=DIRECTION('',(1.,2.72501936239058E-15,4.91547108691514E-15));
#9487=DIRECTION('',(4.91547108691514E-15,0.,-1.));
#9488=DIRECTION('',(1.,0.,0.));
#9489=DIRECTION('',(0.,0.,-1.));
#9490=DIRECTION('',(4.91605234155644E-18,0.951056516761893,0.30901699293847));
#9491=DIRECTION('',(0.,-0.30901699293847,0.951056516761893));
#9492=DIRECTION('',(-1.,0.,0.));
#9493=DIRECTION('',(0.,0.,1.));
#9494=DIRECTION('',(-1.,0.,0.));
#9495=DIRECTION('',(0.,0.,1.));
#9496=DIRECTION('',(2.10154074524954E-18,-0.8090169939875,-0.587785252825749));
#9497=DIRECTION('',(0.,0.587785252825749,-0.8090169939875));
#9498=DIRECTION('',(1.,2.93053751101568E-15,3.4038442990036E-15));
#9499=DIRECTION('',(3.4038442990036E-15,0.,-1.));
#9500=DIRECTION('',(1.,0.,0.));
#9501=DIRECTION('',(0.,0.,-1.));
#9502=DIRECTION('',(2.58121594927379E-20,0.80901699493563,0.58778525152076));
#9503=DIRECTION('',(0.,-0.58778525152076,0.80901699493563));
#9504=DIRECTION('',(-1.,0.,0.));
#9505=DIRECTION('',(0.,0.,1.));
#9506=DIRECTION('',(-1.,0.,0.));
#9507=DIRECTION('',(0.,0.,1.));
#9508=DIRECTION('',(-9.01993783845845E-19,-0.587785251520761,-0.809016994935629));
#9509=DIRECTION('',(0.,0.809016994935629,-0.587785251520761));
#9510=DIRECTION('',(1.,3.54488757105866E-15,2.81393787529969E-15));
#9511=DIRECTION('',(-3.54488757105866E-15,1.,0.));
#9512=DIRECTION('',(1.,0.,0.));
#9513=DIRECTION('',(0.,0.,-1.));
#9514=DIRECTION('',(4.61321756981649E-18,0.587785252825748,0.8090169939875));
#9515=DIRECTION('',(0.,-0.8090169939875,0.587785252825748));
#9516=DIRECTION('',(-1.,0.,0.));
#9517=DIRECTION('',(0.,0.,1.));
#9518=DIRECTION('',(-1.,0.,0.));
#9519=DIRECTION('',(0.,0.,1.));
#9520=DIRECTION('',(5.97474930064793E-18,-0.30901699293847,-0.951056516761894));
#9521=DIRECTION('',(0.,0.951056516761894,-0.30901699293847));
#9522=DIRECTION('',(1.,5.11915082809089E-15,2.61659684133999E-15));
#9523=DIRECTION('',(-5.11915082809089E-15,1.,0.));
#9524=DIRECTION('',(1.,0.,0.));
#9525=DIRECTION('',(0.,0.,-1.));
#9526=DIRECTION('',(-1.90367459747866E-18,0.309016994741914,0.951056516175919));
#9527=DIRECTION('',(0.,-0.951056516175919,0.309016994741914));
#9528=DIRECTION('',(-1.,0.,0.));
#9529=DIRECTION('',(0.,0.,1.));
#9530=DIRECTION('',(-1.,0.,0.));
#9531=DIRECTION('',(0.,0.,1.));
#9532=DIRECTION('',(0.,0.,-1.));
#9533=DIRECTION('',(-1.,0.,0.));
#9534=DIRECTION('',(1.,0.,0.));
#9535=DIRECTION('',(0.,0.,-1.));
#9536=DIRECTION('',(-1.,0.,0.));
#9537=DIRECTION('',(0.,0.,1.));
#9538=DIRECTION('',(1.,0.,0.));
#9539=DIRECTION('',(0.,0.,-1.));
#9540=DIRECTION('',(1.,0.,0.));
#9541=DIRECTION('',(0.,0.,-1.));
#9542=DIRECTION('',(-2.99135772045791E-17,-0.130526192305464,-0.991444861362566));
#9543=DIRECTION('',(0.,0.991444861362566,-0.130526192305464));
#9544=DIRECTION('',(3.22859531325E-17,-0.430511096755578,0.902585284375005));
#9545=DIRECTION('',(0.,-0.902585284375005,-0.430511096755578));
#9546=DIRECTION('',(-1.,0.,0.));
#9547=DIRECTION('',(0.,0.,1.));
#9548=DIRECTION('',(-1.,0.,0.));
#9549=DIRECTION('',(0.,0.,1.));
#9550=DIRECTION('',(-1.,0.,0.));
#9551=DIRECTION('',(0.,0.,1.));
#9552=DIRECTION('',(-1.,0.,0.));
#9553=DIRECTION('',(0.,0.,1.));
#9554=DIRECTION('',(-1.,0.,0.));
#9555=DIRECTION('',(0.,0.,1.));
#9556=DIRECTION('',(-1.,0.,0.));
#9557=DIRECTION('',(0.,0.,1.));
#9558=DIRECTION('',(-1.,0.,0.));
#9559=DIRECTION('',(0.,0.,1.));
#9560=DIRECTION('',(-1.,0.,0.));
#9561=DIRECTION('',(0.,0.,1.));
#9562=DIRECTION('',(-1.,0.,0.));
#9563=DIRECTION('',(0.,0.,1.));
#9564=DIRECTION('',(-1.,0.,0.));
#9565=DIRECTION('',(0.,0.,1.));
#9566=DIRECTION('',(-1.,0.,0.));
#9567=DIRECTION('',(0.,0.,1.));
#9568=DIRECTION('',(-1.,0.,0.));
#9569=DIRECTION('',(0.,0.,1.));
#9570=DIRECTION('',(-1.,0.,0.));
#9571=DIRECTION('',(0.,0.,1.));
#9572=DIRECTION('',(-1.,0.,0.));
#9573=DIRECTION('',(0.,0.,1.));
#9574=DIRECTION('',(-1.,0.,0.));
#9575=DIRECTION('',(0.,0.,1.));
#9576=DIRECTION('',(-1.,0.,0.));
#9577=DIRECTION('',(0.,0.,1.));
#9578=DIRECTION('',(-1.,0.,0.));
#9579=DIRECTION('',(0.,0.,1.));
#9580=DIRECTION('',(-1.,0.,0.));
#9581=DIRECTION('',(0.,0.,1.));
#9582=DIRECTION('',(-1.,0.,0.));
#9583=DIRECTION('',(0.,0.,1.));
#9584=DIRECTION('',(-1.,0.,0.));
#9585=DIRECTION('',(0.,0.,1.));
#9586=DIRECTION('',(-1.,0.,0.));
#9587=DIRECTION('',(0.,0.,1.));
#9588=DIRECTION('',(-1.,0.,0.));
#9589=DIRECTION('',(0.,0.,1.));
#9590=DIRECTION('',(1.,0.,0.));
#9591=DIRECTION('',(0.,0.,-1.));
#9592=DIRECTION('',(1.,0.,0.));
#9593=DIRECTION('',(0.,0.,-1.));
#9594=DIRECTION('',(-6.60825936598169E-17,0.182235525591703,-0.983254907545503));
#9595=DIRECTION('',(0.,0.983254907545503,0.182235525591703));
#9596=DIRECTION('',(2.18592128542802E-17,-0.688354575657138,0.725374371047035));
#9597=DIRECTION('',(0.,-0.725374371047035,-0.688354575657138));
#9598=DIRECTION('',(1.,0.,0.));
#9599=DIRECTION('',(0.,0.,-1.));
#9600=DIRECTION('',(1.,0.,0.));
#9601=DIRECTION('',(0.,0.,-1.));
#9602=DIRECTION('',(8.04110715575716E-17,0.477158760378666,-0.878817112597322));
#9603=DIRECTION('',(0.,0.878817112597322,0.477158760378666));
#9604=DIRECTION('',(7.14896713846317E-17,-0.878817112597323,0.477158760378665));
#9605=DIRECTION('',(0.,-0.477158760378665,-0.878817112597323));
#9606=DIRECTION('',(1.,0.,0.));
#9607=DIRECTION('',(0.,0.,-1.));
#9608=DIRECTION('',(1.,0.,0.));
#9609=DIRECTION('',(0.,0.,-1.));
#9610=DIRECTION('',(1.8186512468286E-16,0.725374371047035,-0.688354575657138));
#9611=DIRECTION('',(0.,0.688354575657138,0.725374371047035));
#9612=DIRECTION('',(-4.64133914967143E-17,-0.983254907545503,0.182235525591703));
#9613=DIRECTION('',(0.,-0.182235525591703,-0.983254907545503));
#9614=DIRECTION('',(1.,0.,0.));
#9615=DIRECTION('',(0.,0.,-1.));
#9616=DIRECTION('',(1.,0.,0.));
#9617=DIRECTION('',(0.,0.,-1.));
#9618=DIRECTION('',(6.48328605787293E-17,0.902585284375005,-0.430511096755578));
#9619=DIRECTION('',(0.,0.430511096755578,0.902585284375005));
#9620=DIRECTION('',(-2.54736739925667E-17,-0.991444861362566,-0.130526192305464));
#9621=DIRECTION('',(0.,0.130526192305464,-0.991444861362566));
#9622=DIRECTION('',(1.,0.,0.));
#9623=DIRECTION('',(0.,0.,-1.));
#9624=DIRECTION('',(1.,0.,0.));
#9625=DIRECTION('',(0.,0.,-1.));
#9626=DIRECTION('',(-2.99135772045791E-17,0.991444861362566,-0.130526192305464));
#9627=DIRECTION('',(0.,0.130526192305464,0.991444861362566));
#9628=DIRECTION('',(3.22859531325E-17,-0.902585284375005,-0.430511096755578));
#9629=DIRECTION('',(0.,0.430511096755578,-0.902585284375005));
#9630=DIRECTION('',(1.,0.,0.));
#9631=DIRECTION('',(0.,0.,-1.));
#9632=DIRECTION('',(1.,0.,0.));
#9633=DIRECTION('',(0.,0.,-1.));
#9634=DIRECTION('',(-6.60825936598169E-17,0.983254907545503,0.182235525591703));
#9635=DIRECTION('',(0.,-0.182235525591703,0.983254907545503));
#9636=DIRECTION('',(2.18592128542802E-17,-0.725374371047035,-0.688354575657138));
#9637=DIRECTION('',(0.,0.688354575657138,-0.725374371047035));
#9638=DIRECTION('',(1.,0.,0.));
#9639=DIRECTION('',(0.,0.,-1.));
#9640=DIRECTION('',(1.,0.,0.));
#9641=DIRECTION('',(0.,0.,-1.));
#9642=DIRECTION('',(8.04110715575716E-17,0.878817112597322,0.477158760378666));
#9643=DIRECTION('',(0.,-0.477158760378666,0.878817112597322));
#9644=DIRECTION('',(7.14896713846317E-17,-0.477158760378665,-0.878817112597323));
#9645=DIRECTION('',(0.,0.878817112597323,-0.477158760378665));
#9646=DIRECTION('',(1.,0.,0.));
#9647=DIRECTION('',(0.,0.,-1.));
#9648=DIRECTION('',(1.,0.,0.));
#9649=DIRECTION('',(0.,0.,-1.));
#9650=DIRECTION('',(1.8186512468286E-16,0.688354575657138,0.725374371047035));
#9651=DIRECTION('',(0.,-0.725374371047035,0.688354575657138));
#9652=DIRECTION('',(-4.64133914967143E-17,-0.182235525591703,-0.983254907545503));
#9653=DIRECTION('',(0.,0.983254907545503,-0.182235525591703));
#9654=DIRECTION('',(1.,0.,0.));
#9655=DIRECTION('',(0.,0.,-1.));
#9656=DIRECTION('',(1.,0.,0.));
#9657=DIRECTION('',(0.,0.,-1.));
#9658=DIRECTION('',(6.48328605787293E-17,0.430511096755578,0.902585284375005));
#9659=DIRECTION('',(0.,-0.902585284375005,0.430511096755578));
#9660=DIRECTION('',(-2.54736739925667E-17,0.130526192305464,-0.991444861362566));
#9661=DIRECTION('',(0.,0.991444861362566,0.130526192305464));
#9662=DIRECTION('',(1.,0.,0.));
#9663=DIRECTION('',(0.,0.,-1.));
#9664=DIRECTION('',(1.,0.,0.));
#9665=DIRECTION('',(0.,0.,-1.));
#9666=DIRECTION('',(-2.99135772045791E-17,0.130526192305464,0.991444861362566));
#9667=DIRECTION('',(0.,-0.991444861362566,0.130526192305464));
#9668=DIRECTION('',(3.22859531325E-17,0.430511096755578,-0.902585284375005));
#9669=DIRECTION('',(0.,0.902585284375005,0.430511096755578));
#9670=DIRECTION('',(1.,0.,0.));
#9671=DIRECTION('',(0.,0.,-1.));
#9672=DIRECTION('',(1.,0.,0.));
#9673=DIRECTION('',(0.,0.,-1.));
#9674=DIRECTION('',(-6.60825936598169E-17,-0.182235525591703,0.983254907545503));
#9675=DIRECTION('',(0.,-0.983254907545503,-0.182235525591703));
#9676=DIRECTION('',(2.18592128542802E-17,0.688354575657138,-0.725374371047035));
#9677=DIRECTION('',(0.,0.725374371047035,0.688354575657138));
#9678=DIRECTION('',(1.,0.,0.));
#9679=DIRECTION('',(0.,0.,-1.));
#9680=DIRECTION('',(1.,0.,0.));
#9681=DIRECTION('',(0.,0.,-1.));
#9682=DIRECTION('',(8.04110715575716E-17,-0.477158760378666,0.878817112597322));
#9683=DIRECTION('',(0.,-0.878817112597322,-0.477158760378666));
#9684=DIRECTION('',(7.14896713846317E-17,0.878817112597323,-0.477158760378665));
#9685=DIRECTION('',(0.,0.477158760378665,0.878817112597323));
#9686=DIRECTION('',(1.,0.,0.));
#9687=DIRECTION('',(0.,0.,-1.));
#9688=DIRECTION('',(1.,0.,0.));
#9689=DIRECTION('',(0.,0.,-1.));
#9690=DIRECTION('',(1.8186512468286E-16,-0.725374371047035,0.688354575657138));
#9691=DIRECTION('',(0.,-0.688354575657138,-0.725374371047035));
#9692=DIRECTION('',(-4.64133914967143E-17,0.983254907545503,-0.182235525591703));
#9693=DIRECTION('',(0.,0.182235525591703,0.983254907545503));
#9694=DIRECTION('',(1.,0.,0.));
#9695=DIRECTION('',(0.,0.,-1.));
#9696=DIRECTION('',(1.,0.,0.));
#9697=DIRECTION('',(0.,0.,-1.));
#9698=DIRECTION('',(6.48328605787293E-17,-0.902585284375005,0.430511096755578));
#9699=DIRECTION('',(0.,-0.430511096755578,-0.902585284375005));
#9700=DIRECTION('',(-2.54736739925667E-17,0.991444861362566,0.130526192305464));
#9701=DIRECTION('',(0.,-0.130526192305464,0.991444861362566));
#9702=DIRECTION('',(1.,0.,0.));
#9703=DIRECTION('',(0.,0.,-1.));
#9704=DIRECTION('',(1.,0.,0.));
#9705=DIRECTION('',(0.,0.,-1.));
#9706=DIRECTION('',(-2.99135772045791E-17,-0.991444861362566,0.130526192305464));
#9707=DIRECTION('',(0.,-0.130526192305464,-0.991444861362566));
#9708=DIRECTION('',(3.22859531325E-17,0.902585284375005,0.430511096755578));
#9709=DIRECTION('',(0.,-0.430511096755578,0.902585284375005));
#9710=DIRECTION('',(1.,0.,0.));
#9711=DIRECTION('',(0.,0.,-1.));
#9712=DIRECTION('',(1.,0.,0.));
#9713=DIRECTION('',(0.,0.,-1.));
#9714=DIRECTION('',(-6.60825936598169E-17,-0.983254907545503,-0.182235525591703));
#9715=DIRECTION('',(0.,0.182235525591703,-0.983254907545503));
#9716=DIRECTION('',(2.18592128542802E-17,0.725374371047035,0.688354575657138));
#9717=DIRECTION('',(0.,-0.688354575657138,0.725374371047035));
#9718=DIRECTION('',(1.,0.,0.));
#9719=DIRECTION('',(0.,0.,-1.));
#9720=DIRECTION('',(1.,0.,0.));
#9721=DIRECTION('',(0.,0.,-1.));
#9722=DIRECTION('',(8.04110715575716E-17,-0.878817112597322,-0.477158760378666));
#9723=DIRECTION('',(0.,0.477158760378666,-0.878817112597322));
#9724=DIRECTION('',(7.14896713846317E-17,0.477158760378665,0.878817112597323));
#9725=DIRECTION('',(0.,-0.878817112597323,0.477158760378665));
#9726=DIRECTION('',(1.,0.,0.));
#9727=DIRECTION('',(0.,0.,-1.));
#9728=DIRECTION('',(1.,0.,0.));
#9729=DIRECTION('',(0.,0.,-1.));
#9730=DIRECTION('',(1.8186512468286E-16,-0.688354575657138,-0.725374371047035));
#9731=DIRECTION('',(0.,0.725374371047035,-0.688354575657138));
#9732=DIRECTION('',(-4.64133914967143E-17,0.182235525591703,0.983254907545503));
#9733=DIRECTION('',(0.,-0.983254907545503,0.182235525591703));
#9734=DIRECTION('',(1.,0.,0.));
#9735=DIRECTION('',(0.,0.,-1.));
#9736=DIRECTION('',(1.,0.,0.));
#9737=DIRECTION('',(0.,0.,-1.));
#9738=DIRECTION('',(6.48328605787293E-17,-0.430511096755578,-0.902585284375005));
#9739=DIRECTION('',(0.,0.902585284375005,-0.430511096755578));
#9740=DIRECTION('',(-2.54736739925667E-17,-0.130526192305464,0.991444861362566));
#9741=DIRECTION('',(0.,-0.991444861362566,-0.130526192305464));
#9742=DIRECTION('',(-1.,0.,0.));
#9743=DIRECTION('',(0.,0.,1.));
#9744=DIRECTION('',(-1.,0.,0.));
#9745=DIRECTION('',(0.,0.,1.));
#9746=DIRECTION('',(1.,-1.23512438660743E-15,-2.69129956548782E-15));
#9747=DIRECTION('',(-2.69129956548782E-15,0.,-1.));
#9748=DIRECTION('',(1.,-1.18123916154446E-15,-1.96770129996799E-15));
#9749=DIRECTION('',(-1.96770129996799E-15,0.,-1.));
#9750=DIRECTION('',(1.,-1.32688644717816E-16,-1.05641119487183E-16));
#9751=DIRECTION('',(1.32688644717816E-16,1.,0.));
#9752=DIRECTION('',(-1.,0.,0.));
#9753=DIRECTION('',(0.,0.,1.));
#9754=DIRECTION('',(1.,-1.23512438660689E-15,-2.69129956548782E-15));
#9755=DIRECTION('',(-2.69129956548782E-15,0.,-1.));
#9756=DIRECTION('',(1.,-1.18123916154475E-15,-1.96770129996799E-15));
#9757=DIRECTION('',(-1.96770129996799E-15,0.,-1.));
#9758=DIRECTION('',(1.,-1.24771907443915E-15,-1.41644362460478E-15));
#9759=DIRECTION('',(-1.41644362460478E-15,0.,-1.));
#9760=DIRECTION('',(1.,-1.4751360399877E-15,-1.19807507943364E-15));
#9761=DIRECTION('',(1.4751360399877E-15,1.,0.));
#9762=DIRECTION('',(1.,-2.04923588422118E-15,-1.13424025591296E-15));
#9763=DIRECTION('',(2.04923588422118E-15,1.,0.));
#9764=DIRECTION('',(1.,0.,0.));
#9765=DIRECTION('',(0.,0.,-1.));
#9766=DIRECTION('',(1.,-2.04923588422095E-15,-1.13424025591296E-15));
#9767=DIRECTION('',(2.04923588422095E-15,1.,0.));
#9768=DIRECTION('',(1.,-1.47513603998919E-15,-1.19807507943364E-15));
#9769=DIRECTION('',(1.47513603998919E-15,1.,0.));
#9770=DIRECTION('',(1.,-1.2477190744389E-15,-1.41644362460479E-15));
#9771=DIRECTION('',(-1.41644362460479E-15,0.,-1.));
#9772=DIRECTION('',(1.,-1.18123916154446E-15,-1.96770129996863E-15));
#9773=DIRECTION('',(-1.96770129996863E-15,0.,-1.));
#9774=DIRECTION('',(1.,-1.2477190744389E-15,-1.41644362460326E-15));
#9775=DIRECTION('',(-1.41644362460326E-15,0.,-1.));
#9776=DIRECTION('',(1.,-1.47513603998919E-15,-1.19807507943552E-15));
#9777=DIRECTION('',(1.47513603998919E-15,1.,0.));
#9778=DIRECTION('',(1.,-2.04923588422095E-15,-1.13424025591304E-15));
#9779=DIRECTION('',(2.04923588422095E-15,1.,0.));
#9780=DIRECTION('',(1.,0.,0.));
#9781=DIRECTION('',(0.,0.,-1.));
#9782=DIRECTION('',(1.,-2.04923588422118E-15,-1.13424025591304E-15));
#9783=DIRECTION('',(2.04923588422118E-15,1.,0.));
#9784=DIRECTION('',(1.,-1.4751360399877E-15,-1.19807507943551E-15));
#9785=DIRECTION('',(1.4751360399877E-15,1.,0.));
#9786=DIRECTION('',(1.,-1.24771907443915E-15,-1.41644362460326E-15));
#9787=DIRECTION('',(-1.41644362460326E-15,0.,-1.));
#9788=DIRECTION('',(1.,-1.18123916154475E-15,-1.96770129996863E-15));
#9789=DIRECTION('',(-1.96770129996863E-15,0.,-1.));
#9790=DIRECTION('',(-1.,-1.5350532643982E-16,1.45008721655328E-16));
#9791=DIRECTION('',(1.5350532643982E-16,-1.,0.));
#9792=DIRECTION('',(-1.,0.,0.));
#9793=DIRECTION('',(0.,0.,1.));
#9794=DIRECTION('',(-1.,0.,0.));
#9795=DIRECTION('',(0.,0.,1.));
#11098=CARTESIAN_POINT('',(0.,0.,0.));
#11099=CARTESIAN_POINT('',(-0.0285,0.,0.));
#11100=CARTESIAN_POINT('',(0.0175,0.,0.));
#11101=CARTESIAN_POINT('',(0.0175,0.,-0.0115));
#11102=CARTESIAN_POINT('',(-0.0285,0.,0.));
#11103=CARTESIAN_POINT('',(-0.0285,0.,-0.0115));
#11104=CARTESIAN_POINT('',(0.0175,1.39645239816133E-18,-5.20417042793042E-19));
#11105=CARTESIAN_POINT('',(0.0175,0.,0.));
#11106=CARTESIAN_POINT('',(0.0175,0.,0.0125));
#11107=CARTESIAN_POINT('',(-0.0285,-1.35308431126191E-18,-3.98986399474666E-19));
#11108=CARTESIAN_POINT('',(-0.0285,0.,0.));
#11109=CARTESIAN_POINT('',(-0.0285,0.,0.016));
#11110=CARTESIAN_POINT('',(-0.034017463007,0.,0.));
#11111=CARTESIAN_POINT('',(0.016499999985,0.,0.));
#11112=CARTESIAN_POINT('',(0.0164999999925,-0.0124599357945358,0.00099999999823281));
#11113=CARTESIAN_POINT('',(0.0164999998675,-0.012459935929733,-0.00100000000090912));
#11114=CARTESIAN_POINT('',(-0.01749999975,-0.0124599357942312,-0.00100000000181829));
#11115=CARTESIAN_POINT('',(-0.00616666658833333,-0.0124599357942312,-0.00100000000181829));
#11116=CARTESIAN_POINT('',(0.00516666657333334,-0.0124599357942312,-0.00100000000181829));
#11117=CARTESIAN_POINT('',(0.016499999735,-0.0124599357942312,-0.00100000000181829));
#11118=CARTESIAN_POINT('',(-0.0175,-0.0124599357941791,-0.00100000000246662));
#11119=CARTESIAN_POINT('',(-0.0175,0.,0.));
#11120=CARTESIAN_POINT('',(-0.0174999998750001,-0.0121591202350319,-0.0028992754281216));
#11121=CARTESIAN_POINT('',(0.016499999735,-0.0121591201246591,-0.00289927539121607));
#11122=CARTESIAN_POINT('',(0.00516666657333334,-0.0121591201246591,-0.00289927539121607));
#11123=CARTESIAN_POINT('',(-0.00616666658833333,-0.0121591201246591,-0.00289927539121607));
#11124=CARTESIAN_POINT('',(-0.01749999975,-0.0121591201246591,-0.00289927539121607));
#11125=CARTESIAN_POINT('',(0.0164999999925,-0.012159120124003,-0.00289927539363961));
#11126=CARTESIAN_POINT('',(0.016499999985,0.,0.));
#11127=CARTESIAN_POINT('',(0.0164999998675,-0.0115410862648032,-0.00480138846587923));
#11128=CARTESIAN_POINT('',(-0.01749999975,-0.0115410861365096,-0.00480138842311952));
#11129=CARTESIAN_POINT('',(-0.00616666658833333,-0.0115410861365096,-0.00480138842311952));
#11130=CARTESIAN_POINT('',(0.00516666657333334,-0.0115410861365096,-0.00480138842311952));
#11131=CARTESIAN_POINT('',(0.016499999735,-0.0115410861365096,-0.00480138842311952));
#11132=CARTESIAN_POINT('',(-0.0175,-0.0115410861354141,-0.00480138842608671));
#11133=CARTESIAN_POINT('',(-0.0175,0.,0.));
#11134=CARTESIAN_POINT('',(-0.0174999998750001,-0.0106680851512765,-0.00651474958006525));
#11135=CARTESIAN_POINT('',(0.016499999735,-0.0106680850555376,-0.00651474951535476));
#11136=CARTESIAN_POINT('',(0.00516666657333334,-0.0106680850555376,-0.00651474951535476));
#11137=CARTESIAN_POINT('',(-0.00616666658833333,-0.0106680850555376,-0.00651474951535476));
#11138=CARTESIAN_POINT('',(-0.01749999975,-0.0106680850555376,-0.00651474951535476));
#11139=CARTESIAN_POINT('',(0.0164999999925,-0.0106680850565945,-0.00651474951411268));
#11140=CARTESIAN_POINT('',(0.016499999985,0.,0.));
#11141=CARTESIAN_POINT('',(0.0164999998675,-0.00949251466237302,-0.00813278358045513));
#11142=CARTESIAN_POINT('',(-0.01749999975,-0.00949251455069876,-0.0081327835028834));
#11143=CARTESIAN_POINT('',(-0.00616666658833333,-0.00949251455069876,-0.0081327835028834));
#11144=CARTESIAN_POINT('',(0.00516666657333334,-0.00949251455069876,-0.0081327835028834));
#11145=CARTESIAN_POINT('',(0.016499999735,-0.00949251455069876,-0.0081327835028834));
#11146=CARTESIAN_POINT('',(-0.0175,-0.00949251455134075,-0.00813278350213407));
#11147=CARTESIAN_POINT('',(-0.0175,0.,0.));
#11148=CARTESIAN_POINT('',(-0.0174999998750001,-0.00813278356681029,-0.00949251464775881));
#11149=CARTESIAN_POINT('',(0.016499999735,-0.00813278349752703,-0.00949251455528787));
#11150=CARTESIAN_POINT('',(0.00516666657333334,-0.00813278349752703,-0.00949251455528787));
#11151=CARTESIAN_POINT('',(-0.00616666658833333,-0.00813278349752703,-0.00949251455528787));
#11152=CARTESIAN_POINT('',(-0.01749999975,-0.00813278349752703,-0.00949251455528787));
#11153=CARTESIAN_POINT('',(0.0164999999925,-0.0081327834971287,-0.00949251455573178));
#11154=CARTESIAN_POINT('',(0.016499999985,0.,0.));
#11155=CARTESIAN_POINT('',(0.0164999998675,-0.00651474958930339,-0.0106680851684153));
#11156=CARTESIAN_POINT('',(-0.01749999975,-0.00651474950933505,-0.0106680850592137));
#11157=CARTESIAN_POINT('',(-0.00616666658833333,-0.00651474950933505,-0.0106680850592137));
#11158=CARTESIAN_POINT('',(0.00516666657333334,-0.00651474950933505,-0.0106680850592137));
#11159=CARTESIAN_POINT('',(0.016499999735,-0.00651474950933505,-0.0106680850592137));
#11160=CARTESIAN_POINT('',(-0.0175,-0.006514749508334,-0.0106680850599212));
#11161=CARTESIAN_POINT('',(-0.0175,0.,0.));
#11162=CARTESIAN_POINT('',(-0.0174999998750001,-0.00480138846316548,-0.0115410862459344));
#11163=CARTESIAN_POINT('',(0.016499999735,-0.00480138842814829,-0.0115410861344175));
#11164=CARTESIAN_POINT('',(0.00516666657333334,-0.00480138842814829,-0.0115410861344175));
#11165=CARTESIAN_POINT('',(-0.00616666658833333,-0.00480138842814829,-0.0115410861344175));
#11166=CARTESIAN_POINT('',(-0.01749999975,-0.00480138842814829,-0.0115410861344175));
#11167=CARTESIAN_POINT('',(0.0164999999925,-0.00480138842564847,-0.0115410861353612));
#11168=CARTESIAN_POINT('',(0.016499999985,0.,0.));
#11169=CARTESIAN_POINT('',(0.0164999998675,-0.00289927543680423,-0.0121591202526653));
#11170=CARTESIAN_POINT('',(-0.01749999975,-0.00289927539651413,-0.0121591201233958));
#11171=CARTESIAN_POINT('',(-0.00616666658833333,-0.00289927539651413,-0.0121591201233958));
#11172=CARTESIAN_POINT('',(0.00516666657333334,-0.00289927539651413,-0.0121591201233958));
#11173=CARTESIAN_POINT('',(0.016499999735,-0.00289927539651413,-0.0121591201233958));
#11174=CARTESIAN_POINT('',(-0.0175,-0.00289927539331615,-0.0121591201243034));
#11175=CARTESIAN_POINT('',(-0.0175,0.,0.));
#11176=CARTESIAN_POINT('',(-0.0174999998750001,-0.000999999997433504,-0.0124599359095369));
#11177=CARTESIAN_POINT('',(0.016499999735,-0.000999999994787424,-0.0124599357947955));
#11178=CARTESIAN_POINT('',(0.00516666657333334,-0.000999999994787424,-0.0124599357947955));
#11179=CARTESIAN_POINT('',(-0.00616666658833333,-0.000999999994787424,-0.0124599357947955));
#11180=CARTESIAN_POINT('',(-0.01749999975,-0.000999999994787424,-0.0124599357947955));
#11181=CARTESIAN_POINT('',(0.0164999999925,-0.000999999995836203,-0.0124599357949205));
#11182=CARTESIAN_POINT('',(0.016499999985,0.,0.));
#11183=CARTESIAN_POINT('',(0.0164999998675,0.00100000000218691,-0.0124599359296304));
#11184=CARTESIAN_POINT('',(-0.01749999975,0.0010000000043738,-0.0124599357940261));
#11185=CARTESIAN_POINT('',(-0.00616666658833333,0.0010000000043738,-0.0124599357940261));
#11186=CARTESIAN_POINT('',(0.00516666657333334,0.0010000000043738,-0.0124599357940261));
#11187=CARTESIAN_POINT('',(0.016499999735,0.0010000000043738,-0.0124599357940261));
#11188=CARTESIAN_POINT('',(-0.0175,0.0010000000037444,-0.0124599357940766));
#11189=CARTESIAN_POINT('',(-0.0175,0.,0.));
#11190=CARTESIAN_POINT('',(-0.0174999998750001,0.00289927542936853,-0.0121591202347346));
#11191=CARTESIAN_POINT('',(0.016499999735,0.00289927539370995,-0.0121591201240644));
#11192=CARTESIAN_POINT('',(0.00516666657333334,0.00289927539370995,-0.0121591201240644));
#11193=CARTESIAN_POINT('',(-0.00616666658833333,0.00289927539370995,-0.0121591201240644));
#11194=CARTESIAN_POINT('',(-0.01749999975,0.00289927539370995,-0.0121591201240644));
#11195=CARTESIAN_POINT('',(0.0164999999925,0.00289927539491823,-0.0121591201238032));
#11196=CARTESIAN_POINT('',(0.016499999985,0.,0.));
#11197=CARTESIAN_POINT('',(0.0164999998674999,0.00480138846706279,-0.0115410862643108));
#11198=CARTESIAN_POINT('',(-0.01749999975,0.00480138842548664,-0.0115410861355248));
#11199=CARTESIAN_POINT('',(-0.00616666658833333,0.00480138842548664,-0.0115410861355248));
#11200=CARTESIAN_POINT('',(0.00516666657333334,0.00480138842548664,-0.0115410861355248));
#11201=CARTESIAN_POINT('',(0.016499999735,0.00480138842548664,-0.0115410861355248));
#11202=CARTESIAN_POINT('',(-0.0175,0.00480138842723857,-0.0115410861348241));
#11203=CARTESIAN_POINT('',(-0.0175,0.,0.));
#11204=CARTESIAN_POINT('',(-0.0174999998750001,0.00651474957582523,-0.0106680851538658));
#11205=CARTESIAN_POINT('',(0.016499999735,0.00651474950687474,-0.0106680850607162));
#11206=CARTESIAN_POINT('',(0.00516666657333334,0.00651474950687474,-0.0106680850607162));
#11207=CARTESIAN_POINT('',(-0.00616666658833333,0.00651474950687474,-0.0106680850607162));
#11208=CARTESIAN_POINT('',(-0.01749999975,0.00651474950687474,-0.0106680850607162));
#11209=CARTESIAN_POINT('',(0.0164999999925,0.00651474950977088,-0.0106680850590437));
#11210=CARTESIAN_POINT('',(0.016499999985,0.,0.));
#11211=CARTESIAN_POINT('',(0.0164999998674999,0.00813278357668235,-0.00949251466560538));
#11212=CARTESIAN_POINT('',(-0.01749999975,0.00813278349533783,-0.00949251455716348));
#11213=CARTESIAN_POINT('',(-0.00616666658833333,0.00813278349533783,-0.00949251455716348));
#11214=CARTESIAN_POINT('',(0.00516666657333334,0.00813278349533783,-0.00949251455716348));
#11215=CARTESIAN_POINT('',(0.016499999735,0.00813278349533783,-0.00949251455716348));
#11216=CARTESIAN_POINT('',(-0.0175,0.00813278349847502,-0.00949251455472967));
#11217=CARTESIAN_POINT('',(-0.0175,0.,0.));
#11218=CARTESIAN_POINT('',(-0.0174999998750001,0.00949251464859284,-0.00813278356583681));
#11219=CARTESIAN_POINT('',(0.016499999735,0.00949251455695593,-0.00813278349558008));
#11220=CARTESIAN_POINT('',(0.00516666657333334,0.00949251455695593,-0.00813278349558008));
#11221=CARTESIAN_POINT('',(-0.00616666658833333,0.00949251455695593,-0.00813278349558008));
#11222=CARTESIAN_POINT('',(-0.01749999975,0.00949251455695593,-0.00813278349558008));
#11223=CARTESIAN_POINT('',(0.0164999999925,0.00949251455664878,-0.0081327834962155));
#11224=CARTESIAN_POINT('',(0.016499999985,0.,0.));
#11225=CARTESIAN_POINT('',(0.0164999998675,0.0106680851690834,-0.00651474958820936));
#11226=CARTESIAN_POINT('',(-0.01749999975,0.0106680850605499,-0.00651474950714699));
#11227=CARTESIAN_POINT('',(-0.00616666658833333,0.0106680850605499,-0.00651474950714699));
#11228=CARTESIAN_POINT('',(0.00516666657333334,0.0106680850605499,-0.00651474950714699));
#11229=CARTESIAN_POINT('',(0.016499999735,0.0106680850605499,-0.00651474950714699));
#11230=CARTESIAN_POINT('',(-0.0175,0.0106680850605893,-0.00651474950723997));
#11231=CARTESIAN_POINT('',(-0.0175,0.,0.));
#11232=CARTESIAN_POINT('',(-0.0174999998750001,0.0115410862464268,-0.00480138846198192));
#11233=CARTESIAN_POINT('',(0.016499999735,0.0115410861354023,-0.00480138842578117));
#11234=CARTESIAN_POINT('',(0.00516666657333334,0.0115410861354023,-0.00480138842578117));
#11235=CARTESIAN_POINT('',(-0.00616666658833333,0.0115410861354023,-0.00480138842578117));
#11236=CARTESIAN_POINT('',(-0.01749999975,0.0115410861354023,-0.00480138842578117));
#11237=CARTESIAN_POINT('',(0.0164999999925,0.0115410861359511,-0.0048013884244966));
#11238=CARTESIAN_POINT('',(0.016499999985,0.,0.));
#11239=CARTESIAN_POINT('',(0.0164999998675,0.0121591202529626,-0.0028992754355573));
#11240=CARTESIAN_POINT('',(-0.01749999975,0.0121591201239904,-0.00289927539402025));
#11241=CARTESIAN_POINT('',(-0.00616666658833333,0.0121591201239904,-0.00289927539402025));
#11242=CARTESIAN_POINT('',(0.00516666657333334,0.0121591201239904,-0.00289927539402025));
#11243=CARTESIAN_POINT('',(0.016499999735,0.0121591201239904,-0.00289927539402025));
#11244=CARTESIAN_POINT('',(-0.0175,0.0121591201245032,-0.00289927539203753));
#11245=CARTESIAN_POINT('',(-0.0175,0.,0.));
#11246=CARTESIAN_POINT('',(-0.0174999998750001,0.0124599359091394,-0.00100000000238569));
#11247=CARTESIAN_POINT('',(0.016499999735,0.0124599357940006,-0.00100000000469178));
#11248=CARTESIAN_POINT('',(0.00516666657333334,0.0124599357940006,-0.00100000000469178));
#11249=CARTESIAN_POINT('',(-0.00616666658833333,0.0124599357940006,-0.00100000000469178));
#11250=CARTESIAN_POINT('',(-0.01749999975,0.0124599357940006,-0.00100000000469178));
#11251=CARTESIAN_POINT('',(0.0164999999925,0.0124599359297427,-0.00100000000078839));
#11252=CARTESIAN_POINT('',(0.016499999985,0.,0.));
#11253=CARTESIAN_POINT('',(0.0164999998675,0.0124599359300279,0.000999999997234729));
#11254=CARTESIAN_POINT('',(-0.01749999975,0.012459935794821,0.000999999994469453));
#11255=CARTESIAN_POINT('',(-0.00616666658833333,0.012459935794821,0.000999999994469453));
#11256=CARTESIAN_POINT('',(0.00516666657333334,0.012459935794821,0.000999999994469453));
#11257=CARTESIAN_POINT('',(0.016499999735,0.012459935794821,0.000999999994469453));
#11258=CARTESIAN_POINT('',(-0.0175,0.012459935794696,0.000999999998792222));
#11259=CARTESIAN_POINT('',(-0.0175,0.,0.));
#11260=CARTESIAN_POINT('',(-0.0174999998750001,0.0121591202344372,0.00289927543061547));
#11261=CARTESIAN_POINT('',(0.016499999735,0.0121591201234698,0.00289927539620384));
#11262=CARTESIAN_POINT('',(0.00516666657333334,0.0121591201234698,0.00289927539620384));
#11263=CARTESIAN_POINT('',(-0.00616666658833333,0.0121591201234698,0.00289927539620384));
#11264=CARTESIAN_POINT('',(-0.01749999975,0.0121591201234698,0.00289927539620384));
#11265=CARTESIAN_POINT('',(0.0164999999925,0.0121591201236034,0.00289927539619686));
#11266=CARTESIAN_POINT('',(0.016499999985,0.,0.));
#11267=CARTESIAN_POINT('',(0.0164999998675,0.0115410862638184,0.00480138846824635));
#11268=CARTESIAN_POINT('',(-0.01749999975,0.01154108613454,0.00480138842785377));
#11269=CARTESIAN_POINT('',(-0.00616666658833333,0.01154108613454,0.00480138842785377));
#11270=CARTESIAN_POINT('',(0.00516666657333334,0.01154108613454,0.00480138842785377));
#11271=CARTESIAN_POINT('',(0.016499999735,0.01154108613454,0.00480138842785377));
#11272=CARTESIAN_POINT('',(-0.0175,0.0115410861343069,0.00480138842841406));
#11273=CARTESIAN_POINT('',(-0.0175,0.,0.));
#11274=CARTESIAN_POINT('',(-0.0174999998750001,0.0106680851531977,0.00651474957691926));
#11275=CARTESIAN_POINT('',(0.016499999735,0.0106680850593799,0.00651474950906283));
#11276=CARTESIAN_POINT('',(0.00516666657333334,0.0106680850593799,0.00651474950906283));
#11277=CARTESIAN_POINT('',(-0.00616666658833333,0.0106680850593799,0.00651474950906283));
#11278=CARTESIAN_POINT('',(-0.01749999975,0.0106680850593799,0.00651474950906283));
#11279=CARTESIAN_POINT('',(0.0164999999925,0.0106680850583756,0.00651474951086491));
#11280=CARTESIAN_POINT('',(0.016499999985,0.,0.));
#11281=CARTESIAN_POINT('',(0.0164999998675,0.00949251466477135,0.00813278357765582));
#11282=CARTESIAN_POINT('',(-0.01749999975,0.0094925145554954,0.0081327834972848));
#11283=CARTESIAN_POINT('',(-0.00616666658833333,0.0094925145554954,0.0081327834972848));
#11284=CARTESIAN_POINT('',(0.00516666657333334,0.0094925145554954,0.0081327834972848));
#11285=CARTESIAN_POINT('',(0.016499999735,0.0094925145554954,0.0081327834972848));
#11286=CARTESIAN_POINT('',(-0.0175,0.00949251455381267,0.00813278349938822));
#11287=CARTESIAN_POINT('',(-0.0175,0.,0.));
#11288=CARTESIAN_POINT('',(-0.0174999998750001,0.0081327835696096,0.00949251464536048));
#11289=CARTESIAN_POINT('',(0.016499999735,0.00813278350312564,0.00949251455049122));
#11290=CARTESIAN_POINT('',(0.00516666657333334,0.00813278350312564,0.00949251455049122));
#11291=CARTESIAN_POINT('',(-0.00616666658833333,0.00813278350312564,0.00949251455049122));
#11292=CARTESIAN_POINT('',(-0.01749999975,0.00813278350312564,0.00949251455049122));
#11293=CARTESIAN_POINT('',(0.0164999999925,0.00813278349987625,0.00949251455326221));
#11294=CARTESIAN_POINT('',(0.016499999985,0.,0.));
#11295=CARTESIAN_POINT('',(0.0164999998675,0.00651474958711533,0.0106680851697515));
#11296=CARTESIAN_POINT('',(-0.01749999975,0.00651474950495892,0.0106680850618861));
#11297=CARTESIAN_POINT('',(-0.00616666658833333,0.00651474950495892,0.0106680850618861));
#11298=CARTESIAN_POINT('',(0.00516666657333334,0.00651474950495892,0.0106680850618861));
#11299=CARTESIAN_POINT('',(0.016499999735,0.00651474950495892,0.0106680850618861));
#11300=CARTESIAN_POINT('',(-0.0175,0.00651474950614593,0.0106680850612574));
#11301=CARTESIAN_POINT('',(-0.0175,0.,0.));
#11302=CARTESIAN_POINT('',(-0.0174999998750001,0.00480138846079837,0.0115410862469192));
#11303=CARTESIAN_POINT('',(0.016499999735,0.00480138842341404,0.0115410861363871));
#11304=CARTESIAN_POINT('',(0.00516666657333334,0.00480138842341404,0.0115410861363871));
#11305=CARTESIAN_POINT('',(-0.00616666658833333,0.00480138842341404,0.0115410861363871));
#11306=CARTESIAN_POINT('',(-0.01749999975,0.00480138842341404,0.0115410861363871));
#11307=CARTESIAN_POINT('',(0.0164999999925,0.00480138842334474,0.011541086136541));
#11308=CARTESIAN_POINT('',(0.016499999985,0.,0.));
#11309=CARTESIAN_POINT('',(0.0164999998675,0.00289927543431036,0.01215912025326));
#11310=CARTESIAN_POINT('',(-0.01749999975,0.00289927539152635,0.0121591201245851));
#11311=CARTESIAN_POINT('',(-0.00616666658833333,0.00289927539152635,0.0121591201245851));
#11312=CARTESIAN_POINT('',(0.00516666657333334,0.00289927539152635,0.0121591201245851));
#11313=CARTESIAN_POINT('',(0.016499999735,0.00289927539152635,0.0121591201245851));
#11314=CARTESIAN_POINT('',(-0.0175,0.00289927539077852,0.0121591201247634));
#11315=CARTESIAN_POINT('',(-0.0175,0.,0.));
#11316=CARTESIAN_POINT('',(-0.0174999998750001,0.0010000000011079,0.012459935909242));
#11317=CARTESIAN_POINT('',(0.016499999735,0.00100000000213619,0.0124599357942057));
#11318=CARTESIAN_POINT('',(0.00516666657333334,0.00100000000213619,0.0124599357942057));
#11319=CARTESIAN_POINT('',(-0.00616666658833333,0.00100000000213619,0.0124599357942057));
#11320=CARTESIAN_POINT('',(-0.01749999975,0.00100000000213619,0.0124599357942057));
#11321=CARTESIAN_POINT('',(0.0164999999925,0.00099999999873186,0.0124599357942903));
#11322=CARTESIAN_POINT('',(0.016499999985,0.,0.));
#11323=CARTESIAN_POINT('',(0.016499999805,-0.000999999998512521,0.0124599359299253));
#11324=CARTESIAN_POINT('',(-0.01749999975,-0.000999999997025032,0.0124599357946159));
#11325=CARTESIAN_POINT('',(-0.00616666658833333,-0.000999999997025032,0.0124599357946159));
#11326=CARTESIAN_POINT('',(0.00516666657333334,-0.000999999997025032,0.0124599357946159));
#11327=CARTESIAN_POINT('',(0.016499999735,-0.000999999997025032,0.0124599357946159));
#11328=CARTESIAN_POINT('',(-0.0175,-0.00100000000007001,0.0124599357944909));
#11329=CARTESIAN_POINT('',(-0.0175,0.,0.));
#11330=CARTESIAN_POINT('',(-0.0174999998750001,-0.00289927543186242,0.0121591202341399));
#11331=CARTESIAN_POINT('',(0.016499999735,-0.00289927539869773,0.0121591201228751));
#11332=CARTESIAN_POINT('',(0.00516666657333334,-0.00289927539869773,0.0121591201228751));
#11333=CARTESIAN_POINT('',(-0.00616666658833333,-0.00289927539869773,0.0121591201228751));
#11334=CARTESIAN_POINT('',(-0.01749999975,-0.00289927539869773,0.0121591201228751));
#11335=CARTESIAN_POINT('',(0.0164999999925,-0.00289927539747549,0.0121591201234037));
#11336=CARTESIAN_POINT('',(0.016499999985,0.,0.));
#11337=CARTESIAN_POINT('',(0.0164999998675,-0.00480138846942991,0.011541086263326));
#11338=CARTESIAN_POINT('',(-0.01749999975,-0.00480138843022089,0.0115410861335552));
#11339=CARTESIAN_POINT('',(-0.00616666658833333,-0.00480138843022089,0.0115410861335552));
#11340=CARTESIAN_POINT('',(0.00516666657333334,-0.00480138843022089,0.0115410861335552));
#11341=CARTESIAN_POINT('',(0.016499999735,-0.00480138843022089,0.0115410861335552));
#11342=CARTESIAN_POINT('',(-0.0175,-0.00480138842959763,0.0115410861338145));
#11343=CARTESIAN_POINT('',(-0.0175,0.,0.));
#11344=CARTESIAN_POINT('',(-0.0174999998750001,-0.00651474957801329,0.0106680851525296));
#11345=CARTESIAN_POINT('',(0.016499999735,-0.00651474951125087,0.0106680850580438));
#11346=CARTESIAN_POINT('',(0.00516666657333334,-0.00651474951125087,0.0106680850580438));
#11347=CARTESIAN_POINT('',(-0.00616666658833333,-0.00651474951125087,0.0106680850580438));
#11348=CARTESIAN_POINT('',(-0.01749999975,-0.00651474951125087,0.0106680850580438));
#11349=CARTESIAN_POINT('',(0.0164999999925,-0.00651474951195894,0.0106680850577075));
#11350=CARTESIAN_POINT('',(0.016499999985,0.,0.));
#11351=CARTESIAN_POINT('',(0.0164999998675,-0.0081327835786293,0.00949251466393732));
#11352=CARTESIAN_POINT('',(-0.01749999975,-0.00813278349923174,0.00949251455382735));
#11353=CARTESIAN_POINT('',(-0.00616666658833333,-0.00813278349923174,0.00949251455382735));
#11354=CARTESIAN_POINT('',(0.00516666657333334,-0.00813278349923174,0.00949251455382735));
#11355=CARTESIAN_POINT('',(0.016499999735,-0.00813278349923174,0.00949251455382735));
#11356=CARTESIAN_POINT('',(-0.0175,-0.00813278350030823,0.00949251455290506));
#11357=CARTESIAN_POINT('',(-0.0175,0.,0.));
#11358=CARTESIAN_POINT('',(-0.0174999998750001,-0.00949251464619451,0.00813278356863612));
#11359=CARTESIAN_POINT('',(0.016499999735,-0.00949251455215928,0.00813278350117869));
#11360=CARTESIAN_POINT('',(0.00516666657333334,-0.00949251455215928,0.00813278350117869));
#11361=CARTESIAN_POINT('',(-0.00616666658833333,-0.00949251455215928,0.00813278350117869));
#11362=CARTESIAN_POINT('',(-0.01749999975,-0.00949251455215928,0.00813278350117869));
#11363=CARTESIAN_POINT('',(0.0164999999925,-0.00949251455409624,0.00813278349890277));
#11364=CARTESIAN_POINT('',(0.016499999985,0.,0.));
#11365=CARTESIAN_POINT('',(0.0164999998675,-0.0106680851671622,0.00651474959135534));
#11366=CARTESIAN_POINT('',(-0.01749999975,-0.0106680850567076,0.00651474951343894));
#11367=CARTESIAN_POINT('',(-0.00616666658833333,-0.0106680850567076,0.00651474951343894));
#11368=CARTESIAN_POINT('',(0.00516666657333334,-0.0106680850567076,0.00651474951343894));
#11369=CARTESIAN_POINT('',(0.016499999735,-0.0106680850567076,0.00651474951343894));
#11370=CARTESIAN_POINT('',(-0.0175,-0.0106680850587356,0.00651474951043495));
#11371=CARTESIAN_POINT('',(-0.0175,0.,0.));
#11372=CARTESIAN_POINT('',(-0.0174999998750001,-0.0115410862474116,0.00480138845961481));
#11373=CARTESIAN_POINT('',(0.016499999735,-0.0115410861373718,0.00480138842104692));
#11374=CARTESIAN_POINT('',(0.00516666657333334,-0.0115410861373718,0.00480138842104692));
#11375=CARTESIAN_POINT('',(-0.00616666658833333,-0.0115410861373718,0.00480138842104692));
#11376=CARTESIAN_POINT('',(-0.01749999975,-0.0115410861373718,0.00480138842104692));
#11377=CARTESIAN_POINT('',(0.0164999999925,-0.0115410861371309,0.00480138842219287));
#11378=CARTESIAN_POINT('',(0.016499999985,0.,0.));
#11379=CARTESIAN_POINT('',(0.0164999998675,-0.0121591202535573,0.00289927543306342));
#11380=CARTESIAN_POINT('',(-0.01749999975,-0.0121591201251797,0.00289927538903248));
#11381=CARTESIAN_POINT('',(-0.00616666658833333,-0.0121591201251797,0.00289927538903248));
#11382=CARTESIAN_POINT('',(0.00516666657333334,-0.0121591201251797,0.00289927538903248));
#11383=CARTESIAN_POINT('',(0.016499999735,-0.0121591201251797,0.00289927538903248));
#11384=CARTESIAN_POINT('',(-0.0175,-0.0121591201250607,0.00289927538953159));
#11385=CARTESIAN_POINT('',(-0.0175,0.,0.));
#11386=CARTESIAN_POINT('',(-0.0174999998750001,-0.0124599359093445,0.000999999999830113));
#11387=CARTESIAN_POINT('',(0.016499999735,-0.0124599357944108,0.000999999999580603));
#11388=CARTESIAN_POINT('',(0.00516666657333334,-0.0124599357944108,0.000999999999580603));
#11389=CARTESIAN_POINT('',(-0.00616666658833333,-0.0124599357944108,0.000999999999580603));
#11390=CARTESIAN_POINT('',(-0.01749999975,-0.0124599357944108,0.000999999999580603));
#11391=CARTESIAN_POINT('',(-0.034017463007,0.,0.));
#11392=CARTESIAN_POINT('',(-0.0215,0.,0.));
#11393=CARTESIAN_POINT('',(-0.0215,0.,0.016));
#11394=CARTESIAN_POINT('',(0.0165,0.012729967897,-1.56125112837913E-19));
#11395=CARTESIAN_POINT('',(0.0165,0.0124599359297427,-0.001));
#11396=CARTESIAN_POINT('',(0.0165,0.012627117751961,-0.001));
#11397=CARTESIAN_POINT('',(0.0165,0.0127942995741793,-0.001));
#11398=CARTESIAN_POINT('',(0.0165,0.0129614813963976,-0.001));
#11399=CARTESIAN_POINT('',(0.016499999875,0.0129614813972715,-0.000999999995286969));
#11400=CARTESIAN_POINT('',(0.0165,0.,0.));
#11401=CARTESIAN_POINT('',(0.0165,0.0129614812809713,0.001));
#11402=CARTESIAN_POINT('',(0.0165,0.0129614812809713,0.001));
#11403=CARTESIAN_POINT('',(0.0165,0.0127942994973235,0.001));
#11404=CARTESIAN_POINT('',(0.0165,0.0126271177136757,0.001));
#11405=CARTESIAN_POINT('',(0.0165,0.0124599359300279,0.001));
#11406=CARTESIAN_POINT('',(-0.0005,0.0127107085955,0.001));
#11407=CARTESIAN_POINT('',(0.0165,0.012961481397,0.001));
#11408=CARTESIAN_POINT('',(0.00550000000333333,0.012961481397,0.001));
#11409=CARTESIAN_POINT('',(-0.00549999999333333,0.012961481397,0.001));
#11410=CARTESIAN_POINT('',(-0.01649999999,0.012961481397,0.001));
#11411=CARTESIAN_POINT('',(-0.016499999995,0.0129614813969079,0.001));
#11412=CARTESIAN_POINT('',(-0.01649999999,0.012961481397,0.001));
#11413=CARTESIAN_POINT('',(-0.0168333333266667,0.012961481397,0.001));
#11414=CARTESIAN_POINT('',(-0.0171666666633333,0.012961481397,0.001));
#11415=CARTESIAN_POINT('',(-0.0175,0.012961481397,0.001));
#11416=CARTESIAN_POINT('',(-0.0175,0.0129614813972181,0.00100000000002654));
#11417=CARTESIAN_POINT('',(-0.0175,0.012961481397,0.001));
#11418=CARTESIAN_POINT('',(-0.0175,0.0127942995293333,0.001));
#11419=CARTESIAN_POINT('',(-0.0175,0.0126271176616667,0.001));
#11420=CARTESIAN_POINT('',(-0.0175,0.012459935794,0.001));
#11421=CARTESIAN_POINT('',(-0.0175,0.014827238428,0.002713045933));
#11422=CARTESIAN_POINT('',(-0.0175000000005,0.,0.));
#11423=CARTESIAN_POINT('',(-0.0175,0.0167636388755286,0.00502298781439511));
#11424=CARTESIAN_POINT('',(-0.0174999998755,0.0174953567318995,0.000403103986062307));
#11425=CARTESIAN_POINT('',(-0.0175,0.0126361183371985,0.00305426150693499));
#11426=CARTESIAN_POINT('',(-0.0175,0.0140119585166962,0.00371050360930785));
#11427=CARTESIAN_POINT('',(-0.0175,0.0153877986961938,0.0043667457116807));
#11428=CARTESIAN_POINT('',(-0.0175,0.0167636388756915,0.00502298781405356));
#11429=CARTESIAN_POINT('',(-0.0175,0.0126361183374657,0.00305426150728999));
#11430=CARTESIAN_POINT('',(-0.0175,0.0121591202349204,0.00289927542912857));
#11431=CARTESIAN_POINT('',(-0.0175,0.0123181196023464,0.00295093745506404));
#11432=CARTESIAN_POINT('',(-0.0175,0.0124771189697725,0.00300259948099951));
#11433=CARTESIAN_POINT('',(-0.0175,0.0126361183371985,0.00305426150693499));
#11434=CARTESIAN_POINT('',(-0.0175,0.0174953567323097,0.000403103989178478));
#11435=CARTESIAN_POINT('',(-0.0175,0.0159840649540913,0.000602069326145522));
#11436=CARTESIAN_POINT('',(-0.0175,0.0144727731758729,0.000801034663112566));
#11437=CARTESIAN_POINT('',(-0.0175,0.0129614813976545,0.00100000000007961));
#11438=CARTESIAN_POINT('',(-0.0005,0.012397619231,0.0029767684505));
#11439=CARTESIAN_POINT('',(-0.0175,0.012636118338,0.003054261508));
#11440=CARTESIAN_POINT('',(-0.0171666666633333,0.012636118338,0.003054261508));
#11441=CARTESIAN_POINT('',(-0.0168333333266667,0.012636118338,0.003054261508));
#11442=CARTESIAN_POINT('',(-0.01649999999,0.012636118338,0.003054261508));
#11443=CARTESIAN_POINT('',(-0.016499999995,0.0126361183378015,0.00305426150790531));
#11444=CARTESIAN_POINT('',(-0.01649999999,0.012636118338,0.003054261508));
#11445=CARTESIAN_POINT('',(-0.00549999999333333,0.012636118338,0.003054261508));
#11446=CARTESIAN_POINT('',(0.00550000000333333,0.012636118338,0.003054261508));
#11447=CARTESIAN_POINT('',(0.0165,0.012636118338,0.003054261508));
#11448=CARTESIAN_POINT('',(0.0165,0.0126361181000306,0.00305426143067905));
#11449=CARTESIAN_POINT('',(0.0165,0.0126361181000306,0.00305426143067905));
#11450=CARTESIAN_POINT('',(0.0165,0.0124771187746871,0.00300259941811937));
#11451=CARTESIAN_POINT('',(0.0165,0.0123181194493435,0.00295093740555969));
#11452=CARTESIAN_POINT('',(0.0165,0.012159120124,0.002899275393));
#11453=CARTESIAN_POINT('',(0.0165,0.0120886022365,0.00392782496649999));
#11454=CARTESIAN_POINT('',(0.0165,0.,0.));
#11455=CARTESIAN_POINT('',(0.0165,0.0120180842387746,0.00495637450404248));
#11456=CARTESIAN_POINT('',(0.0165,0.0120180842388167,0.00495637450391302));
#11457=CARTESIAN_POINT('',(0.0165,0.0118590849139752,0.00490471249153795));
#11458=CARTESIAN_POINT('',(0.0165,0.0117000855891338,0.00485305047916288));
#11459=CARTESIAN_POINT('',(0.0165,0.0115410862642923,0.00480138846678781));
#11460=CARTESIAN_POINT('',(-0.0005,0.011779585242,0.004878881483));
#11461=CARTESIAN_POINT('',(0.0165,0.012018084349,0.00495637454));
#11462=CARTESIAN_POINT('',(0.00550000000333333,0.012018084349,0.00495637454));
#11463=CARTESIAN_POINT('',(-0.00549999999333332,0.012018084349,0.00495637454));
#11464=CARTESIAN_POINT('',(-0.01649999999,0.012018084349,0.00495637454));
#11465=CARTESIAN_POINT('',(-0.016499999995,0.0120180843489919,0.00495637453999739));
#11466=CARTESIAN_POINT('',(-0.01649999999,0.012018084349,0.00495637454));
#11467=CARTESIAN_POINT('',(-0.0168333333266667,0.012018084349,0.00495637454));
#11468=CARTESIAN_POINT('',(-0.0171666666633333,0.012018084349,0.00495637454));
#11469=CARTESIAN_POINT('',(-0.0175,0.012018084349,0.00495637454));
#11470=CARTESIAN_POINT('',(-0.0175,0.0120180843492958,0.00495637454010061));
#11471=CARTESIAN_POINT('',(-0.0175,0.012018084349,0.00495637454));
#11472=CARTESIAN_POINT('',(-0.0175,0.0118590849443333,0.004904712502));
#11473=CARTESIAN_POINT('',(-0.0175,0.0117000855396667,0.004853050464));
#11474=CARTESIAN_POINT('',(-0.0175,0.011541086135,0.004801388426));
#11475=CARTESIAN_POINT('',(-0.0175,0.0135912960505,0.0073793915595));
#11476=CARTESIAN_POINT('',(-0.0175,0.016514507041402,0.00578973722594494));
#11477=CARTESIAN_POINT('',(-0.0175,0.0150156994775638,0.0055119496640639));
#11478=CARTESIAN_POINT('',(-0.0175,0.0135168919137255,0.00523416210218287));
#11479=CARTESIAN_POINT('',(-0.0175,0.0120180843498873,0.00495637454030183));
#11480=CARTESIAN_POINT('',(-0.0174999997505,0.0165145070402477,0.00578973723217286));
#11481=CARTESIAN_POINT('',(-0.0175000000005,0.,0.));
#11482=CARTESIAN_POINT('',(-0.0174999998752501,0.0143909793913725,0.00995739459196203));
#11483=CARTESIAN_POINT('',(-0.0175,0.0110738439744768,0.00680955061903613));
#11484=CARTESIAN_POINT('',(-0.0175,0.0121795557799528,0.00785883194350906));
#11485=CARTESIAN_POINT('',(-0.0175,0.0132852675854288,0.00890811326798199));
#11486=CARTESIAN_POINT('',(-0.0175,0.0143909793909048,0.00995739459245492));
#11487=CARTESIAN_POINT('',(-0.0175,0.0110738439746512,0.00680955061902408));
#11488=CARTESIAN_POINT('',(-0.0175,0.0106680851533433,0.00651474957671889));
#11489=CARTESIAN_POINT('',(-0.0175,0.0108033380937212,0.00661301659082463));
#11490=CARTESIAN_POINT('',(-0.0175,0.010938591034099,0.00671128360493038));
#11491=CARTESIAN_POINT('',(-0.0175,0.0110738439744768,0.00680955061903613));
#11492=CARTESIAN_POINT('',(-0.0005,0.010870964517,0.00666215006449998));
#11493=CARTESIAN_POINT('',(-0.0175,0.011073843975,0.00680955061899999));
#11494=CARTESIAN_POINT('',(-0.0171666666633333,0.011073843975,0.00680955061899999));
#11495=CARTESIAN_POINT('',(-0.0168333333266667,0.011073843975,0.00680955061899999));
#11496=CARTESIAN_POINT('',(-0.01649999999,0.011073843975,0.00680955061899999));
#11497=CARTESIAN_POINT('',(-0.016499999995,0.0110738439747809,0.00680955061879209));
#11498=CARTESIAN_POINT('',(-0.01649999999,0.011073843975,0.00680955061899999));
#11499=CARTESIAN_POINT('',(-0.00549999999333334,0.011073843975,0.00680955061899999));
#11500=CARTESIAN_POINT('',(0.00550000000333334,0.011073843975,0.00680955061899999));
#11501=CARTESIAN_POINT('',(0.0165,0.011073843975,0.00680955061899999));
#11502=CARTESIAN_POINT('',(0.0165,0.011073843772506,0.00680955047187945));
#11503=CARTESIAN_POINT('',(0.0165,0.011073843772506,0.00680955047187945));
#11504=CARTESIAN_POINT('',(0.0165,0.010938590868004,0.0067112834845863));
#11505=CARTESIAN_POINT('',(0.0165,0.010803337963502,0.00661301649729314));
#11506=CARTESIAN_POINT('',(0.0165,0.010668085059,0.00651474950999999));
#11507=CARTESIAN_POINT('',(0.0165,0.0102831792645,0.0074711670585));
#11508=CARTESIAN_POINT('',(0.0165,0.,0.));
#11509=CARTESIAN_POINT('',(0.0165,0.00989827337663452,0.00842758453894735));
#11510=CARTESIAN_POINT('',(0.0165,0.00989827337673848,0.00842758453880426));
#11511=CARTESIAN_POINT('',(0.0165,0.00976302047259451,0.00832931755196802));
#11512=CARTESIAN_POINT('',(0.0165,0.00962776756845054,0.00823105056513178));
#11513=CARTESIAN_POINT('',(0.0165,0.00949251466430657,0.00813278357829554));
#11514=CARTESIAN_POINT('',(-0.0005,0.00969539401200001,0.00828018405299999));
#11515=CARTESIAN_POINT('',(0.0165,0.00989827347000001,0.00842758460699999));
#11516=CARTESIAN_POINT('',(0.00550000000333334,0.00989827347000001,0.00842758460699999));
#11517=CARTESIAN_POINT('',(-0.00549999999333334,0.00989827347000001,0.00842758460699999));
#11518=CARTESIAN_POINT('',(-0.01649999999,0.00989827347000001,0.00842758460699999));
#11519=CARTESIAN_POINT('',(-0.016499999995,0.00989827347007726,0.00842758460705612));
#11520=CARTESIAN_POINT('',(-0.01649999999,0.00989827347000001,0.00842758460699999));
#11521=CARTESIAN_POINT('',(-0.0168333333266667,0.00989827347000001,0.00842758460699999));
#11522=CARTESIAN_POINT('',(-0.0171666666633333,0.00989827347000001,0.00842758460699999));
#11523=CARTESIAN_POINT('',(-0.0175,0.00989827347000001,0.00842758460699999));
#11524=CARTESIAN_POINT('',(-0.0175,0.0098982734697996,0.00842758460672372));
#11525=CARTESIAN_POINT('',(-0.0175,0.00989827347000001,0.00842758460699999));
#11526=CARTESIAN_POINT('',(-0.0175,0.00976302049800001,0.00832931757099999));
#11527=CARTESIAN_POINT('',(-0.0175,0.00962776752600001,0.00823105053499999));
#11528=CARTESIAN_POINT('',(-0.0175,0.00949251455400001,0.00813278349899999));
#11529=CARTESIAN_POINT('',(-0.0175,0.011024942919,0.011024942919));
#11530=CARTESIAN_POINT('',(-0.0175,0.0139171023379207,0.010609630650532));
#11531=CARTESIAN_POINT('',(-0.0175,0.0125774927150801,0.00988228196907837));
#11532=CARTESIAN_POINT('',(-0.0175,0.0112378830922394,0.00915493328762477));
#11533=CARTESIAN_POINT('',(-0.0175,0.00989827346939877,0.00842758460617117));
#11534=CARTESIAN_POINT('',(-0.0174999997505,0.0139171023401316,0.01060963064646));
#11535=CARTESIAN_POINT('',(-0.0175000000005,0.,0.));
#11536=CARTESIAN_POINT('',(-0.0174999998752501,0.010609630582124,0.0139171022078995));
#11537=CARTESIAN_POINT('',(-0.0175,0.00842758460617116,0.00989827346939878));
#11538=CARTESIAN_POINT('',(-0.0175,0.00915493326425888,0.0112378830492048));
#11539=CARTESIAN_POINT('',(-0.0175,0.00988228192234659,0.0125774926290109));
#11540=CARTESIAN_POINT('',(-0.0175,0.0106096305804343,0.0139171022088169));
#11541=CARTESIAN_POINT('',(-0.0175,0.00842758460644744,0.00989827346959919));
#11542=CARTESIAN_POINT('',(-0.0175,0.0081327835680109,0.00949251464652199));
#11543=CARTESIAN_POINT('',(-0.0175,0.00823105058073098,0.00962776758748092));
#11544=CARTESIAN_POINT('',(-0.0175,0.00832931759345107,0.00976302052843985));
#11545=CARTESIAN_POINT('',(-0.0175,0.00842758460617116,0.00989827346939878));
#11546=CARTESIAN_POINT('',(-0.0005,0.00828018405299999,0.009695394012));
#11547=CARTESIAN_POINT('',(-0.0175,0.00842758460699999,0.00989827347000001));
#11548=CARTESIAN_POINT('',(-0.0171666666633333,0.00842758460699999,0.00989827347000001));
#11549=CARTESIAN_POINT('',(-0.0168333333266667,0.00842758460699999,0.00989827347000001));
#11550=CARTESIAN_POINT('',(-0.01649999999,0.00842758460699999,0.00989827347000001));
#11551=CARTESIAN_POINT('',(-0.016499999995,0.00842758460704643,0.00989827347008551));
#11552=CARTESIAN_POINT('',(-0.01649999999,0.00842758460699999,0.00989827347000001));
#11553=CARTESIAN_POINT('',(-0.00549999999333333,0.00842758460699999,0.00989827347000001));
#11554=CARTESIAN_POINT('',(0.00550000000333333,0.00842758460699999,0.00989827347000001));
#11555=CARTESIAN_POINT('',(0.0165,0.00842758460699999,0.00989827347000001));
#11556=CARTESIAN_POINT('',(0.0165,0.00842758446010981,0.00989827326782301));
#11557=CARTESIAN_POINT('',(0.0165,0.00842758446010981,0.00989827326782301));
#11558=CARTESIAN_POINT('',(0.0165,0.0083293174730732,0.00976302036321534));
#11559=CARTESIAN_POINT('',(0.0165,0.0082310504860366,0.00962776745860767));
#11560=CARTESIAN_POINT('',(0.0165,0.00813278349899999,0.009492514554));
#11561=CARTESIAN_POINT('',(0.0165,0.0074711670585,0.0102831792645));
#11562=CARTESIAN_POINT('',(0.0165,0.,0.));
#11563=CARTESIAN_POINT('',(0.0165,0.0068095505505698,0.0110738438809193));
#11564=CARTESIAN_POINT('',(0.0165,0.0068095505505197,0.0110738438809557));
#11565=CARTESIAN_POINT('',(0.0165,0.00671128356354459,0.0109385909766206));
#11566=CARTESIAN_POINT('',(0.0165,0.00661301657656948,0.0108033380722855));
#11567=CARTESIAN_POINT('',(0.0165,0.00651474958959437,0.0106680851679504));
#11568=CARTESIAN_POINT('',(-0.0005,0.00666215006449997,0.010870964517));
#11569=CARTESIAN_POINT('',(0.0165,0.00680955061899998,0.011073843975));
#11570=CARTESIAN_POINT('',(0.00550000000333333,0.00680955061899998,0.011073843975));
#11571=CARTESIAN_POINT('',(-0.00549999999333332,0.00680955061899998,0.011073843975));
#11572=CARTESIAN_POINT('',(-0.01649999999,0.00680955061899998,0.011073843975));
#11573=CARTESIAN_POINT('',(-0.016499999995,0.00680955061882576,0.0110738439747602));
#11574=CARTESIAN_POINT('',(-0.01649999999,0.00680955061899998,0.011073843975));
#11575=CARTESIAN_POINT('',(-0.0168333333266667,0.00680955061899998,0.011073843975));
#11576=CARTESIAN_POINT('',(-0.0171666666633333,0.00680955061899998,0.011073843975));
#11577=CARTESIAN_POINT('',(-0.0175,0.00680955061899998,0.011073843975));
#11578=CARTESIAN_POINT('',(-0.0175,0.00680955061901203,0.0110738439748256));
#11579=CARTESIAN_POINT('',(-0.0175,0.00680955061899998,0.011073843975));
#11580=CARTESIAN_POINT('',(-0.0175,0.00671128358266665,0.010938591003));
#11581=CARTESIAN_POINT('',(-0.0175,0.00661301654633331,0.010803338031));
#11582=CARTESIAN_POINT('',(-0.0175,0.00651474950999998,0.010668085059));
#11583=CARTESIAN_POINT('',(-0.0175,0.0073793915595,0.0135912960505));
#11584=CARTESIAN_POINT('',(-0.0175,0.00995739469288571,0.0143909794967367));
#11585=CARTESIAN_POINT('',(-0.0175,0.00890811333493585,0.0132852676559834));
#11586=CARTESIAN_POINT('',(-0.0175,0.00785883197698599,0.0121795558152301));
#11587=CARTESIAN_POINT('',(-0.0175,0.00680955061903612,0.0110738439744768));
#11588=CARTESIAN_POINT('',(-0.0174999997505,0.00995739468550641,0.0143909795037394));
#11589=CARTESIAN_POINT('',(-0.0175000000005,0.,0.));
#11590=CARTESIAN_POINT('',(-0.0174999998752501,0.00578973719816985,0.0165145068983457));
#11591=CARTESIAN_POINT('',(-0.0175,0.00495637454030183,0.0120180843498873));
#11592=CARTESIAN_POINT('',(-0.0175,0.00523416209333093,0.0135168918659648));
#11593=CARTESIAN_POINT('',(-0.0175,0.00551194964636003,0.0150156993820422));
#11594=CARTESIAN_POINT('',(-0.0175,0.00578973719938913,0.0165145068981197));
#11595=CARTESIAN_POINT('',(-0.0175,0.00495637454020122,0.0120180843495915));
#11596=CARTESIAN_POINT('',(-0.0175,0.00480138846212824,0.0115410862464871));
#11597=CARTESIAN_POINT('',(-0.0175,0.0048530504881861,0.0117000856142871));
#11598=CARTESIAN_POINT('',(-0.0175,0.00490471251424396,0.0118590849820872));
#11599=CARTESIAN_POINT('',(-0.0175,0.00495637454030183,0.0120180843498873));
#11600=CARTESIAN_POINT('',(-0.0005,0.004878881483,0.011779585242));
#11601=CARTESIAN_POINT('',(-0.0175,0.00495637454,0.012018084349));
#11602=CARTESIAN_POINT('',(-0.0171666666633333,0.00495637454,0.012018084349));
#11603=CARTESIAN_POINT('',(-0.0168333333266667,0.00495637454,0.012018084349));
#11604=CARTESIAN_POINT('',(-0.01649999999,0.00495637454,0.012018084349));
#11605=CARTESIAN_POINT('',(-0.016499999995,0.00495637453999843,0.0120180843489915));
#11606=CARTESIAN_POINT('',(-0.01649999999,0.00495637454,0.012018084349));
#11607=CARTESIAN_POINT('',(-0.00549999999333334,0.00495637454,0.012018084349));
#11608=CARTESIAN_POINT('',(0.00550000000333334,0.00495637454,0.012018084349));
#11609=CARTESIAN_POINT('',(0.0165,0.00495637454,0.012018084349));
#11610=CARTESIAN_POINT('',(0.0165,0.00495637446274314,0.0120180841112278));
#11611=CARTESIAN_POINT('',(0.0165,0.00495637446274314,0.0120180841112278));
#11612=CARTESIAN_POINT('',(0.0165,0.00490471245049542,0.0118590847858185));
#11613=CARTESIAN_POINT('',(0.0165,0.00485305043824771,0.0117000854604093));
#11614=CARTESIAN_POINT('',(0.0165,0.004801388426,0.011541086135));
#11615=CARTESIAN_POINT('',(0.0165,0.0039278249665,0.0120886022365));
#11616=CARTESIAN_POINT('',(0.0165,0.,0.));
#11617=CARTESIAN_POINT('',(0.0165,0.0030542614722702,0.0126361182276936));
#11618=CARTESIAN_POINT('',(0.0165,0.00305426147237052,0.012636118227661));
#11619=CARTESIAN_POINT('',(0.0165,0.00300259945997777,0.0124771189027652));
#11620=CARTESIAN_POINT('',(0.0165,0.00295093744758501,0.0123181195778693));
#11621=CARTESIAN_POINT('',(0.0165,0.00289927543519226,0.0121591202529734));
#11622=CARTESIAN_POINT('',(-0.0005,0.0029767684505,0.012397619231));
#11623=CARTESIAN_POINT('',(0.0165,0.003054261508,0.012636118338));
#11624=CARTESIAN_POINT('',(0.00550000000333333,0.003054261508,0.012636118338));
#11625=CARTESIAN_POINT('',(-0.00549999999333333,0.003054261508,0.012636118338));
#11626=CARTESIAN_POINT('',(-0.01649999999,0.003054261508,0.012636118338));
#11627=CARTESIAN_POINT('',(-0.016499999995,0.00305426150793331,0.0126361183377947));
#11628=CARTESIAN_POINT('',(-0.01649999999,0.003054261508,0.012636118338));
#11629=CARTESIAN_POINT('',(-0.0168333333266667,0.003054261508,0.012636118338));
#11630=CARTESIAN_POINT('',(-0.0171666666633333,0.003054261508,0.012636118338));
#11631=CARTESIAN_POINT('',(-0.0175,0.003054261508,0.012636118338));
#11632=CARTESIAN_POINT('',(-0.0175,0.003054261507645,0.0126361183377328));
#11633=CARTESIAN_POINT('',(-0.0175,0.003054261508,0.012636118338));
#11634=CARTESIAN_POINT('',(-0.0175,0.00300259946966667,0.0124771189333333));
#11635=CARTESIAN_POINT('',(-0.0175,0.00295093743133333,0.0123181195286667));
#11636=CARTESIAN_POINT('',(-0.0175,0.002899275393,0.012159120124));
#11637=CARTESIAN_POINT('',(-0.0175,0.002713045933,0.0148272384279999));
#11638=CARTESIAN_POINT('',(-0.0175,0.00502298787693344,0.0167636390075219));
#11639=CARTESIAN_POINT('',(-0.0175,0.00436674575360062,0.0153877987840808));
#11640=CARTESIAN_POINT('',(-0.0175,0.0037105036302678,0.0140119585606397));
#11641=CARTESIAN_POINT('',(-0.0175,0.00305426150693498,0.0126361183371986));
#11642=CARTESIAN_POINT('',(-0.0174999997505,0.00502298787463437,0.0167636390086185));
#11643=CARTESIAN_POINT('',(-0.0175000000005,0.,0.));
#11644=CARTESIAN_POINT('',(-0.0174999998752501,0.000403104009047257,0.0174953565861415));
#11645=CARTESIAN_POINT('',(-0.0175,0.00100000000007961,0.0129614813976545));
#11646=CARTESIAN_POINT('',(-0.0175,0.000801034669530588,0.0144727731271232));
#11647=CARTESIAN_POINT('',(-0.0175,0.000602069338981565,0.0159840648565919));
#11648=CARTESIAN_POINT('',(-0.0175,0.000403104008432543,0.0174953565860606));
#11649=CARTESIAN_POINT('',(-0.0175,0.00100000000005307,0.0129614813974363));
#11650=CARTESIAN_POINT('',(-0.0175,0.00100000000007961,0.012459935909242));
#11651=CARTESIAN_POINT('',(-0.0175,0.00100000000007961,0.0126271177387128));
#11652=CARTESIAN_POINT('',(-0.0175,0.00100000000007961,0.0127942995681836));
#11653=CARTESIAN_POINT('',(-0.0175,0.00100000000007961,0.0129614813976545));
#11654=CARTESIAN_POINT('',(-0.0005,0.001,0.0127107085955));
#11655=CARTESIAN_POINT('',(-0.0175,0.001,0.012961481397));
#11656=CARTESIAN_POINT('',(-0.0171666666633333,0.001,0.012961481397));
#11657=CARTESIAN_POINT('',(-0.0168333333266667,0.001,0.012961481397));
#11658=CARTESIAN_POINT('',(-0.01649999999,0.001,0.012961481397));
#11659=CARTESIAN_POINT('',(-0.016499999995,0.00100000000001226,0.0129614813969069));
#11660=CARTESIAN_POINT('',(-0.01649999999,0.001,0.012961481397));
#11661=CARTESIAN_POINT('',(-0.00549999999333333,0.001,0.012961481397));
#11662=CARTESIAN_POINT('',(0.00550000000333333,0.001,0.012961481397));
#11663=CARTESIAN_POINT('',(0.0165,0.001,0.012961481397));
#11664=CARTESIAN_POINT('',(0.0165,0.001,0.0129614811469079));
#11665=CARTESIAN_POINT('',(0.0165,0.001,0.0129614811469079));
#11666=CARTESIAN_POINT('',(0.0165,0.001,0.0127942993626052));
#11667=CARTESIAN_POINT('',(0.0165,0.001,0.0126271175783026));
#11668=CARTESIAN_POINT('',(0.0165,0.001,0.012459935794));
#11669=CARTESIAN_POINT('',(0.0165,-1.73472347597681E-19,0.0127315880896833));
#11670=CARTESIAN_POINT('',(0.0165,0.,0.));
#11671=CARTESIAN_POINT('',(0.0165,-0.001,0.0129614812809713));
#11672=CARTESIAN_POINT('',(0.0165,-0.001,0.0129614812809713));
#11673=CARTESIAN_POINT('',(0.0165,-0.001,0.0127942994972893));
#11674=CARTESIAN_POINT('',(0.0165,-0.001,0.0126271177136073));
#11675=CARTESIAN_POINT('',(0.0165,-0.001,0.0124599359299253));
#11676=CARTESIAN_POINT('',(-0.0005,-0.001,0.0127107085955));
#11677=CARTESIAN_POINT('',(0.0165,-0.001,0.012961481397));
#11678=CARTESIAN_POINT('',(0.00550000000333333,-0.001,0.012961481397));
#11679=CARTESIAN_POINT('',(-0.00549999999333333,-0.001,0.012961481397));
#11680=CARTESIAN_POINT('',(-0.01649999999,-0.001,0.012961481397));
#11681=CARTESIAN_POINT('',(-0.016499999995,-0.001,0.0129614813969079));
#11682=CARTESIAN_POINT('',(-0.01649999999,-0.001,0.012961481397));
#11683=CARTESIAN_POINT('',(-0.0168333333266667,-0.001,0.012961481397));
#11684=CARTESIAN_POINT('',(-0.0171666666633333,-0.001,0.012961481397));
#11685=CARTESIAN_POINT('',(-0.0175,-0.001,0.012961481397));
#11686=CARTESIAN_POINT('',(-0.0175,-0.00100000000002654,0.0129614813972181));
#11687=CARTESIAN_POINT('',(-0.0175,-0.001,0.012961481397));
#11688=CARTESIAN_POINT('',(-0.0175,-0.001,0.0127942995293333));
#11689=CARTESIAN_POINT('',(-0.0175,-0.001,0.0126271176616667));
#11690=CARTESIAN_POINT('',(-0.0175,-0.001,0.012459935794));
#11691=CARTESIAN_POINT('',(-0.0175,-0.002713045933,0.0148272384279999));
#11692=CARTESIAN_POINT('',(-0.0175,-0.00040310398916736,0.0174953567323942));
#11693=CARTESIAN_POINT('',(-0.0175,-0.00060206932613811,0.0159840649541476));
#11694=CARTESIAN_POINT('',(-0.0175,-0.00080103466310886,0.014472773175901));
#11695=CARTESIAN_POINT('',(-0.0175,-0.00100000000007961,0.0129614813976545));
#11696=CARTESIAN_POINT('',(-0.0174999997505,-0.00040310398550689,0.0174953567319123));
#11697=CARTESIAN_POINT('',(-0.0175000000005,0.,0.));
#11698=CARTESIAN_POINT('',(-0.0174999998752501,-0.00502298781032175,0.0167636388765541));
#11699=CARTESIAN_POINT('',(-0.0175,-0.00305426150693499,0.0126361183371986));
#11700=CARTESIAN_POINT('',(-0.0175,-0.00371050360918903,0.0140119585164471));
#11701=CARTESIAN_POINT('',(-0.0175,-0.00436674571144307,0.0153877986956956));
#11702=CARTESIAN_POINT('',(-0.0175,-0.00502298781369711,0.0167636388749442));
#11703=CARTESIAN_POINT('',(-0.0175,-0.00305426150728999,0.0126361183374657));
#11704=CARTESIAN_POINT('',(-0.0175,-0.00289927542916025,0.0121591202350179));
#11705=CARTESIAN_POINT('',(-0.0175,-0.00295093745508516,0.0123181196024115));
#11706=CARTESIAN_POINT('',(-0.0175,-0.00300259948101008,0.012477118969805));
#11707=CARTESIAN_POINT('',(-0.0175,-0.00305426150693499,0.0126361183371986));
#11708=CARTESIAN_POINT('',(-0.0005,-0.0029767684505,0.012397619231));
#11709=CARTESIAN_POINT('',(-0.0175,-0.003054261508,0.012636118338));
#11710=CARTESIAN_POINT('',(-0.0171666666633333,-0.003054261508,0.012636118338));
#11711=CARTESIAN_POINT('',(-0.0168333333266667,-0.003054261508,0.012636118338));
#11712=CARTESIAN_POINT('',(-0.01649999999,-0.003054261508,0.012636118338));
#11713=CARTESIAN_POINT('',(-0.016499999995,-0.00305426150790531,0.0126361183378015));
#11714=CARTESIAN_POINT('',(-0.01649999999,-0.003054261508,0.012636118338));
#11715=CARTESIAN_POINT('',(-0.00549999999333333,-0.003054261508,0.012636118338));
#11716=CARTESIAN_POINT('',(0.00550000000333333,-0.003054261508,0.012636118338));
#11717=CARTESIAN_POINT('',(0.0165,-0.003054261508,0.012636118338));
#11718=CARTESIAN_POINT('',(0.0165,-0.00305426143067905,0.0126361181000306));
#11719=CARTESIAN_POINT('',(0.0165,-0.00305426143067905,0.0126361181000306));
#11720=CARTESIAN_POINT('',(0.0165,-0.00300259941811937,0.0124771187746871));
#11721=CARTESIAN_POINT('',(0.0165,-0.00295093740555969,0.0123181194493435));
#11722=CARTESIAN_POINT('',(0.0165,-0.002899275393,0.012159120124));
#11723=CARTESIAN_POINT('',(0.0165,-0.0039278249665,0.0120886022365));
#11724=CARTESIAN_POINT('',(0.0165,0.,0.));
#11725=CARTESIAN_POINT('',(0.0165,-0.00495637450404248,0.0120180842387746));
#11726=CARTESIAN_POINT('',(0.0165,-0.00495637450391302,0.0120180842388167));
#11727=CARTESIAN_POINT('',(0.0165,-0.00490471249152739,0.0118590849139427));
#11728=CARTESIAN_POINT('',(0.0165,-0.00485305047914175,0.0117000855890688));
#11729=CARTESIAN_POINT('',(0.0165,-0.00480138846675611,0.0115410862641948));
#11730=CARTESIAN_POINT('',(-0.0005,-0.004878881483,0.011779585242));
#11731=CARTESIAN_POINT('',(0.0165,-0.00495637454,0.012018084349));
#11732=CARTESIAN_POINT('',(0.00550000000333333,-0.00495637454,0.012018084349));
#11733=CARTESIAN_POINT('',(-0.00549999999333332,-0.00495637454,0.012018084349));
#11734=CARTESIAN_POINT('',(-0.01649999999,-0.00495637454,0.012018084349));
#11735=CARTESIAN_POINT('',(-0.016499999995,-0.00495637453999739,0.0120180843489919));
#11736=CARTESIAN_POINT('',(-0.01649999999,-0.00495637454,0.012018084349));
#11737=CARTESIAN_POINT('',(-0.0168333333266667,-0.00495637454,0.012018084349));
#11738=CARTESIAN_POINT('',(-0.0171666666633333,-0.00495637454,0.012018084349));
#11739=CARTESIAN_POINT('',(-0.0175,-0.00495637454,0.012018084349));
#11740=CARTESIAN_POINT('',(-0.0175,-0.00495637454010061,0.0120180843492958));
#11741=CARTESIAN_POINT('',(-0.0175,-0.00495637454,0.012018084349));
#11742=CARTESIAN_POINT('',(-0.0175,-0.004904712502,0.0118590849443333));
#11743=CARTESIAN_POINT('',(-0.0175,-0.004853050464,0.0117000855396667));
#11744=CARTESIAN_POINT('',(-0.0175,-0.004801388426,0.011541086135));
#11745=CARTESIAN_POINT('',(-0.0175,-0.0073793915595,0.0135912960505));
#11746=CARTESIAN_POINT('',(-0.0175,-0.00578973722584464,0.0165145070408609));
#11747=CARTESIAN_POINT('',(-0.0175,-0.00551194966399704,0.015015699477203));
#11748=CARTESIAN_POINT('',(-0.0175,-0.00523416210214944,0.0135168919135451));
#11749=CARTESIAN_POINT('',(-0.0175,-0.00495637454030183,0.0120180843498873));
#11750=CARTESIAN_POINT('',(-0.0174999997505,-0.00578973723556005,0.0165145070390602));
#11751=CARTESIAN_POINT('',(-0.0175000000005,0.,0.));
#11752=CARTESIAN_POINT('',(-0.0174999998752501,-0.00995739459343785,0.0143909793903514));
#11753=CARTESIAN_POINT('',(-0.0175,-0.00680955061903612,0.0110738439744768));
#11754=CARTESIAN_POINT('',(-0.0175,-0.0078588319435722,0.0121795557800194));
#11755=CARTESIAN_POINT('',(-0.0175,-0.00890811326810827,0.0132852675855619));
#11756=CARTESIAN_POINT('',(-0.0175,-0.00995739459264434,0.0143909793911044));
#11757=CARTESIAN_POINT('',(-0.0175,-0.00680955061902408,0.0110738439746512));
#11758=CARTESIAN_POINT('',(-0.0175,-0.00651474957677916,0.0106680851534263));
#11759=CARTESIAN_POINT('',(-0.0175,-0.00661301659086482,0.0108033380937765));
#11760=CARTESIAN_POINT('',(-0.0175,-0.00671128360495047,0.0109385910341267));
#11761=CARTESIAN_POINT('',(-0.0175,-0.00680955061903612,0.0110738439744768));
#11762=CARTESIAN_POINT('',(-0.0005,-0.00666215006449998,0.010870964517));
#11763=CARTESIAN_POINT('',(-0.0175,-0.00680955061899999,0.011073843975));
#11764=CARTESIAN_POINT('',(-0.0171666666633333,-0.00680955061899999,0.011073843975));
#11765=CARTESIAN_POINT('',(-0.0168333333266667,-0.00680955061899999,0.011073843975));
#11766=CARTESIAN_POINT('',(-0.01649999999,-0.00680955061899999,0.011073843975));
#11767=CARTESIAN_POINT('',(-0.016499999995,-0.00680955061879209,0.0110738439747809));
#11768=CARTESIAN_POINT('',(-0.01649999999,-0.00680955061899999,0.011073843975));
#11769=CARTESIAN_POINT('',(-0.00549999999333334,-0.00680955061899999,0.011073843975));
#11770=CARTESIAN_POINT('',(0.00550000000333334,-0.00680955061899999,0.011073843975));
#11771=CARTESIAN_POINT('',(0.0165,-0.00680955061899999,0.011073843975));
#11772=CARTESIAN_POINT('',(0.0165,-0.00680955047187945,0.011073843772506));
#11773=CARTESIAN_POINT('',(0.0165,-0.00680955047187945,0.011073843772506));
#11774=CARTESIAN_POINT('',(0.0165,-0.0067112834845863,0.010938590868004));
#11775=CARTESIAN_POINT('',(0.0165,-0.00661301649729314,0.010803337963502));
#11776=CARTESIAN_POINT('',(0.0165,-0.00651474950999999,0.010668085059));
#11777=CARTESIAN_POINT('',(0.0165,-0.0074711670585,0.0102831792645));
#11778=CARTESIAN_POINT('',(0.0165,0.,0.));
#11779=CARTESIAN_POINT('',(0.0165,-0.00842758453894735,0.00989827337663452));
#11780=CARTESIAN_POINT('',(0.0165,-0.00842758453880426,0.00989827337673848));
#11781=CARTESIAN_POINT('',(0.0165,-0.00832931755194793,0.00976302047256686));
#11782=CARTESIAN_POINT('',(0.0165,-0.0082310505650916,0.00962776756839523));
#11783=CARTESIAN_POINT('',(0.0165,-0.00813278357823527,0.00949251466422361));
#11784=CARTESIAN_POINT('',(-0.0005,-0.00828018405299999,0.00969539401200001));
#11785=CARTESIAN_POINT('',(0.0165,-0.00842758460699999,0.00989827347000001));
#11786=CARTESIAN_POINT('',(0.00550000000333334,-0.00842758460699999,0.00989827347000001));
#11787=CARTESIAN_POINT('',(-0.00549999999333334,-0.00842758460699999,0.00989827347000001));
#11788=CARTESIAN_POINT('',(-0.01649999999,-0.00842758460699999,0.00989827347000001));
#11789=CARTESIAN_POINT('',(-0.016499999995,-0.00842758460705612,0.00989827347007726));
#11790=CARTESIAN_POINT('',(-0.01649999999,-0.00842758460699999,0.00989827347000001));
#11791=CARTESIAN_POINT('',(-0.0168333333266667,-0.00842758460699999,0.00989827347000001));
#11792=CARTESIAN_POINT('',(-0.0171666666633333,-0.00842758460699999,0.00989827347000001));
#11793=CARTESIAN_POINT('',(-0.0175,-0.00842758460699999,0.00989827347000001));
#11794=CARTESIAN_POINT('',(-0.0175,-0.00842758460672372,0.0098982734697996));
#11795=CARTESIAN_POINT('',(-0.0175,-0.00842758460699999,0.00989827347000001));
#11796=CARTESIAN_POINT('',(-0.0175,-0.00832931757099999,0.00976302049800001));
#11797=CARTESIAN_POINT('',(-0.0175,-0.00823105053499999,0.00962776752600001));
#11798=CARTESIAN_POINT('',(-0.0175,-0.00813278349899999,0.00949251455400001));
#11799=CARTESIAN_POINT('',(-0.0175,-0.011024942919,0.011024942919));
#11800=CARTESIAN_POINT('',(-0.0175,-0.0106096306502694,0.0139171023374371));
#11801=CARTESIAN_POINT('',(-0.0175,-0.0098822819689033,0.0125774927147576));
#11802=CARTESIAN_POINT('',(-0.0175,-0.00915493328753723,0.0112378830920782));
#11803=CARTESIAN_POINT('',(-0.0175,-0.00842758460617116,0.00989827346939878));
#11804=CARTESIAN_POINT('',(-0.0174999997505,-0.0106096306493144,0.0139171023379556));
#11805=CARTESIAN_POINT('',(-0.0175000000005,0.,0.));
#11806=CARTESIAN_POINT('',(-0.0174999998752501,-0.0139171022089875,0.0106096305806968));
#11807=CARTESIAN_POINT('',(-0.0175,-0.00989827346939877,0.00842758460617117));
#11808=CARTESIAN_POINT('',(-0.0175,-0.0112378830492854,0.00915493326430265));
#11809=CARTESIAN_POINT('',(-0.0175,-0.0125774926291721,0.00988228192243413));
#11810=CARTESIAN_POINT('',(-0.0175,-0.0139171022090587,0.0106096305805656));
#11811=CARTESIAN_POINT('',(-0.0175,-0.00989827346959919,0.00842758460644744));
#11812=CARTESIAN_POINT('',(-0.0175,-0.00949251464660495,0.00813278356807117));
#11813=CARTESIAN_POINT('',(-0.0175,-0.00962776758753623,0.00823105058077117));
#11814=CARTESIAN_POINT('',(-0.0175,-0.0097630205284675,0.00832931759347117));
#11815=CARTESIAN_POINT('',(-0.0175,-0.00989827346939877,0.00842758460617117));
#11816=CARTESIAN_POINT('',(-0.0005,-0.009695394012,0.00828018405299999));
#11817=CARTESIAN_POINT('',(-0.0175,-0.00989827347000001,0.00842758460699999));
#11818=CARTESIAN_POINT('',(-0.0171666666633333,-0.00989827347000001,0.00842758460699999));
#11819=CARTESIAN_POINT('',(-0.0168333333266667,-0.00989827347000001,0.00842758460699999));
#11820=CARTESIAN_POINT('',(-0.01649999999,-0.00989827347000001,0.00842758460699999));
#11821=CARTESIAN_POINT('',(-0.016499999995,-0.00989827347008551,0.00842758460704643));
#11822=CARTESIAN_POINT('',(-0.01649999999,-0.00989827347000001,0.00842758460699999));
#11823=CARTESIAN_POINT('',(-0.00549999999333333,-0.00989827347000001,0.00842758460699999));
#11824=CARTESIAN_POINT('',(0.00550000000333333,-0.00989827347000001,0.00842758460699999));
#11825=CARTESIAN_POINT('',(0.0165,-0.00989827347000001,0.00842758460699999));
#11826=CARTESIAN_POINT('',(0.0165,-0.00989827326782301,0.00842758446010981));
#11827=CARTESIAN_POINT('',(0.0165,-0.00989827326782301,0.00842758446010981));
#11828=CARTESIAN_POINT('',(0.0165,-0.00976302036321534,0.0083293174730732));
#11829=CARTESIAN_POINT('',(0.0165,-0.00962776745860767,0.0082310504860366));
#11830=CARTESIAN_POINT('',(0.0165,-0.009492514554,0.00813278349899999));
#11831=CARTESIAN_POINT('',(0.0165,-0.0102831792645,0.0074711670585));
#11832=CARTESIAN_POINT('',(0.0165,0.,0.));
#11833=CARTESIAN_POINT('',(0.0165,-0.0110738438809193,0.0068095505505698));
#11834=CARTESIAN_POINT('',(0.0165,-0.0110738438809557,0.0068095505505197));
#11835=CARTESIAN_POINT('',(0.0165,-0.0109385909767278,0.00671128356362246));
#11836=CARTESIAN_POINT('',(0.0165,-0.0108033380724998,0.00661301657672522));
#11837=CARTESIAN_POINT('',(0.0165,-0.0106680851682719,0.00651474958982798));
#11838=CARTESIAN_POINT('',(-0.0005,-0.010870964517,0.00666215006449997));
#11839=CARTESIAN_POINT('',(0.0165,-0.011073843975,0.00680955061899998));
#11840=CARTESIAN_POINT('',(0.00550000000333333,-0.011073843975,0.00680955061899998));
#11841=CARTESIAN_POINT('',(-0.00549999999333332,-0.011073843975,0.00680955061899998));
#11842=CARTESIAN_POINT('',(-0.01649999999,-0.011073843975,0.00680955061899998));
#11843=CARTESIAN_POINT('',(-0.016499999995,-0.0110738439747602,0.00680955061882576));
#11844=CARTESIAN_POINT('',(-0.01649999999,-0.011073843975,0.00680955061899998));
#11845=CARTESIAN_POINT('',(-0.0168333333266667,-0.011073843975,0.00680955061899998));
#11846=CARTESIAN_POINT('',(-0.0171666666633333,-0.011073843975,0.00680955061899998));
#11847=CARTESIAN_POINT('',(-0.0175,-0.011073843975,0.00680955061899998));
#11848=CARTESIAN_POINT('',(-0.0175,-0.0110738439748256,0.00680955061901203));
#11849=CARTESIAN_POINT('',(-0.0175,-0.011073843975,0.00680955061899998));
#11850=CARTESIAN_POINT('',(-0.0175,-0.010938591003,0.00671128358266665));
#11851=CARTESIAN_POINT('',(-0.0175,-0.010803338031,0.00661301654633331));
#11852=CARTESIAN_POINT('',(-0.0175,-0.010668085059,0.00651474950999998));
#11853=CARTESIAN_POINT('',(-0.0175,-0.0135912960505,0.0073793915595));
#11854=CARTESIAN_POINT('',(-0.0175,-0.0143909794982839,0.00995739469435391));
#11855=CARTESIAN_POINT('',(-0.0175,-0.0132852676570149,0.00890811333591465));
#11856=CARTESIAN_POINT('',(-0.0175,-0.0121795558157459,0.00785883197747539));
#11857=CARTESIAN_POINT('',(-0.0175,-0.0110738439744768,0.00680955061903613));
#11858=CARTESIAN_POINT('',(-0.0174999997505,-0.0143909794958243,0.00995739469694575));
#11859=CARTESIAN_POINT('',(-0.0175000000005,0.,0.));
#11860=CARTESIAN_POINT('',(-0.0174999998752501,-0.0165145068989394,0.00578973719647625));
#11861=CARTESIAN_POINT('',(-0.0175,-0.0120180843498873,0.00495637454030183));
#11862=CARTESIAN_POINT('',(-0.0175,-0.013516891866055,0.00523416209334765));
#11863=CARTESIAN_POINT('',(-0.0175,-0.0150156993822226,0.00551194964639347));
#11864=CARTESIAN_POINT('',(-0.0175,-0.0165145068983903,0.00578973719943929));
#11865=CARTESIAN_POINT('',(-0.0175,-0.0120180843495915,0.00495637454020122));
#11866=CARTESIAN_POINT('',(-0.0175,-0.0115410862465846,0.00480138846215994));
#11867=CARTESIAN_POINT('',(-0.0175,-0.0117000856143522,0.00485305048820723));
#11868=CARTESIAN_POINT('',(-0.0175,-0.0118590849821197,0.00490471251425453));
#11869=CARTESIAN_POINT('',(-0.0175,-0.0120180843498873,0.00495637454030183));
#11870=CARTESIAN_POINT('',(-0.0005,-0.011779585242,0.004878881483));
#11871=CARTESIAN_POINT('',(-0.0175,-0.012018084349,0.00495637454));
#11872=CARTESIAN_POINT('',(-0.0171666666633333,-0.012018084349,0.00495637454));
#11873=CARTESIAN_POINT('',(-0.0168333333266667,-0.012018084349,0.00495637454));
#11874=CARTESIAN_POINT('',(-0.01649999999,-0.012018084349,0.00495637454));
#11875=CARTESIAN_POINT('',(-0.016499999995,-0.0120180843489915,0.00495637453999843));
#11876=CARTESIAN_POINT('',(-0.01649999999,-0.012018084349,0.00495637454));
#11877=CARTESIAN_POINT('',(-0.00549999999333334,-0.012018084349,0.00495637454));
#11878=CARTESIAN_POINT('',(0.00550000000333334,-0.012018084349,0.00495637454));
#11879=CARTESIAN_POINT('',(0.0165,-0.012018084349,0.00495637454));
#11880=CARTESIAN_POINT('',(0.0165,-0.0120180841112278,0.00495637446274314));
#11881=CARTESIAN_POINT('',(0.0165,-0.0120180841112278,0.00495637446274314));
#11882=CARTESIAN_POINT('',(0.0165,-0.0118590847858185,0.00490471245049542));
#11883=CARTESIAN_POINT('',(0.0165,-0.0117000854604093,0.00485305043824771));
#11884=CARTESIAN_POINT('',(0.0165,-0.011541086135,0.004801388426));
#11885=CARTESIAN_POINT('',(0.0165,-0.0120886022365,0.00392782496649999));
#11886=CARTESIAN_POINT('',(0.0165,0.,0.));
#11887=CARTESIAN_POINT('',(0.0165,-0.0126361182276936,0.0030542614722702));
#11888=CARTESIAN_POINT('',(0.0165,-0.012636118227661,0.00305426147237052));
#11889=CARTESIAN_POINT('',(0.0165,-0.0124771189027327,0.0030025994599672));
#11890=CARTESIAN_POINT('',(0.0165,-0.0123181195778043,0.00295093744756389));
#11891=CARTESIAN_POINT('',(0.0165,-0.0121591202528759,0.00289927543516057));
#11892=CARTESIAN_POINT('',(-0.0005,-0.012397619231,0.0029767684505));
#11893=CARTESIAN_POINT('',(0.0165,-0.012636118338,0.003054261508));
#11894=CARTESIAN_POINT('',(0.00550000000333333,-0.012636118338,0.003054261508));
#11895=CARTESIAN_POINT('',(-0.00549999999333333,-0.012636118338,0.003054261508));
#11896=CARTESIAN_POINT('',(-0.01649999999,-0.012636118338,0.003054261508));
#11897=CARTESIAN_POINT('',(-0.016499999995,-0.0126361183377947,0.00305426150793331));
#11898=CARTESIAN_POINT('',(-0.01649999999,-0.012636118338,0.003054261508));
#11899=CARTESIAN_POINT('',(-0.0168333333266667,-0.012636118338,0.003054261508));
#11900=CARTESIAN_POINT('',(-0.0171666666633333,-0.012636118338,0.003054261508));
#11901=CARTESIAN_POINT('',(-0.0175,-0.012636118338,0.003054261508));
#11902=CARTESIAN_POINT('',(-0.0175,-0.0126361183377328,0.003054261507645));
#11903=CARTESIAN_POINT('',(-0.0175,-0.012636118338,0.003054261508));
#11904=CARTESIAN_POINT('',(-0.0175,-0.0124771189333333,0.00300259946966667));
#11905=CARTESIAN_POINT('',(-0.0175,-0.0123181195286667,0.00295093743133333));
#11906=CARTESIAN_POINT('',(-0.0175,-0.012159120124,0.002899275393));
#11907=CARTESIAN_POINT('',(-0.0175,-0.014827238428,0.002713045933));
#11908=CARTESIAN_POINT('',(-0.0175,-0.0167636390070252,0.00502298787669651));
#11909=CARTESIAN_POINT('',(-0.0175,-0.0153877987837496,0.00436674575344267));
#11910=CARTESIAN_POINT('',(-0.0175,-0.0140119585604741,0.00371050363018883));
#11911=CARTESIAN_POINT('',(-0.0175,-0.0126361183371986,0.00305426150693499));
#11912=CARTESIAN_POINT('',(-0.0174999997505,-0.0167636390096488,0.00502298787119609));
#11913=CARTESIAN_POINT('',(-0.0175000000005,0.,0.));
#11914=CARTESIAN_POINT('',(-0.0174999998752501,-0.0174953565861828,0.000403104007253075));
#11915=CARTESIAN_POINT('',(-0.0175,-0.0129614813976545,0.00100000000007961));
#11916=CARTESIAN_POINT('',(-0.0175,-0.0144727731272141,0.000801034669518615));
#11917=CARTESIAN_POINT('',(-0.0175,-0.0159840648567738,0.000602069338957621));
#11918=CARTESIAN_POINT('',(-0.0175,-0.0174953565863334,0.000403104008396626));
#11919=CARTESIAN_POINT('',(-0.0175,-0.0129614813974363,0.00100000000005307));
#11920=CARTESIAN_POINT('',(-0.0175,-0.0124599359093445,0.00100000000007961));
#11921=CARTESIAN_POINT('',(-0.0175,-0.0126271177387812,0.00100000000007961));
#11922=CARTESIAN_POINT('',(-0.0175,-0.0127942995682178,0.00100000000007961));
#11923=CARTESIAN_POINT('',(-0.0175,-0.0129614813976545,0.00100000000007961));
#11924=CARTESIAN_POINT('',(-0.0005,-0.0127107085955,0.001));
#11925=CARTESIAN_POINT('',(-0.0175,-0.012961481397,0.001));
#11926=CARTESIAN_POINT('',(-0.0171666666633333,-0.012961481397,0.001));
#11927=CARTESIAN_POINT('',(-0.0168333333266667,-0.012961481397,0.001));
#11928=CARTESIAN_POINT('',(-0.01649999999,-0.012961481397,0.001));
#11929=CARTESIAN_POINT('',(-0.016499999995,-0.0129614813969069,0.00100000000001226));
#11930=CARTESIAN_POINT('',(-0.01649999999,-0.012961481397,0.001));
#11931=CARTESIAN_POINT('',(-0.00549999999333333,-0.012961481397,0.001));
#11932=CARTESIAN_POINT('',(0.00550000000333333,-0.012961481397,0.001));
#11933=CARTESIAN_POINT('',(0.0165,-0.012961481397,0.001));
#11934=CARTESIAN_POINT('',(0.0165,-0.0129614811469079,0.001));
#11935=CARTESIAN_POINT('',(0.0165,-0.0129614811469079,0.001));
#11936=CARTESIAN_POINT('',(0.0165,-0.0127942993626052,0.001));
#11937=CARTESIAN_POINT('',(0.0165,-0.0126271175783026,0.001));
#11938=CARTESIAN_POINT('',(0.0165,-0.012459935794,0.001));
#11939=CARTESIAN_POINT('',(0.0165,-0.0127315880896833,-1.56125112837913E-19));
#11940=CARTESIAN_POINT('',(0.0165,0.,0.));
#11941=CARTESIAN_POINT('',(0.0165,-0.0129614812809713,-0.001));
#11942=CARTESIAN_POINT('',(0.0165,-0.0129614812809713,-0.001));
#11943=CARTESIAN_POINT('',(0.0165,-0.0127942994972252,-0.001));
#11944=CARTESIAN_POINT('',(0.0165,-0.0126271177134791,-0.001));
#11945=CARTESIAN_POINT('',(0.0165,-0.012459935929733,-0.001));
#11946=CARTESIAN_POINT('',(-0.0005,-0.0127107085955,-0.001));
#11947=CARTESIAN_POINT('',(0.0165,-0.012961481397,-0.001));
#11948=CARTESIAN_POINT('',(0.00550000000333333,-0.012961481397,-0.001));
#11949=CARTESIAN_POINT('',(-0.00549999999333333,-0.012961481397,-0.001));
#11950=CARTESIAN_POINT('',(-0.01649999999,-0.012961481397,-0.001));
#11951=CARTESIAN_POINT('',(-0.016499999995,-0.0129614813969079,-0.001));
#11952=CARTESIAN_POINT('',(-0.01649999999,-0.012961481397,-0.001));
#11953=CARTESIAN_POINT('',(-0.0168333333266667,-0.012961481397,-0.001));
#11954=CARTESIAN_POINT('',(-0.0171666666633333,-0.012961481397,-0.001));
#11955=CARTESIAN_POINT('',(-0.0175,-0.012961481397,-0.001));
#11956=CARTESIAN_POINT('',(-0.0175,-0.0129614813972181,-0.00100000000002654));
#11957=CARTESIAN_POINT('',(-0.0175,-0.012961481397,-0.001));
#11958=CARTESIAN_POINT('',(-0.0175,-0.0127942995293333,-0.001));
#11959=CARTESIAN_POINT('',(-0.0175,-0.0126271176616667,-0.001));
#11960=CARTESIAN_POINT('',(-0.0175,-0.012459935794,-0.001));
#11961=CARTESIAN_POINT('',(-0.0175,-0.014827238428,-0.002713045933));
#11962=CARTESIAN_POINT('',(-0.0175,-0.0174953567315252,-0.000403103989281762));
#11963=CARTESIAN_POINT('',(-0.0175,-0.0159840649535683,-0.000602069326214379));
#11964=CARTESIAN_POINT('',(-0.0175,-0.0144727731756114,-0.000801034663146997));
#11965=CARTESIAN_POINT('',(-0.0175,-0.0129614813976545,-0.00100000000007961));
#11966=CARTESIAN_POINT('',(-0.0174999998755,-0.0174953567317806,-0.000403103991221634));
#11967=CARTESIAN_POINT('',(-0.0175000000005,0.,0.));
#11968=CARTESIAN_POINT('',(-0.0174999998752501,-0.016763638875588,-0.00502298781354615));
#11969=CARTESIAN_POINT('',(-0.0175,-0.0126361183371986,-0.00305426150693499));
#11970=CARTESIAN_POINT('',(-0.0175,-0.0140119585166024,-0.00371050360926309));
#11971=CARTESIAN_POINT('',(-0.0175,-0.0153877986960062,-0.00436674571159119));
#11972=CARTESIAN_POINT('',(-0.0175,-0.01676363887541,-0.0050229878139193));
#11973=CARTESIAN_POINT('',(-0.0175,-0.0126361183374657,-0.00305426150728999));
#11974=CARTESIAN_POINT('',(-0.0175,-0.0121591202347253,-0.00289927542906519));
#11975=CARTESIAN_POINT('',(-0.0175,-0.0123181196022164,-0.00295093745502179));
#11976=CARTESIAN_POINT('',(-0.0175,-0.0124771189697075,-0.00300259948097839));
#11977=CARTESIAN_POINT('',(-0.0175,-0.0126361183371986,-0.00305426150693499));
#11978=CARTESIAN_POINT('',(-0.0005,-0.012397619231,-0.0029767684505));
#11979=CARTESIAN_POINT('',(-0.0175,-0.012636118338,-0.003054261508));
#11980=CARTESIAN_POINT('',(-0.0171666666633333,-0.012636118338,-0.003054261508));
#11981=CARTESIAN_POINT('',(-0.0168333333266667,-0.012636118338,-0.003054261508));
#11982=CARTESIAN_POINT('',(-0.01649999999,-0.012636118338,-0.003054261508));
#11983=CARTESIAN_POINT('',(-0.016499999995,-0.0126361183378015,-0.00305426150790531));
#11984=CARTESIAN_POINT('',(-0.01649999999,-0.012636118338,-0.003054261508));
#11985=CARTESIAN_POINT('',(-0.00549999999333333,-0.012636118338,-0.003054261508));
#11986=CARTESIAN_POINT('',(0.00550000000333333,-0.012636118338,-0.003054261508));
#11987=CARTESIAN_POINT('',(0.0165,-0.012636118338,-0.003054261508));
#11988=CARTESIAN_POINT('',(0.0165,-0.0126361181000306,-0.00305426143067905));
#11989=CARTESIAN_POINT('',(0.0165,-0.0126361181000306,-0.00305426143067905));
#11990=CARTESIAN_POINT('',(0.0165,-0.0124771187746871,-0.00300259941811937));
#11991=CARTESIAN_POINT('',(0.0165,-0.0123181194493435,-0.00295093740555969));
#11992=CARTESIAN_POINT('',(0.0165,-0.012159120124,-0.002899275393));
#11993=CARTESIAN_POINT('',(0.0165,-0.0120886022365,-0.00392782496650001));
#11994=CARTESIAN_POINT('',(0.0165,0.,0.));
#11995=CARTESIAN_POINT('',(0.0165,-0.0120180842387746,-0.00495637450404248));
#11996=CARTESIAN_POINT('',(0.0165,-0.0120180842388167,-0.00495637450391302));
#11997=CARTESIAN_POINT('',(0.0165,-0.0118590849140403,-0.00490471249155908));
#11998=CARTESIAN_POINT('',(0.0165,-0.0117000855892638,-0.00485305047920513));
#11999=CARTESIAN_POINT('',(0.0165,-0.0115410862644874,-0.00480138846685119));
#12000=CARTESIAN_POINT('',(-0.0005,-0.011779585242,-0.004878881483));
#12001=CARTESIAN_POINT('',(0.0165,-0.012018084349,-0.00495637454));
#12002=CARTESIAN_POINT('',(0.00550000000333333,-0.012018084349,-0.00495637454));
#12003=CARTESIAN_POINT('',(-0.00549999999333332,-0.012018084349,-0.00495637454));
#12004=CARTESIAN_POINT('',(-0.01649999999,-0.012018084349,-0.00495637454));
#12005=CARTESIAN_POINT('',(-0.016499999995,-0.0120180843489919,-0.00495637453999739));
#12006=CARTESIAN_POINT('',(-0.01649999999,-0.012018084349,-0.00495637454));
#12007=CARTESIAN_POINT('',(-0.0168333333266667,-0.012018084349,-0.00495637454));
#12008=CARTESIAN_POINT('',(-0.0171666666633333,-0.012018084349,-0.00495637454));
#12009=CARTESIAN_POINT('',(-0.0175,-0.012018084349,-0.00495637454));
#12010=CARTESIAN_POINT('',(-0.0175,-0.0120180843492958,-0.00495637454010061));
#12011=CARTESIAN_POINT('',(-0.0175,-0.012018084349,-0.00495637454));
#12012=CARTESIAN_POINT('',(-0.0175,-0.0118590849443333,-0.004904712502));
#12013=CARTESIAN_POINT('',(-0.0175,-0.0117000855396667,-0.004853050464));
#12014=CARTESIAN_POINT('',(-0.0175,-0.011541086135,-0.004801388426));
#12015=CARTESIAN_POINT('',(-0.0175,-0.0135912960505,-0.0073793915595));
#12016=CARTESIAN_POINT('',(-0.0175,-0.0165145070424843,-0.00578973722614552));
#12017=CARTESIAN_POINT('',(-0.0175,-0.0150156994782853,-0.00551194966419762));
#12018=CARTESIAN_POINT('',(-0.0175,-0.0135168919140863,-0.00523416210224972));
#12019=CARTESIAN_POINT('',(-0.0175,-0.0120180843498873,-0.00495637454030183));
#12020=CARTESIAN_POINT('',(-0.0174999997505,-0.0165145070426227,-0.0057897372253985));
#12021=CARTESIAN_POINT('',(-0.0175000000005,0.,0.));
#12022=CARTESIAN_POINT('',(-0.0174999998752501,-0.0143909793934148,-0.0099573945890104));
#12023=CARTESIAN_POINT('',(-0.0175,-0.0110738439744768,-0.00680955061903612));
#12024=CARTESIAN_POINT('',(-0.0175,-0.0121795557798198,-0.00785883194338278));
#12025=CARTESIAN_POINT('',(-0.0175,-0.0132852675851627,-0.00890811326772944));
#12026=CARTESIAN_POINT('',(-0.0175,-0.0143909793905056,-0.00995739459207609));
#12027=CARTESIAN_POINT('',(-0.0175,-0.0110738439746512,-0.00680955061902408));
#12028=CARTESIAN_POINT('',(-0.0175,-0.0106680851535819,-0.00651474957689222));
#12029=CARTESIAN_POINT('',(-0.0175,-0.0108033380938802,-0.00661301659094019));
#12030=CARTESIAN_POINT('',(-0.0175,-0.0109385910341785,-0.00671128360498816));
#12031=CARTESIAN_POINT('',(-0.0175,-0.0110738439744768,-0.00680955061903612));
#12032=CARTESIAN_POINT('',(-0.0005,-0.010870964517,-0.00666215006449998));
#12033=CARTESIAN_POINT('',(-0.0175,-0.011073843975,-0.00680955061899999));
#12034=CARTESIAN_POINT('',(-0.0171666666633333,-0.011073843975,-0.00680955061899999));
#12035=CARTESIAN_POINT('',(-0.0168333333266667,-0.011073843975,-0.00680955061899999));
#12036=CARTESIAN_POINT('',(-0.01649999999,-0.011073843975,-0.00680955061899999));
#12037=CARTESIAN_POINT('',(-0.016499999995,-0.0110738439747809,-0.00680955061879209));
#12038=CARTESIAN_POINT('',(-0.01649999999,-0.011073843975,-0.00680955061899999));
#12039=CARTESIAN_POINT('',(-0.00549999999333334,-0.011073843975,-0.00680955061899999));
#12040=CARTESIAN_POINT('',(0.00550000000333334,-0.011073843975,-0.00680955061899999));
#12041=CARTESIAN_POINT('',(0.0165,-0.011073843975,-0.00680955061899999));
#12042=CARTESIAN_POINT('',(0.0165,-0.011073843772506,-0.00680955047187945));
#12043=CARTESIAN_POINT('',(0.0165,-0.011073843772506,-0.00680955047187945));
#12044=CARTESIAN_POINT('',(0.0165,-0.010938590868004,-0.0067112834845863));
#12045=CARTESIAN_POINT('',(0.0165,-0.010803337963502,-0.00661301649729314));
#12046=CARTESIAN_POINT('',(0.0165,-0.010668085059,-0.00651474950999999));
#12047=CARTESIAN_POINT('',(0.0165,-0.0102831792645,-0.0074711670585));
#12048=CARTESIAN_POINT('',(0.0165,0.,0.));
#12049=CARTESIAN_POINT('',(0.0165,-0.00989827337663452,-0.00842758453894735));
#12050=CARTESIAN_POINT('',(0.0165,-0.00989827337673848,-0.00842758453880425));
#12051=CARTESIAN_POINT('',(0.0165,-0.00976302047251499,-0.00832931755191023));
#12052=CARTESIAN_POINT('',(0.0165,-0.00962776756829149,-0.00823105056501622));
#12053=CARTESIAN_POINT('',(0.0165,-0.00949251466406799,-0.0081327835781222));
#12054=CARTESIAN_POINT('',(-0.0005,-0.00969539401200001,-0.00828018405299999));
#12055=CARTESIAN_POINT('',(0.0165,-0.00989827347000001,-0.00842758460699999));
#12056=CARTESIAN_POINT('',(0.00550000000333334,-0.00989827347000001,-0.00842758460699999));
#12057=CARTESIAN_POINT('',(-0.00549999999333334,-0.00989827347000001,-0.00842758460699999));
#12058=CARTESIAN_POINT('',(-0.01649999999,-0.00989827347000001,-0.00842758460699999));
#12059=CARTESIAN_POINT('',(-0.016499999995,-0.00989827347007726,-0.00842758460705612));
#12060=CARTESIAN_POINT('',(-0.01649999999,-0.00989827347000001,-0.00842758460699999));
#12061=CARTESIAN_POINT('',(-0.0168333333266667,-0.00989827347000001,-0.00842758460699999));
#12062=CARTESIAN_POINT('',(-0.0171666666633333,-0.00989827347000001,-0.00842758460699999));
#12063=CARTESIAN_POINT('',(-0.0175,-0.00989827347000001,-0.00842758460699999));
#12064=CARTESIAN_POINT('',(-0.0175,-0.0098982734697996,-0.00842758460672372));
#12065=CARTESIAN_POINT('',(-0.0175,-0.00989827347000001,-0.00842758460699999));
#12066=CARTESIAN_POINT('',(-0.0175,-0.00976302049800001,-0.00832931757099999));
#12067=CARTESIAN_POINT('',(-0.0175,-0.00962776752600001,-0.00823105053499999));
#12068=CARTESIAN_POINT('',(-0.0175,-0.00949251455400001,-0.00813278349899999));
#12069=CARTESIAN_POINT('',(-0.0175,-0.011024942919,-0.011024942919));
#12070=CARTESIAN_POINT('',(-0.0175,-0.0139171023365299,-0.0106096306497768));
#12071=CARTESIAN_POINT('',(-0.0175,-0.0125774927141529,-0.00988228196857495));
#12072=CARTESIAN_POINT('',(-0.0175,-0.0112378830917758,-0.00915493328737306));
#12073=CARTESIAN_POINT('',(-0.0175,-0.00989827346939877,-0.00842758460617117));
#12074=CARTESIAN_POINT('',(-0.0174999997505,-0.0139171023338741,-0.0106096306546682));
#12075=CARTESIAN_POINT('',(-0.0175000000005,0.,0.));
#12076=CARTESIAN_POINT('',(-0.0174999998752501,-0.0106096305780199,-0.0139171022110282));
#12077=CARTESIAN_POINT('',(-0.0175,-0.00842758460617116,-0.00989827346939879));
#12078=CARTESIAN_POINT('',(-0.0175,-0.00915493326438473,-0.0112378830494366));
#12079=CARTESIAN_POINT('',(-0.0175,-0.0098822819225983,-0.0125774926294745));
#12080=CARTESIAN_POINT('',(-0.0175,-0.0106096305808119,-0.0139171022095123));
#12081=CARTESIAN_POINT('',(-0.0175,-0.00842758460644744,-0.00989827346959919));
#12082=CARTESIAN_POINT('',(-0.0175,-0.00813278356818423,-0.00949251464676057));
#12083=CARTESIAN_POINT('',(-0.0175,-0.00823105058084654,-0.00962776758763998));
#12084=CARTESIAN_POINT('',(-0.0175,-0.00832931759350885,-0.00976302052851938));
#12085=CARTESIAN_POINT('',(-0.0175,-0.00842758460617116,-0.00989827346939879));
#12086=CARTESIAN_POINT('',(-0.0005,-0.00828018405299999,-0.009695394012));
#12087=CARTESIAN_POINT('',(-0.0175,-0.00842758460699999,-0.00989827347000001));
#12088=CARTESIAN_POINT('',(-0.0171666666633333,-0.00842758460699999,-0.00989827347000001));
#12089=CARTESIAN_POINT('',(-0.0168333333266667,-0.00842758460699999,-0.00989827347000001));
#12090=CARTESIAN_POINT('',(-0.01649999999,-0.00842758460699999,-0.00989827347000001));
#12091=CARTESIAN_POINT('',(-0.016499999995,-0.00842758460704643,-0.00989827347008551));
#12092=CARTESIAN_POINT('',(-0.01649999999,-0.00842758460699999,-0.00989827347000001));
#12093=CARTESIAN_POINT('',(-0.00549999999333333,-0.00842758460699999,-0.00989827347000001));
#12094=CARTESIAN_POINT('',(0.00550000000333333,-0.00842758460699999,-0.00989827347000001));
#12095=CARTESIAN_POINT('',(0.0165,-0.00842758460699999,-0.00989827347000001));
#12096=CARTESIAN_POINT('',(0.0165,-0.00842758446010981,-0.00989827326782301));
#12097=CARTESIAN_POINT('',(0.0165,-0.00842758446010981,-0.00989827326782301));
#12098=CARTESIAN_POINT('',(0.0165,-0.0083293174730732,-0.00976302036321534));
#12099=CARTESIAN_POINT('',(0.0165,-0.0082310504860366,-0.00962776745860767));
#12100=CARTESIAN_POINT('',(0.0165,-0.00813278349899999,-0.009492514554));
#12101=CARTESIAN_POINT('',(0.0165,-0.0074711670585,-0.0102831792645));
#12102=CARTESIAN_POINT('',(0.0165,0.,0.));
#12103=CARTESIAN_POINT('',(0.0165,-0.0068095505505698,-0.0110738438809193));
#12104=CARTESIAN_POINT('',(0.0165,-0.00680955055051969,-0.0110738438809557));
#12105=CARTESIAN_POINT('',(0.0165,-0.00671128356358477,-0.0109385909766759));
#12106=CARTESIAN_POINT('',(0.0165,-0.00661301657664984,-0.0108033380723961));
#12107=CARTESIAN_POINT('',(0.0165,-0.00651474958971492,-0.0106680851681163));
#12108=CARTESIAN_POINT('',(-0.0005,-0.00666215006449997,-0.010870964517));
#12109=CARTESIAN_POINT('',(0.0165,-0.00680955061899998,-0.011073843975));
#12110=CARTESIAN_POINT('',(0.00550000000333333,-0.00680955061899998,-0.011073843975));
#12111=CARTESIAN_POINT('',(-0.00549999999333332,-0.00680955061899998,-0.011073843975));
#12112=CARTESIAN_POINT('',(-0.01649999999,-0.00680955061899998,-0.011073843975));
#12113=CARTESIAN_POINT('',(-0.016499999995,-0.00680955061882576,-0.0110738439747602));
#12114=CARTESIAN_POINT('',(-0.01649999999,-0.00680955061899998,-0.011073843975));
#12115=CARTESIAN_POINT('',(-0.0168333333266667,-0.00680955061899998,-0.011073843975));
#12116=CARTESIAN_POINT('',(-0.0171666666633333,-0.00680955061899998,-0.011073843975));
#12117=CARTESIAN_POINT('',(-0.0175,-0.00680955061899998,-0.011073843975));
#12118=CARTESIAN_POINT('',(-0.0175,-0.00680955061901203,-0.0110738439748256));
#12119=CARTESIAN_POINT('',(-0.0175,-0.00680955061899998,-0.011073843975));
#12120=CARTESIAN_POINT('',(-0.0175,-0.00671128358266665,-0.010938591003));
#12121=CARTESIAN_POINT('',(-0.0175,-0.00661301654633331,-0.010803338031));
#12122=CARTESIAN_POINT('',(-0.0175,-0.00651474950999998,-0.010668085059));
#12123=CARTESIAN_POINT('',(-0.0175,-0.0073793915595,-0.0135912960505));
#12124=CARTESIAN_POINT('',(-0.0175,-0.00995739469364337,-0.0143909794975352));
#12125=CARTESIAN_POINT('',(-0.0175,-0.00890811333544096,-0.0132852676565157));
#12126=CARTESIAN_POINT('',(-0.0175,-0.00785883197723854,-0.0121795558154963));
#12127=CARTESIAN_POINT('',(-0.0175,-0.00680955061903612,-0.0110738439744768));
#12128=CARTESIAN_POINT('',(-0.0174999997505,-0.00995739469140969,-0.0143909794996549));
#12129=CARTESIAN_POINT('',(-0.0175000000005,0.,0.));
#12130=CARTESIAN_POINT('',(-0.0174999998752501,-0.00578973720155703,-0.0165145068971582));
#12131=CARTESIAN_POINT('',(-0.0175,-0.00495637454030183,-0.0120180843498873));
#12132=CARTESIAN_POINT('',(-0.0175,-0.0052341620932975,-0.0135168918657844));
#12133=CARTESIAN_POINT('',(-0.0175,-0.00551194964629317,-0.0150156993816815));
#12134=CARTESIAN_POINT('',(-0.0175,-0.00578973719928885,-0.0165145068975786));
#12135=CARTESIAN_POINT('',(-0.0175,-0.00495637454020122,-0.0120180843495915));
#12136=CARTESIAN_POINT('',(-0.0175,-0.00480138846206486,-0.011541086246292));
#12137=CARTESIAN_POINT('',(-0.0175,-0.00485305048814385,-0.0117000856141571));
#12138=CARTESIAN_POINT('',(-0.0175,-0.00490471251422284,-0.0118590849820222));
#12139=CARTESIAN_POINT('',(-0.0175,-0.00495637454030183,-0.0120180843498873));
#12140=CARTESIAN_POINT('',(-0.0005,-0.004878881483,-0.011779585242));
#12141=CARTESIAN_POINT('',(-0.0175,-0.00495637454,-0.012018084349));
#12142=CARTESIAN_POINT('',(-0.0171666666633333,-0.00495637454,-0.012018084349));
#12143=CARTESIAN_POINT('',(-0.0168333333266667,-0.00495637454,-0.012018084349));
#12144=CARTESIAN_POINT('',(-0.01649999999,-0.00495637454,-0.012018084349));
#12145=CARTESIAN_POINT('',(-0.016499999995,-0.00495637453999843,-0.0120180843489915));
#12146=CARTESIAN_POINT('',(-0.01649999999,-0.00495637454,-0.012018084349));
#12147=CARTESIAN_POINT('',(-0.00549999999333334,-0.00495637454,-0.012018084349));
#12148=CARTESIAN_POINT('',(0.00550000000333334,-0.00495637454,-0.012018084349));
#12149=CARTESIAN_POINT('',(0.0165,-0.00495637454,-0.012018084349));
#12150=CARTESIAN_POINT('',(0.0165,-0.00495637446274314,-0.0120180841112278));
#12151=CARTESIAN_POINT('',(0.0165,-0.00495637446274314,-0.0120180841112278));
#12152=CARTESIAN_POINT('',(0.0165,-0.00490471245049542,-0.0118590847858185));
#12153=CARTESIAN_POINT('',(0.0165,-0.00485305043824771,-0.0117000854604093));
#12154=CARTESIAN_POINT('',(0.0165,-0.004801388426,-0.011541086135));
#12155=CARTESIAN_POINT('',(0.0165,-0.0039278249665,-0.0120886022365));
#12156=CARTESIAN_POINT('',(0.0165,0.,0.));
#12157=CARTESIAN_POINT('',(0.0165,-0.0030542614722702,-0.0126361182276936));
#12158=CARTESIAN_POINT('',(0.0165,-0.00305426147237052,-0.012636118227661));
#12159=CARTESIAN_POINT('',(0.0165,-0.0030025994599989,-0.0124771189028302));
#12160=CARTESIAN_POINT('',(0.0165,-0.00295093744762727,-0.0123181195779993));
#12161=CARTESIAN_POINT('',(0.0165,-0.00289927543525564,-0.0121591202531685));
#12162=CARTESIAN_POINT('',(-0.0005,-0.0029767684505,-0.012397619231));
#12163=CARTESIAN_POINT('',(0.0165,-0.003054261508,-0.012636118338));
#12164=CARTESIAN_POINT('',(0.00550000000333333,-0.003054261508,-0.012636118338));
#12165=CARTESIAN_POINT('',(-0.00549999999333333,-0.003054261508,-0.012636118338));
#12166=CARTESIAN_POINT('',(-0.01649999999,-0.003054261508,-0.012636118338));
#12167=CARTESIAN_POINT('',(-0.016499999995,-0.00305426150793331,-0.0126361183377947));
#12168=CARTESIAN_POINT('',(-0.01649999999,-0.003054261508,-0.012636118338));
#12169=CARTESIAN_POINT('',(-0.0168333333266667,-0.003054261508,-0.012636118338));
#12170=CARTESIAN_POINT('',(-0.0171666666633333,-0.003054261508,-0.012636118338));
#12171=CARTESIAN_POINT('',(-0.0175,-0.003054261508,-0.012636118338));
#12172=CARTESIAN_POINT('',(-0.0175,-0.003054261507645,-0.0126361183377328));
#12173=CARTESIAN_POINT('',(-0.0175,-0.003054261508,-0.012636118338));
#12174=CARTESIAN_POINT('',(-0.0175,-0.00300259946966667,-0.0124771189333333));
#12175=CARTESIAN_POINT('',(-0.0175,-0.00295093743133333,-0.0123181195286667));
#12176=CARTESIAN_POINT('',(-0.0175,-0.002899275393,-0.012159120124));
#12177=CARTESIAN_POINT('',(-0.0175,-0.002713045933,-0.0148272384280001));
#12178=CARTESIAN_POINT('',(-0.0175,-0.0050229878774073,-0.0167636390085154));
#12179=CARTESIAN_POINT('',(-0.0175,-0.00436674575391653,-0.0153877987847431));
#12180=CARTESIAN_POINT('',(-0.0175,-0.00371050363042576,-0.0140119585609708));
#12181=CARTESIAN_POINT('',(-0.0175,-0.00305426150693499,-0.0126361183371985));
#12182=CARTESIAN_POINT('',(-0.0174999997505,-0.00502298788151093,-0.016763639006558));
#12183=CARTESIAN_POINT('',(-0.0175000000005,0.,0.));
#12184=CARTESIAN_POINT('',(-0.0174999998752501,-0.000403104003887938,-0.0174953565862604));
#12185=CARTESIAN_POINT('',(-0.0175,-0.00100000000007961,-0.0129614813976545));
#12186=CARTESIAN_POINT('',(-0.0175,-0.00080103466949616,-0.0144727731273847));
#12187=CARTESIAN_POINT('',(-0.0175,-0.00060206933891271,-0.0159840648571149));
#12188=CARTESIAN_POINT('',(-0.0175,-0.00040310400832926,-0.0174953565868451));
#12189=CARTESIAN_POINT('',(-0.0175,-0.00100000000005307,-0.0129614813974363));
#12190=CARTESIAN_POINT('',(-0.0175,-0.00100000000007961,-0.0124599359095369));
#12191=CARTESIAN_POINT('',(-0.0175,-0.00100000000007961,-0.0126271177389094));
#12192=CARTESIAN_POINT('',(-0.0175,-0.00100000000007961,-0.0127942995682819));
#12193=CARTESIAN_POINT('',(-0.0175,-0.00100000000007961,-0.0129614813976545));
#12194=CARTESIAN_POINT('',(-0.0005,-0.001,-0.0127107085955));
#12195=CARTESIAN_POINT('',(-0.0175,-0.001,-0.012961481397));
#12196=CARTESIAN_POINT('',(-0.0171666666633333,-0.001,-0.012961481397));
#12197=CARTESIAN_POINT('',(-0.0168333333266667,-0.001,-0.012961481397));
#12198=CARTESIAN_POINT('',(-0.01649999999,-0.001,-0.012961481397));
#12199=CARTESIAN_POINT('',(-0.016499999995,-0.00100000000001226,-0.0129614813969069));
#12200=CARTESIAN_POINT('',(-0.01649999999,-0.001,-0.012961481397));
#12201=CARTESIAN_POINT('',(-0.00549999999333333,-0.001,-0.012961481397));
#12202=CARTESIAN_POINT('',(0.00550000000333333,-0.001,-0.012961481397));
#12203=CARTESIAN_POINT('',(0.0165,-0.001,-0.012961481397));
#12204=CARTESIAN_POINT('',(0.0165,-0.001,-0.0129614811469079));
#12205=CARTESIAN_POINT('',(0.0165,-0.001,-0.0129614811469079));
#12206=CARTESIAN_POINT('',(0.0165,-0.001,-0.0127942993626052));
#12207=CARTESIAN_POINT('',(0.0165,-0.001,-0.0126271175783026));
#12208=CARTESIAN_POINT('',(0.0165,-0.001,-0.012459935794));
#12209=CARTESIAN_POINT('',(0.0165,-1.73472347597681E-19,-0.0127315880896832));
#12210=CARTESIAN_POINT('',(0.0165,0.,0.));
#12211=CARTESIAN_POINT('',(0.0165,0.001,-0.0129614812809713));
#12212=CARTESIAN_POINT('',(0.0165,0.001,-0.0129614812809713));
#12213=CARTESIAN_POINT('',(0.0165,0.001,-0.012794299497191));
#12214=CARTESIAN_POINT('',(0.0165,0.001,-0.0126271177134107));
#12215=CARTESIAN_POINT('',(0.0165,0.001,-0.0124599359296304));
#12216=CARTESIAN_POINT('',(-0.0005,0.001,-0.0127107085955));
#12217=CARTESIAN_POINT('',(0.0165,0.001,-0.012961481397));
#12218=CARTESIAN_POINT('',(0.00550000000333333,0.001,-0.012961481397));
#12219=CARTESIAN_POINT('',(-0.00549999999333333,0.001,-0.012961481397));
#12220=CARTESIAN_POINT('',(-0.01649999999,0.001,-0.012961481397));
#12221=CARTESIAN_POINT('',(-0.016499999995,0.001,-0.0129614813969079));
#12222=CARTESIAN_POINT('',(-0.01649999999,0.001,-0.012961481397));
#12223=CARTESIAN_POINT('',(-0.0168333333266667,0.001,-0.012961481397));
#12224=CARTESIAN_POINT('',(-0.0171666666633333,0.001,-0.012961481397));
#12225=CARTESIAN_POINT('',(-0.0175,0.001,-0.012961481397));
#12226=CARTESIAN_POINT('',(-0.0175,0.00100000000002654,-0.0129614813972181));
#12227=CARTESIAN_POINT('',(-0.0175,0.001,-0.012961481397));
#12228=CARTESIAN_POINT('',(-0.0175,0.001,-0.0127942995293333));
#12229=CARTESIAN_POINT('',(-0.0175,0.001,-0.0126271176616667));
#12230=CARTESIAN_POINT('',(-0.0175,0.001,-0.012459935794));
#12231=CARTESIAN_POINT('',(-0.0175,0.002713045933,-0.0148272384280001));
#12232=CARTESIAN_POINT('',(-0.0175,0.000403103989373926,-0.0174953567308252));
#12233=CARTESIAN_POINT('',(-0.0175,0.00060206932627582,-0.0159840649531016));
#12234=CARTESIAN_POINT('',(-0.0175,0.000801034663177715,-0.014472773175378));
#12235=CARTESIAN_POINT('',(-0.0175,0.00100000000007961,-0.0129614813976545));
#12236=CARTESIAN_POINT('',(-0.0174999997505,0.000403103995825536,-0.0174953567316746));
#12237=CARTESIAN_POINT('',(-0.0175000000005,0.,0.));
#12238=CARTESIAN_POINT('',(-0.0174999998752501,0.00502298781526529,-0.0167636388750728));
#12239=CARTESIAN_POINT('',(-0.0175,0.00305426150693498,-0.0126361183371985));
#12240=CARTESIAN_POINT('',(-0.0175,0.00371050360930258,-0.0140119585166852));
#12241=CARTESIAN_POINT('',(-0.0175,0.00436674571167017,-0.0153877986961718));
#12242=CARTESIAN_POINT('',(-0.0175,0.00502298781403776,-0.0167636388756584));
#12243=CARTESIAN_POINT('',(-0.0175,0.00305426150728999,-0.0126361183374657));
#12244=CARTESIAN_POINT('',(-0.0175,0.00289927542909687,-0.0121591202348228));
#12245=CARTESIAN_POINT('',(-0.0175,0.00295093745504291,-0.0123181196022814));
#12246=CARTESIAN_POINT('',(-0.0175,0.00300259948098895,-0.01247711896974));
#12247=CARTESIAN_POINT('',(-0.0175,0.00305426150693498,-0.0126361183371985));
#12248=CARTESIAN_POINT('',(-0.0005,0.0029767684505,-0.012397619231));
#12249=CARTESIAN_POINT('',(-0.0175,0.003054261508,-0.012636118338));
#12250=CARTESIAN_POINT('',(-0.0171666666633333,0.003054261508,-0.012636118338));
#12251=CARTESIAN_POINT('',(-0.0168333333266667,0.003054261508,-0.012636118338));
#12252=CARTESIAN_POINT('',(-0.01649999999,0.003054261508,-0.012636118338));
#12253=CARTESIAN_POINT('',(-0.016499999995,0.00305426150790531,-0.0126361183378015));
#12254=CARTESIAN_POINT('',(-0.01649999999,0.003054261508,-0.012636118338));
#12255=CARTESIAN_POINT('',(-0.00549999999333333,0.003054261508,-0.012636118338));
#12256=CARTESIAN_POINT('',(0.00550000000333333,0.003054261508,-0.012636118338));
#12257=CARTESIAN_POINT('',(0.0165,0.003054261508,-0.012636118338));
#12258=CARTESIAN_POINT('',(0.0165,0.00305426143067905,-0.0126361181000306));
#12259=CARTESIAN_POINT('',(0.0165,0.00305426143067905,-0.0126361181000306));
#12260=CARTESIAN_POINT('',(0.0165,0.00300259941811937,-0.0124771187746871));
#12261=CARTESIAN_POINT('',(0.0165,0.00295093740555969,-0.0123181194493435));
#12262=CARTESIAN_POINT('',(0.0165,0.002899275393,-0.012159120124));
#12263=CARTESIAN_POINT('',(0.0165,0.0039278249665,-0.0120886022365));
#12264=CARTESIAN_POINT('',(0.0165,0.,0.));
#12265=CARTESIAN_POINT('',(0.0165,0.00495637450404248,-0.0120180842387746));
#12266=CARTESIAN_POINT('',(0.0165,0.00495637450391302,-0.0120180842388167));
#12267=CARTESIAN_POINT('',(0.0165,0.00490471249154851,-0.0118590849140078));
#12268=CARTESIAN_POINT('',(0.0165,0.00485305047918401,-0.0117000855891988));
#12269=CARTESIAN_POINT('',(0.0165,0.0048013884668195,-0.0115410862643899));
#12270=CARTESIAN_POINT('',(-0.0005,0.004878881483,-0.011779585242));
#12271=CARTESIAN_POINT('',(0.0165,0.00495637454,-0.012018084349));
#12272=CARTESIAN_POINT('',(0.00550000000333333,0.00495637454,-0.012018084349));
#12273=CARTESIAN_POINT('',(-0.00549999999333332,0.00495637454,-0.012018084349));
#12274=CARTESIAN_POINT('',(-0.01649999999,0.00495637454,-0.012018084349));
#12275=CARTESIAN_POINT('',(-0.016499999995,0.00495637453999739,-0.0120180843489919));
#12276=CARTESIAN_POINT('',(-0.01649999999,0.00495637454,-0.012018084349));
#12277=CARTESIAN_POINT('',(-0.0168333333266667,0.00495637454,-0.012018084349));
#12278=CARTESIAN_POINT('',(-0.0171666666633333,0.00495637454,-0.012018084349));
#12279=CARTESIAN_POINT('',(-0.0175,0.00495637454,-0.012018084349));
#12280=CARTESIAN_POINT('',(-0.0175,0.00495637454010061,-0.0120180843492958));
#12281=CARTESIAN_POINT('',(-0.0175,0.00495637454,-0.012018084349));
#12282=CARTESIAN_POINT('',(-0.0175,0.004904712502,-0.0118590849443333));
#12283=CARTESIAN_POINT('',(-0.0175,0.004853050464,-0.0117000855396667));
#12284=CARTESIAN_POINT('',(-0.0175,0.004801388426,-0.011541086135));
#12285=CARTESIAN_POINT('',(-0.0175,0.0073793915595,-0.0135912960505));
#12286=CARTESIAN_POINT('',(-0.0175,0.00578973722604522,-0.0165145070419431));
#12287=CARTESIAN_POINT('',(-0.0175,0.00551194966413076,-0.0150156994779245));
#12288=CARTESIAN_POINT('',(-0.0175,0.00523416210221629,-0.0135168919139059));
#12289=CARTESIAN_POINT('',(-0.0175,0.00495637454030183,-0.0120180843498873));
#12290=CARTESIAN_POINT('',(-0.0174999997505,0.00578973722878568,-0.0165145070414352));
#12291=CARTESIAN_POINT('',(-0.0175000000005,0.,0.));
#12292=CARTESIAN_POINT('',(-0.0174999998752501,0.00995739459048621,-0.0143909793923937));
#12293=CARTESIAN_POINT('',(-0.0175,0.00680955061903612,-0.0110738439744768));
#12294=CARTESIAN_POINT('',(-0.0175,0.00785883194344592,-0.0121795557798863));
#12295=CARTESIAN_POINT('',(-0.0175,0.00890811326785571,-0.0132852675852957));
#12296=CARTESIAN_POINT('',(-0.0175,0.00995739459226551,-0.0143909793907052));
#12297=CARTESIAN_POINT('',(-0.0175,0.00680955061902408,-0.0110738439746512));
#12298=CARTESIAN_POINT('',(-0.0175,0.0065147495766586,-0.0106680851532603));
#12299=CARTESIAN_POINT('',(-0.0175,0.00661301659078444,-0.0108033380936658));
#12300=CARTESIAN_POINT('',(-0.0175,0.00671128360491028,-0.0109385910340713));
#12301=CARTESIAN_POINT('',(-0.0175,0.00680955061903612,-0.0110738439744768));
#12302=CARTESIAN_POINT('',(-0.0005,0.00666215006449998,-0.010870964517));
#12303=CARTESIAN_POINT('',(-0.0175,0.00680955061899999,-0.011073843975));
#12304=CARTESIAN_POINT('',(-0.0171666666633333,0.00680955061899999,-0.011073843975));
#12305=CARTESIAN_POINT('',(-0.0168333333266667,0.00680955061899999,-0.011073843975));
#12306=CARTESIAN_POINT('',(-0.01649999999,0.00680955061899999,-0.011073843975));
#12307=CARTESIAN_POINT('',(-0.016499999995,0.00680955061879209,-0.0110738439747809));
#12308=CARTESIAN_POINT('',(-0.01649999999,0.00680955061899999,-0.011073843975));
#12309=CARTESIAN_POINT('',(-0.00549999999333334,0.00680955061899999,-0.011073843975));
#12310=CARTESIAN_POINT('',(0.00550000000333334,0.00680955061899999,-0.011073843975));
#12311=CARTESIAN_POINT('',(0.0165,0.00680955061899999,-0.011073843975));
#12312=CARTESIAN_POINT('',(0.0165,0.00680955047187945,-0.011073843772506));
#12313=CARTESIAN_POINT('',(0.0165,0.00680955047187945,-0.011073843772506));
#12314=CARTESIAN_POINT('',(0.0165,0.0067112834845863,-0.010938590868004));
#12315=CARTESIAN_POINT('',(0.0165,0.00661301649729314,-0.010803337963502));
#12316=CARTESIAN_POINT('',(0.0165,0.00651474950999999,-0.010668085059));
#12317=CARTESIAN_POINT('',(0.0165,0.0074711670585,-0.0102831792645));
#12318=CARTESIAN_POINT('',(0.0165,0.,0.));
#12319=CARTESIAN_POINT('',(0.0165,0.00842758453894735,-0.00989827337663452));
#12320=CARTESIAN_POINT('',(0.0165,0.00842758453880426,-0.00989827337673848));
#12321=CARTESIAN_POINT('',(0.0165,0.00832931755198811,-0.00976302047262217));
#12322=CARTESIAN_POINT('',(0.0165,0.00823105056517196,-0.00962776756850585));
#12323=CARTESIAN_POINT('',(0.0165,0.00813278357835582,-0.00949251466438954));
#12324=CARTESIAN_POINT('',(-0.0005,0.00828018405299999,-0.00969539401200001));
#12325=CARTESIAN_POINT('',(0.0165,0.00842758460699999,-0.00989827347000001));
#12326=CARTESIAN_POINT('',(0.00550000000333334,0.00842758460699999,-0.00989827347000001));
#12327=CARTESIAN_POINT('',(-0.00549999999333334,0.00842758460699999,-0.00989827347000001));
#12328=CARTESIAN_POINT('',(-0.01649999999,0.00842758460699999,-0.00989827347000001));
#12329=CARTESIAN_POINT('',(-0.016499999995,0.00842758460705612,-0.00989827347007726));
#12330=CARTESIAN_POINT('',(-0.01649999999,0.00842758460699999,-0.00989827347000001));
#12331=CARTESIAN_POINT('',(-0.0168333333266667,0.00842758460699999,-0.00989827347000001));
#12332=CARTESIAN_POINT('',(-0.0171666666633333,0.00842758460699999,-0.00989827347000001));
#12333=CARTESIAN_POINT('',(-0.0175,0.00842758460699999,-0.00989827347000001));
#12334=CARTESIAN_POINT('',(-0.0175,0.00842758460672372,-0.0098982734697996));
#12335=CARTESIAN_POINT('',(-0.0175,0.00842758460699999,-0.00989827347000001));
#12336=CARTESIAN_POINT('',(-0.0175,0.00832931757099999,-0.00976302049800001));
#12337=CARTESIAN_POINT('',(-0.0175,0.00823105053499999,-0.00962776752600001));
#12338=CARTESIAN_POINT('',(-0.0175,0.00813278349899999,-0.00949251455400001));
#12339=CARTESIAN_POINT('',(-0.0175,0.011024942919,-0.011024942919));
#12340=CARTESIAN_POINT('',(-0.0175,0.0106096306507946,-0.0139171023384044));
#12341=CARTESIAN_POINT('',(-0.0175,0.00988228196925343,-0.0125774927154025));
#12342=CARTESIAN_POINT('',(-0.0175,0.0091549332877123,-0.0112378830924007));
#12343=CARTESIAN_POINT('',(-0.0175,0.00842758460617116,-0.00989827346939879));
#12344=CARTESIAN_POINT('',(-0.0174999997505,0.0106096306436055,-0.0139171023423077));
#12345=CARTESIAN_POINT('',(-0.0175000000005,0.,0.));
#12346=CARTESIAN_POINT('',(-0.0174999998752501,0.0139171022121162,-0.0106096305765927));
#12347=CARTESIAN_POINT('',(-0.0175,0.00989827346939877,-0.00842758460617117));
#12348=CARTESIAN_POINT('',(-0.0175,0.0112378830495172,-0.00915493326442851));
#12349=CARTESIAN_POINT('',(-0.0175,0.0125774926296357,-0.00988228192268585));
#12350=CARTESIAN_POINT('',(-0.0175,0.0139171022097541,-0.0106096305809432));
#12351=CARTESIAN_POINT('',(-0.0175,0.00989827346959919,-0.00842758460644744));
#12352=CARTESIAN_POINT('',(-0.0175,0.00949251464684353,-0.00813278356824452));
#12353=CARTESIAN_POINT('',(-0.0175,0.00962776758769528,-0.00823105058088674));
#12354=CARTESIAN_POINT('',(-0.0175,0.00976302052854702,-0.00832931759352895));
#12355=CARTESIAN_POINT('',(-0.0175,0.00989827346939877,-0.00842758460617117));
#12356=CARTESIAN_POINT('',(-0.0005,0.009695394012,-0.00828018405299999));
#12357=CARTESIAN_POINT('',(-0.0175,0.00989827347000001,-0.00842758460699999));
#12358=CARTESIAN_POINT('',(-0.0171666666633333,0.00989827347000001,-0.00842758460699999));
#12359=CARTESIAN_POINT('',(-0.0168333333266667,0.00989827347000001,-0.00842758460699999));
#12360=CARTESIAN_POINT('',(-0.01649999999,0.00989827347000001,-0.00842758460699999));
#12361=CARTESIAN_POINT('',(-0.016499999995,0.00989827347008551,-0.00842758460704643));
#12362=CARTESIAN_POINT('',(-0.01649999999,0.00989827347000001,-0.00842758460699999));
#12363=CARTESIAN_POINT('',(-0.00549999999333333,0.00989827347000001,-0.00842758460699999));
#12364=CARTESIAN_POINT('',(0.00550000000333333,0.00989827347000001,-0.00842758460699999));
#12365=CARTESIAN_POINT('',(0.0165,0.00989827347000001,-0.00842758460699999));
#12366=CARTESIAN_POINT('',(0.0165,0.00989827326782301,-0.00842758446010981));
#12367=CARTESIAN_POINT('',(0.0165,0.00989827326782301,-0.00842758446010981));
#12368=CARTESIAN_POINT('',(0.0165,0.00976302036321534,-0.0083293174730732));
#12369=CARTESIAN_POINT('',(0.0165,0.00962776745860767,-0.0082310504860366));
#12370=CARTESIAN_POINT('',(0.0165,0.009492514554,-0.00813278349899999));
#12371=CARTESIAN_POINT('',(0.0165,0.0102831792645,-0.0074711670585));
#12372=CARTESIAN_POINT('',(0.0165,0.,0.));
#12373=CARTESIAN_POINT('',(0.0165,0.0110738438809193,-0.0068095505505698));
#12374=CARTESIAN_POINT('',(0.0165,0.0110738438809557,-0.00680955055051969));
#12375=CARTESIAN_POINT('',(0.0165,0.0109385909766482,-0.00671128356356468));
#12376=CARTESIAN_POINT('',(0.0165,0.0108033380723408,-0.00661301657660966));
#12377=CARTESIAN_POINT('',(0.0165,0.0106680851680333,-0.00651474958965464));
#12378=CARTESIAN_POINT('',(-0.0005,0.010870964517,-0.00666215006449997));
#12379=CARTESIAN_POINT('',(0.0165,0.011073843975,-0.00680955061899998));
#12380=CARTESIAN_POINT('',(0.00550000000333333,0.011073843975,-0.00680955061899998));
#12381=CARTESIAN_POINT('',(-0.00549999999333332,0.011073843975,-0.00680955061899998));
#12382=CARTESIAN_POINT('',(-0.01649999999,0.011073843975,-0.00680955061899998));
#12383=CARTESIAN_POINT('',(-0.016499999995,0.0110738439747602,-0.00680955061882576));
#12384=CARTESIAN_POINT('',(-0.01649999999,0.011073843975,-0.00680955061899998));
#12385=CARTESIAN_POINT('',(-0.0168333333266667,0.011073843975,-0.00680955061899998));
#12386=CARTESIAN_POINT('',(-0.0171666666633333,0.011073843975,-0.00680955061899998));
#12387=CARTESIAN_POINT('',(-0.0175,0.011073843975,-0.00680955061899998));
#12388=CARTESIAN_POINT('',(-0.0175,0.0110738439748256,-0.00680955061901203));
#12389=CARTESIAN_POINT('',(-0.0175,0.011073843975,-0.00680955061899998));
#12390=CARTESIAN_POINT('',(-0.0175,0.010938591003,-0.00671128358266665));
#12391=CARTESIAN_POINT('',(-0.0175,0.010803338031,-0.00661301654633331));
#12392=CARTESIAN_POINT('',(-0.0175,0.010668085059,-0.00651474950999998));
#12393=CARTESIAN_POINT('',(-0.0175,0.0135912960505,-0.0073793915595));
#12394=CARTESIAN_POINT('',(-0.0175,0.014390979497136,-0.00995739469326454));
#12395=CARTESIAN_POINT('',(-0.0175,0.0132852676562496,-0.0089081133351884));
#12396=CARTESIAN_POINT('',(-0.0175,0.0121795558153632,-0.00785883197711226));
#12397=CARTESIAN_POINT('',(-0.0175,0.0110738439744768,-0.00680955061903612));
#12398=CARTESIAN_POINT('',(-0.0174999997505,0.0143909795016971,-0.00995739468845805));
#12399=CARTESIAN_POINT('',(-0.0175000000005,0.,0.));
#12400=CARTESIAN_POINT('',(-0.0174999998752501,0.0165145068977519,-0.00578973719986344));
#12401=CARTESIAN_POINT('',(-0.0175,0.0120180843498873,-0.00495637454030183));
#12402=CARTESIAN_POINT('',(-0.0175,0.0135168918658746,-0.00523416209331421));
#12403=CARTESIAN_POINT('',(-0.0175,0.0150156993818619,-0.0055119496463266));
#12404=CARTESIAN_POINT('',(-0.0175,0.0165145068978492,-0.00578973719933899));
#12405=CARTESIAN_POINT('',(-0.0175,0.0120180843495915,-0.00495637454020122));
#12406=CARTESIAN_POINT('',(-0.0175,0.0115410862463895,-0.00480138846209655));
#12407=CARTESIAN_POINT('',(-0.0175,0.0117000856142221,-0.00485305048816498));
#12408=CARTESIAN_POINT('',(-0.0175,0.0118590849820547,-0.0049047125142334));
#12409=CARTESIAN_POINT('',(-0.0175,0.0120180843498873,-0.00495637454030183));
#12410=CARTESIAN_POINT('',(-0.0005,0.011779585242,-0.004878881483));
#12411=CARTESIAN_POINT('',(-0.0175,0.012018084349,-0.00495637454));
#12412=CARTESIAN_POINT('',(-0.0171666666633333,0.012018084349,-0.00495637454));
#12413=CARTESIAN_POINT('',(-0.0168333333266667,0.012018084349,-0.00495637454));
#12414=CARTESIAN_POINT('',(-0.01649999999,0.012018084349,-0.00495637454));
#12415=CARTESIAN_POINT('',(-0.016499999995,0.0120180843489915,-0.00495637453999843));
#12416=CARTESIAN_POINT('',(-0.01649999999,0.012018084349,-0.00495637454));
#12417=CARTESIAN_POINT('',(-0.00549999999333334,0.012018084349,-0.00495637454));
#12418=CARTESIAN_POINT('',(0.00550000000333334,0.012018084349,-0.00495637454));
#12419=CARTESIAN_POINT('',(0.0165,0.012018084349,-0.00495637454));
#12420=CARTESIAN_POINT('',(0.0165,0.0120180841112278,-0.00495637446274314));
#12421=CARTESIAN_POINT('',(0.0165,0.0120180841112278,-0.00495637446274314));
#12422=CARTESIAN_POINT('',(0.0165,0.0118590847858185,-0.00490471245049542));
#12423=CARTESIAN_POINT('',(0.0165,0.0117000854604093,-0.00485305043824771));
#12424=CARTESIAN_POINT('',(0.0165,0.011541086135,-0.004801388426));
#12425=CARTESIAN_POINT('',(0.0165,0.0120886022365,-0.00392782496650001));
#12426=CARTESIAN_POINT('',(0.0165,0.,0.));
#12427=CARTESIAN_POINT('',(0.0165,0.0126361182276936,-0.0030542614722702));
#12428=CARTESIAN_POINT('',(0.0165,0.012636118227661,-0.00305426147237052));
#12429=CARTESIAN_POINT('',(0.0165,0.0124771189027977,-0.00300259945998833));
#12430=CARTESIAN_POINT('',(0.0165,0.0123181195779343,-0.00295093744760614));
#12431=CARTESIAN_POINT('',(0.0165,0.0121591202530709,-0.00289927543522395));
#12432=CARTESIAN_POINT('',(-0.0005,0.012397619231,-0.0029767684505));
#12433=CARTESIAN_POINT('',(0.0165,0.012636118338,-0.003054261508));
#12434=CARTESIAN_POINT('',(0.00550000000333333,0.012636118338,-0.003054261508));
#12435=CARTESIAN_POINT('',(-0.00549999999333333,0.012636118338,-0.003054261508));
#12436=CARTESIAN_POINT('',(-0.01649999999,0.012636118338,-0.003054261508));
#12437=CARTESIAN_POINT('',(-0.016499999995,0.0126361183377947,-0.00305426150793331));
#12438=CARTESIAN_POINT('',(-0.01649999999,0.012636118338,-0.003054261508));
#12439=CARTESIAN_POINT('',(-0.0168333333266667,0.012636118338,-0.003054261508));
#12440=CARTESIAN_POINT('',(-0.0171666666633333,0.012636118338,-0.003054261508));
#12441=CARTESIAN_POINT('',(-0.0175,0.012636118338,-0.003054261508));
#12442=CARTESIAN_POINT('',(-0.0175,0.0126361183377328,-0.003054261507645));
#12443=CARTESIAN_POINT('',(-0.0175,0.012636118338,-0.003054261508));
#12444=CARTESIAN_POINT('',(-0.0175,0.0124771189333333,-0.00300259946966667));
#12445=CARTESIAN_POINT('',(-0.0175,0.0123181195286667,-0.00295093743133333));
#12446=CARTESIAN_POINT('',(-0.0175,0.012159120124,-0.002899275393));
#12447=CARTESIAN_POINT('',(-0.0175,0.014827238428,-0.002713045933));
#12448=CARTESIAN_POINT('',(-0.0175,0.0167636390080186,-0.00502298787717037));
#12449=CARTESIAN_POINT('',(-0.0175,0.0153877987844119,-0.00436674575375858));
#12450=CARTESIAN_POINT('',(-0.0175,0.0140119585608052,-0.00371050363034678));
#12451=CARTESIAN_POINT('',(-0.0175,0.0126361183371985,-0.00305426150693499));
#12452=CARTESIAN_POINT('',(-0.0174999997505,0.0167636390075883,-0.00502298787807265));
#12453=CARTESIAN_POINT('',(-0.0175000000005,0.,0.));
#12454=CARTESIAN_POINT('',(-0.0174999998752501,0.0174953565861002,-0.000403104010841439));
#12455=CARTESIAN_POINT('',(-0.0175,0.0129614813976545,-0.00100000000007961));
#12456=CARTESIAN_POINT('',(-0.0175,0.0144727731270322,-0.000801034669542563));
#12457=CARTESIAN_POINT('',(-0.0175,0.01598406485641,-0.000602069339005512));
#12458=CARTESIAN_POINT('',(-0.0175,0.0174953565857878,-0.000403104008468461));
#12459=CARTESIAN_POINT('',(-0.0175,0.0129614813974363,-0.00100000000005307));
#12460=CARTESIAN_POINT('',(-0.0175,0.0124599359091394,-0.00100000000007962));
#12461=CARTESIAN_POINT('',(-0.0175,0.0126271177386444,-0.00100000000007962));
#12462=CARTESIAN_POINT('',(-0.0175,0.0127942995681494,-0.00100000000007962));
#12463=CARTESIAN_POINT('',(-0.0175,0.0129614813976545,-0.00100000000007962));
#12464=CARTESIAN_POINT('',(-0.0005,0.0127107085955,-0.001));
#12465=CARTESIAN_POINT('',(-0.0175,0.012961481397,-0.001));
#12466=CARTESIAN_POINT('',(-0.0171666666633333,0.012961481397,-0.001));
#12467=CARTESIAN_POINT('',(-0.0168333333266667,0.012961481397,-0.001));
#12468=CARTESIAN_POINT('',(-0.01649999999,0.012961481397,-0.001));
#12469=CARTESIAN_POINT('',(-0.016499999995,0.0129614813969069,-0.00100000000001226));
#12470=CARTESIAN_POINT('',(-0.01649999999,0.012961481397,-0.001));
#12471=CARTESIAN_POINT('',(-0.005500000035,0.012961481397,-0.001));
#12472=CARTESIAN_POINT('',(0.00549999992,0.012961481397,-0.001));
#12473=CARTESIAN_POINT('',(0.016499999875,0.012961481397,-0.001));
#12474=CARTESIAN_POINT('',(-0.0215,0.,-3.07046055247895E-18));
#12475=CARTESIAN_POINT('',(-0.0215,0.,0.));
#12476=CARTESIAN_POINT('',(-0.0215,0.,0.0175));
#12477=CARTESIAN_POINT('',(-0.019981842228,0.,0.));
#12478=CARTESIAN_POINT('',(-0.0165,0.,0.));
#12479=CARTESIAN_POINT('',(-0.017,0.0152284190645,0.000701551994));
#12480=CARTESIAN_POINT('',(-0.0174999998755,0.017495356732,0.000403103988));
#12481=CARTESIAN_POINT('',(-0.017166666667,0.017495356732,0.000403103988));
#12482=CARTESIAN_POINT('',(-0.0168333334585,0.017495356732,0.000403103988));
#12483=CARTESIAN_POINT('',(-0.01650000025,0.017495356732,0.000403103988));
#12484=CARTESIAN_POINT('',(-0.01650000025,0.0174953567319272,0.000403103988009585));
#12485=CARTESIAN_POINT('',(-0.0165,0.0174953567319272,0.000403103988009584));
#12486=CARTESIAN_POINT('',(-0.0165,0.0159840649536181,0.000602069325339723));
#12487=CARTESIAN_POINT('',(-0.0165,0.0144727731753091,0.000801034662669862));
#12488=CARTESIAN_POINT('',(-0.0165,0.012961481397,0.001));
#12489=CARTESIAN_POINT('',(-0.017,0.014699878673,0.004038624693));
#12490=CARTESIAN_POINT('',(-0.0165,0.016763639008,0.005022987878));
#12491=CARTESIAN_POINT('',(-0.0168333333333333,0.016763639008,0.005022987878));
#12492=CARTESIAN_POINT('',(-0.0171666666666667,0.016763639008,0.005022987878));
#12493=CARTESIAN_POINT('',(-0.0175,0.016763639008,0.005022987878));
#12494=CARTESIAN_POINT('',(-0.0165,0.0167636387823537,0.00502298777037222));
#12495=CARTESIAN_POINT('',(-0.0165,0.012636118338,0.003054261508));
#12496=CARTESIAN_POINT('',(-0.0165,0.0140119584861179,0.00371050359545741));
#12497=CARTESIAN_POINT('',(-0.0165,0.0153877986342358,0.00436674568291482));
#12498=CARTESIAN_POINT('',(-0.0165,0.0167636387823537,0.00502298777037223));
#12499=CARTESIAN_POINT('',(-0.034017463007,0.,0.));
#12500=CARTESIAN_POINT('',(-0.0174999998755,-0.017495356732,-0.000403103988));
#12501=CARTESIAN_POINT('',(-0.017166666667,-0.017495356732,-0.000403103988));
#12502=CARTESIAN_POINT('',(-0.0168333334585,-0.017495356732,-0.000403103988));
#12503=CARTESIAN_POINT('',(-0.01650000025,-0.017495356732,-0.000403103988));
#12504=CARTESIAN_POINT('',(-0.01650000025,-0.0174953567319272,-0.000403103988009585));
#12505=CARTESIAN_POINT('',(-0.0165,0.,0.));
#12506=CARTESIAN_POINT('',(-0.016500000125,-0.01749535673194,0.000403103987454157));
#12507=CARTESIAN_POINT('',(-0.0174999997505,-0.01749535673188,0.000403103986908313));
#12508=CARTESIAN_POINT('',(-0.0171666665836667,-0.01749535673188,0.000403103986908313));
#12509=CARTESIAN_POINT('',(-0.0168333334168333,-0.01749535673188,0.000403103986908313));
#12510=CARTESIAN_POINT('',(-0.01650000025,-0.01749535673188,0.000403103986908313));
#12511=CARTESIAN_POINT('',(-0.01650000025,-0.0167636390090209,0.00502298787329154));
#12512=CARTESIAN_POINT('',(-0.0168333334168333,-0.0167636390090209,0.00502298787329154));
#12513=CARTESIAN_POINT('',(-0.0171666665836667,-0.0167636390090209,0.00502298787329154));
#12514=CARTESIAN_POINT('',(-0.0174999997505,-0.0167636390090209,0.00502298787329154));
#12515=CARTESIAN_POINT('',(-0.0165,-0.0167636390078825,0.00502298787774123));
#12516=CARTESIAN_POINT('',(-0.0165,0.,0.));
#12517=CARTESIAN_POINT('',(-0.016500000125,-0.0165145070431931,0.0057897372241842));
#12518=CARTESIAN_POINT('',(-0.0174999997505,-0.0165145070443862,0.00578973722036841));
#12519=CARTESIAN_POINT('',(-0.0171666665836667,-0.0165145070443862,0.00578973722036841));
#12520=CARTESIAN_POINT('',(-0.0168333334168333,-0.0165145070443862,0.00578973722036841));
#12521=CARTESIAN_POINT('',(-0.01650000025,-0.0165145070443862,0.00578973722036841));
#12522=CARTESIAN_POINT('',(-0.01650000025,-0.0143909794945797,0.00995739469874462));
#12523=CARTESIAN_POINT('',(-0.0168333334168333,-0.0143909794945797,0.00995739469874462));
#12524=CARTESIAN_POINT('',(-0.0171666665836667,-0.0143909794945797,0.00995739469874462));
#12525=CARTESIAN_POINT('',(-0.0174999997505,-0.0143909794945797,0.00995739469874462));
#12526=CARTESIAN_POINT('',(-0.0165,-0.0143909794950452,0.00995739469767118));
#12527=CARTESIAN_POINT('',(-0.0165,0.,0.));
#12528=CARTESIAN_POINT('',(-0.016500000125,-0.0139171023380528,0.0106096306492146));
#12529=CARTESIAN_POINT('',(-0.0174999997505,-0.0139171023371057,0.0106096306504292));
#12530=CARTESIAN_POINT('',(-0.0171666665836667,-0.0139171023371057,0.0106096306504292));
#12531=CARTESIAN_POINT('',(-0.0168333334168333,-0.0139171023371057,0.0106096306504292));
#12532=CARTESIAN_POINT('',(-0.01650000025,-0.0139171023371057,0.0106096306504292));
#12533=CARTESIAN_POINT('',(-0.01650000025,-0.0106096306475748,0.0139171023392818));
#12534=CARTESIAN_POINT('',(-0.0168333334168333,-0.0106096306475748,0.0139171023392818));
#12535=CARTESIAN_POINT('',(-0.0171666665836667,-0.0106096306475748,0.0139171023392818));
#12536=CARTESIAN_POINT('',(-0.0174999997505,-0.0106096306475748,0.0139171023392818));
#12537=CARTESIAN_POINT('',(-0.0165,-0.0106096306460396,0.0139171023404521));
#12538=CARTESIAN_POINT('',(-0.0165,0.,0.));
#12539=CARTESIAN_POINT('',(-0.016500000125,-0.00995739469439649,0.014390979497311));
#12540=CARTESIAN_POINT('',(-0.0174999997505,-0.00995739469579297,0.014390979496622));
#12541=CARTESIAN_POINT('',(-0.0171666665836667,-0.00995739469579297,0.014390979496622));
#12542=CARTESIAN_POINT('',(-0.0168333334168333,-0.00995739469579297,0.014390979496622));
#12543=CARTESIAN_POINT('',(-0.01650000025,-0.00995739469579297,0.014390979496622));
#12544=CARTESIAN_POINT('',(-0.01650000025,-0.00578973723349574,0.0165145070397839));
#12545=CARTESIAN_POINT('',(-0.0168333334168333,-0.00578973723349574,0.0165145070397839));
#12546=CARTESIAN_POINT('',(-0.0171666665836667,-0.00578973723349574,0.0165145070397839));
#12547=CARTESIAN_POINT('',(-0.0174999997505,-0.00578973723349574,0.0165145070397839));
#12548=CARTESIAN_POINT('',(-0.0165,-0.00578973722868356,0.0165145070416157));
#12549=CARTESIAN_POINT('',(-0.0165,0.,0.));
#12550=CARTESIAN_POINT('',(-0.016500000125,-0.00502298787392663,0.0167636390090256));
#12551=CARTESIAN_POINT('',(-0.0174999997505,-0.00502298786985327,0.0167636390100511));
#12552=CARTESIAN_POINT('',(-0.0171666665836667,-0.00502298786985327,0.0167636390100511));
#12553=CARTESIAN_POINT('',(-0.0168333334168333,-0.00502298786985327,0.0167636390100511));
#12554=CARTESIAN_POINT('',(-0.01650000025,-0.00502298786985327,0.0167636390100511));
#12555=CARTESIAN_POINT('',(-0.01650000025,-0.000403103983319961,0.0174953567319627));
#12556=CARTESIAN_POINT('',(-0.0168333334168333,-0.000403103983319961,0.0174953567319627));
#12557=CARTESIAN_POINT('',(-0.0171666665836667,-0.000403103983319961,0.0174953567319627));
#12558=CARTESIAN_POINT('',(-0.0174999997505,-0.000403103983319961,0.0174953567319627));
#12559=CARTESIAN_POINT('',(-0.0165,-0.000403103982389193,0.0174953567319841));
#12560=CARTESIAN_POINT('',(-0.0165,0.,0.));
#12561=CARTESIAN_POINT('',(-0.0165000001875,0.000403103989248338,0.0174953567318987));
#12562=CARTESIAN_POINT('',(-0.0174999997505,0.000403103990496676,0.0174953567317973));
#12563=CARTESIAN_POINT('',(-0.0171666665836667,0.000403103990496676,0.0174953567317973));
#12564=CARTESIAN_POINT('',(-0.0168333334168333,0.000403103990496676,0.0174953567317973));
#12565=CARTESIAN_POINT('',(-0.01650000025,0.000403103990496676,0.0174953567317973));
#12566=CARTESIAN_POINT('',(-0.01650000025,0.00502298787672982,0.0167636390079906));
#12567=CARTESIAN_POINT('',(-0.0168333334168333,0.00502298787672982,0.0167636390079906));
#12568=CARTESIAN_POINT('',(-0.0171666665836667,0.00502298787672982,0.0167636390079906));
#12569=CARTESIAN_POINT('',(-0.0174999997505,0.00502298787672982,0.0167636390079906));
#12570=CARTESIAN_POINT('',(-0.0165,0.005022987879379,0.0167636390071969));
#12571=CARTESIAN_POINT('',(-0.0165,0.,0.));
#12572=CARTESIAN_POINT('',(-0.016500000125,0.0057897372258778,0.0165145070425994));
#12573=CARTESIAN_POINT('',(-0.0174999997505,0.00578973722375559,0.0165145070431987));
#12574=CARTESIAN_POINT('',(-0.0171666665836667,0.00578973722375559,0.0165145070431987));
#12575=CARTESIAN_POINT('',(-0.0168333334168333,0.00578973722375559,0.0165145070431987));
#12576=CARTESIAN_POINT('',(-0.01650000025,0.00578973722375559,0.0165145070431987));
#12577=CARTESIAN_POINT('',(-0.01650000025,0.00995739468730528,0.0143909795024948));
#12578=CARTESIAN_POINT('',(-0.0168333334168333,0.00995739468730528,0.0143909795024948));
#12579=CARTESIAN_POINT('',(-0.0171666665836667,0.00995739468730528,0.0143909795024948));
#12580=CARTESIAN_POINT('',(-0.0174999997505,0.00995739468730528,0.0143909795024948));
#12581=CARTESIAN_POINT('',(-0.0165,0.00995739469211033,0.0143909794991701));
#12582=CARTESIAN_POINT('',(-0.0165,0.,0.));
#12583=CARTESIAN_POINT('',(-0.016500000125,0.0106096306506418,0.0139171023369648));
#12584=CARTESIAN_POINT('',(-0.0174999997505,0.0106096306532837,0.0139171023349296));
#12585=CARTESIAN_POINT('',(-0.0171666665836667,0.0106096306532837,0.0139171023349296));
#12586=CARTESIAN_POINT('',(-0.0168333334168333,0.0106096306532837,0.0139171023349296));
#12587=CARTESIAN_POINT('',(-0.01650000025,0.0106096306532837,0.0139171023349296));
#12588=CARTESIAN_POINT('',(-0.01650000025,0.0139171023414578,0.0106096306447203));
#12589=CARTESIAN_POINT('',(-0.0168333334168333,0.0139171023414578,0.0106096306447203));
#12590=CARTESIAN_POINT('',(-0.0171666665836667,0.0139171023414578,0.0106096306447203));
#12591=CARTESIAN_POINT('',(-0.0174999997505,0.0139171023414578,0.0106096306447203));
#12592=CARTESIAN_POINT('',(-0.0165,0.0139171023415401,0.0106096306446124));
#12593=CARTESIAN_POINT('',(-0.0165,0.,0.));
#12594=CARTESIAN_POINT('',(-0.016500000125,0.0143909794983321,0.00995739469292067));
#12595=CARTESIAN_POINT('',(-0.0174999997505,0.0143909794986643,0.00995739469284135));
#12596=CARTESIAN_POINT('',(-0.0171666665836667,0.0143909794986643,0.00995739469284135));
#12597=CARTESIAN_POINT('',(-0.0168333334168333,0.0143909794986643,0.00995739469284135));
#12598=CARTESIAN_POINT('',(-0.01650000025,0.0143909794986643,0.00995739469284135));
#12599=CARTESIAN_POINT('',(-0.01650000025,0.0165145070409714,0.00578973723010854));
#12600=CARTESIAN_POINT('',(-0.0168333334168333,0.0165145070409714,0.00578973723010854));
#12601=CARTESIAN_POINT('',(-0.0171666665836667,0.0165145070409714,0.00578973723010854));
#12602=CARTESIAN_POINT('',(-0.0174999997505,0.0165145070409714,0.00578973723010854));
#12603=CARTESIAN_POINT('',(-0.0165,0.0165145070420736,0.00578973722696479));
#12604=CARTESIAN_POINT('',(-0.0165,0.,0.));
#12605=CARTESIAN_POINT('',(-0.0165,0.,0.));
#12606=CARTESIAN_POINT('',(-0.016500000125,0.0174953567318573,-0.000403103991042516));
#12607=CARTESIAN_POINT('',(-0.0174999997505,0.0174953567317146,-0.000403103994085063));
#12608=CARTESIAN_POINT('',(-0.0171666665836667,0.0174953567317146,-0.000403103994085063));
#12609=CARTESIAN_POINT('',(-0.0168333334168333,0.0174953567317146,-0.000403103994085063));
#12610=CARTESIAN_POINT('',(-0.01650000025,0.0174953567317146,-0.000403103994085063));
#12611=CARTESIAN_POINT('',(-0.01650000025,0.0167636390069604,-0.00502298788016813));
#12612=CARTESIAN_POINT('',(-0.0168333334168333,0.0167636390069604,-0.00502298788016813));
#12613=CARTESIAN_POINT('',(-0.0171666665836667,0.0167636390069604,-0.00502298788016813));
#12614=CARTESIAN_POINT('',(-0.0174999997505,0.0167636390069604,-0.00502298788016813));
#12615=CARTESIAN_POINT('',(-0.0165,0.0167636390066817,-0.00502298788109814));
#12616=CARTESIAN_POINT('',(-0.0165,0.,0.));
#12617=CARTESIAN_POINT('',(-0.016500000125,0.0165145070420056,-0.00578973722757139));
#12618=CARTESIAN_POINT('',(-0.0174999997505,0.0165145070420112,-0.0057897372271428));
#12619=CARTESIAN_POINT('',(-0.0171666665836667,0.0165145070420112,-0.0057897372271428));
#12620=CARTESIAN_POINT('',(-0.0168333334168333,0.0165145070420112,-0.0057897372271428));
#12621=CARTESIAN_POINT('',(-0.01650000025,0.0165145070420112,-0.0057897372271428));
#12622=CARTESIAN_POINT('',(-0.01650000025,0.0143909795004525,-0.00995739469025694));
#12623=CARTESIAN_POINT('',(-0.0168333334168333,0.0143909795004525,-0.00995739469025694));
#12624=CARTESIAN_POINT('',(-0.0171666665836667,0.0143909795004525,-0.00995739469025694));
#12625=CARTESIAN_POINT('',(-0.0174999997505,0.0143909795004525,-0.00995739469025694));
#12626=CARTESIAN_POINT('',(-0.0165,0.0143909794979816,-0.00995739469342733));
#12627=CARTESIAN_POINT('',(-0.0165,0.,0.));
#12628=CARTESIAN_POINT('',(-0.016500000125,0.0139171023411816,-0.0106096306451105));
#12629=CARTESIAN_POINT('',(-0.0174999997505,0.0139171023433632,-0.010609630642221));
#12630=CARTESIAN_POINT('',(-0.0171666665836667,0.0139171023433632,-0.010609630642221));
#12631=CARTESIAN_POINT('',(-0.0168333334168333,0.0139171023433632,-0.010609630642221));
#12632=CARTESIAN_POINT('',(-0.01650000025,0.0139171023433632,-0.010609630642221));
#12633=CARTESIAN_POINT('',(-0.01650000025,0.0106096306418659,-0.0139171023436339));
#12634=CARTESIAN_POINT('',(-0.0168333334168333,0.0106096306418659,-0.0139171023436339));
#12635=CARTESIAN_POINT('',(-0.0171666665836667,0.0106096306418659,-0.0139171023436339));
#12636=CARTESIAN_POINT('',(-0.0174999997505,0.0106096306418659,-0.0139171023436339));
#12637=CARTESIAN_POINT('',(-0.0165,0.0106096306431852,-0.0139171023426282));
#12638=CARTESIAN_POINT('',(-0.0165,0.,0.));
#12639=CARTESIAN_POINT('',(-0.016500000125,0.00995739469144485,-0.0143909794993533));
#12640=CARTESIAN_POINT('',(-0.0174999997505,0.00995739468988968,-0.0143909795007066));
#12641=CARTESIAN_POINT('',(-0.0171666665836667,0.00995739468988968,-0.0143909795007066));
#12642=CARTESIAN_POINT('',(-0.0168333334168333,0.00995739468988968,-0.0143909795007066));
#12643=CARTESIAN_POINT('',(-0.01650000025,0.00995739468988968,-0.0143909795007066));
#12644=CARTESIAN_POINT('',(-0.01650000025,0.00578973722672135,-0.0165145070421589));
#12645=CARTESIAN_POINT('',(-0.0168333334168333,0.00578973722672135,-0.0165145070421589));
#12646=CARTESIAN_POINT('',(-0.0171666665836667,0.00578973722672135,-0.0165145070421589));
#12647=CARTESIAN_POINT('',(-0.0174999997505,0.00578973722672135,-0.0165145070421589));
#12648=CARTESIAN_POINT('',(-0.0165,0.00578973722527119,-0.0165145070426674));
#12649=CARTESIAN_POINT('',(-0.0165,0.,0.));
#12650=CARTESIAN_POINT('',(-0.016500000125,0.00502298787887017,-0.0167636390075443));
#12651=CARTESIAN_POINT('',(-0.0174999997505,0.00502298787974032,-0.0167636390070886));
#12652=CARTESIAN_POINT('',(-0.0171666665836667,0.00502298787974032,-0.0167636390070886));
#12653=CARTESIAN_POINT('',(-0.0168333334168333,0.00502298787974032,-0.0167636390070886));
#12654=CARTESIAN_POINT('',(-0.01650000025,0.00502298787974032,-0.0167636390070886));
#12655=CARTESIAN_POINT('',(-0.01650000025,0.000403103993638577,-0.0174953567317249));
#12656=CARTESIAN_POINT('',(-0.0168333334168333,0.000403103993638577,-0.0174953567317249));
#12657=CARTESIAN_POINT('',(-0.0171666665836667,0.000403103993638577,-0.0174953567317249));
#12658=CARTESIAN_POINT('',(-0.0174999997505,0.000403103993638577,-0.0174953567317249));
#12659=CARTESIAN_POINT('',(-0.0165,0.000403103988632388,-0.0174953567319128));
#12660=CARTESIAN_POINT('',(-0.0165,0.,0.));
#12661=CARTESIAN_POINT('',(-0.016500000125,-0.000403103984089013,-0.0174953567320176));
#12662=CARTESIAN_POINT('',(-0.0174999997505,-0.000403103980178063,-0.0174953567320351));
#12663=CARTESIAN_POINT('',(-0.0171666665836667,-0.000403103980178063,-0.0174953567320351));
#12664=CARTESIAN_POINT('',(-0.0168333334168333,-0.000403103980178063,-0.0174953567320351));
#12665=CARTESIAN_POINT('',(-0.01650000025,-0.000403103980178063,-0.0174953567320351));
#12666=CARTESIAN_POINT('',(-0.01650000025,-0.00502298788360641,-0.0167636390059302));
#12667=CARTESIAN_POINT('',(-0.0168333334168333,-0.00502298788360641,-0.0167636390059302));
#12668=CARTESIAN_POINT('',(-0.0171666665836667,-0.00502298788360641,-0.0167636390059302));
#12669=CARTESIAN_POINT('',(-0.0174999997505,-0.00502298788360641,-0.0167636390059302));
#12670=CARTESIAN_POINT('',(-0.0165,-0.00502298788281727,-0.0167636390061666));
#12671=CARTESIAN_POINT('',(-0.0165,0.,0.));
#12672=CARTESIAN_POINT('',(-0.016500000125,-0.00578973722926497,-0.0165145070414119));
#12673=CARTESIAN_POINT('',(-0.0174999997505,-0.00578973723052998,-0.0165145070408237));
#12674=CARTESIAN_POINT('',(-0.0171666665836667,-0.00578973723052998,-0.0165145070408237));
#12675=CARTESIAN_POINT('',(-0.0168333334168333,-0.00578973723052998,-0.0165145070408237));
#12676=CARTESIAN_POINT('',(-0.01650000025,-0.00578973723052998,-0.0165145070408237));
#12677=CARTESIAN_POINT('',(-0.01650000025,-0.00995739469320859,-0.0143909794984102));
#12678=CARTESIAN_POINT('',(-0.0168333334168333,-0.00995739469320859,-0.0143909794984102));
#12679=CARTESIAN_POINT('',(-0.0171666665836667,-0.00995739469320859,-0.0143909794984102));
#12680=CARTESIAN_POINT('',(-0.0174999997505,-0.00995739469320859,-0.0143909794984102));
#12681=CARTESIAN_POINT('',(-0.0165,-0.00995739469490315,-0.0143909794969604));
#12682=CARTESIAN_POINT('',(-0.0165,0.,0.));
#12683=CARTESIAN_POINT('',(-0.016500000125,-0.0106096306465377,-0.0139171023400936));
#12684=CARTESIAN_POINT('',(-0.0174999997505,-0.0106096306450755,-0.0139171023411871));
#12685=CARTESIAN_POINT('',(-0.0171666665836667,-0.0106096306450755,-0.0139171023411871));
#12686=CARTESIAN_POINT('',(-0.0168333334168333,-0.0106096306450755,-0.0139171023411871));
#12687=CARTESIAN_POINT('',(-0.01650000025,-0.0106096306450755,-0.0139171023411871));
#12688=CARTESIAN_POINT('',(-0.01650000025,-0.0139171023352004,-0.0106096306529285));
#12689=CARTESIAN_POINT('',(-0.0168333334168333,-0.0139171023352004,-0.0106096306529285));
#12690=CARTESIAN_POINT('',(-0.0171666665836667,-0.0139171023352004,-0.0106096306529285));
#12691=CARTESIAN_POINT('',(-0.0174999997505,-0.0139171023352004,-0.0106096306529285));
#12692=CARTESIAN_POINT('',(-0.0165,-0.0139171023384264,-0.0106096306487246));
#12693=CARTESIAN_POINT('',(-0.0165,0.,0.));
#12694=CARTESIAN_POINT('',(-0.016500000125,-0.0143909795003744,-0.00995739468996904));
#12695=CARTESIAN_POINT('',(-0.0174999997505,-0.0143909795027489,-0.00995739468693804));
#12696=CARTESIAN_POINT('',(-0.0171666665836667,-0.0143909795027489,-0.00995739468693804));
#12697=CARTESIAN_POINT('',(-0.0168333334168333,-0.0143909795027489,-0.00995739468693804));
#12698=CARTESIAN_POINT('',(-0.01650000025,-0.0143909795027489,-0.00995739468693804));
#12699=CARTESIAN_POINT('',(-0.01650000025,-0.0165145070433464,-0.00578973722333416));
#12700=CARTESIAN_POINT('',(-0.0168333334168333,-0.0165145070433464,-0.00578973722333416));
#12701=CARTESIAN_POINT('',(-0.0171666665836667,-0.0165145070433464,-0.00578973722333416));
#12702=CARTESIAN_POINT('',(-0.0174999997505,-0.0165145070433464,-0.00578973722333416));
#12703=CARTESIAN_POINT('',(-0.0165,-0.0165145070432611,-0.00578973722357761));
#12704=CARTESIAN_POINT('',(-0.0165,0.,0.));
#12705=CARTESIAN_POINT('',(-0.016500000125,-0.0167636390080594,-0.00502298787715103));
#12706=CARTESIAN_POINT('',(-0.0174999997505,-0.0167636390081188,-0.00502298787630204));
#12707=CARTESIAN_POINT('',(-0.0171666665836667,-0.0167636390081188,-0.00502298787630204));
#12708=CARTESIAN_POINT('',(-0.0168333334168333,-0.0167636390081188,-0.00502298787630204));
#12709=CARTESIAN_POINT('',(-0.01650000025,-0.0167636390081188,-0.00502298787630204));
#12710=CARTESIAN_POINT('',(-0.018,0.,0.));
#12711=CARTESIAN_POINT('',(-0.018,0.,0.0175));
#12712=CARTESIAN_POINT('',(-0.019981842228,0.,0.));
#12713=CARTESIAN_POINT('',(-0.0165,0.,0.));
#12714=CARTESIAN_POINT('',(-0.017,0.0142662956955,0.005373055884));
#12715=CARTESIAN_POINT('',(-0.0165,0.016514507042,0.005789737228));
#12716=CARTESIAN_POINT('',(-0.0165,0.0150156994776667,0.00551194966533333));
#12717=CARTESIAN_POINT('',(-0.0165,0.0135168919133333,0.00523416210266667));
#12718=CARTESIAN_POINT('',(-0.0165,0.012018084349,0.00495637454));
#12719=CARTESIAN_POINT('',(-0.017,0.0127324117365,0.008383472656));
#12720=CARTESIAN_POINT('',(-0.0165,0.011073843975,0.006809550619));
#12721=CARTESIAN_POINT('',(-0.0165,0.012179555816,0.007858831977));
#12722=CARTESIAN_POINT('',(-0.0165,0.013285267657,0.008908113335));
#12723=CARTESIAN_POINT('',(-0.0165,0.014390979498,0.009957394693));
#12724=CARTESIAN_POINT('',(-0.019981842228,0.,0.));
#12725=CARTESIAN_POINT('',(-0.0165,0.,0.));
#12726=CARTESIAN_POINT('',(-0.017,0.0119076879045,0.00951860762750001));
#12727=CARTESIAN_POINT('',(-0.0165,0.013917102339,0.010609630648));
#12728=CARTESIAN_POINT('',(-0.0165,0.012577492716,0.00988228196766668));
#12729=CARTESIAN_POINT('',(-0.0165,0.011237883093,0.00915493328733334));
#12730=CARTESIAN_POINT('',(-0.0165,0.00989827347,0.00842758460700001));
#12731=CARTESIAN_POINT('',(-0.017,0.00951860762750001,0.0119076879045));
#12732=CARTESIAN_POINT('',(-0.0165,0.00842758460700001,0.00989827347));
#12733=CARTESIAN_POINT('',(-0.0165,0.00915493328724936,0.0112378830928453));
#12734=CARTESIAN_POINT('',(-0.0165,0.00988228196749871,0.0125774927156907));
#12735=CARTESIAN_POINT('',(-0.0165,0.0106096306477481,0.013917102338536));
#12736=CARTESIAN_POINT('',(-0.019981842228,0.,0.));
#12737=CARTESIAN_POINT('',(-0.0165,0.,0.));
#12738=CARTESIAN_POINT('',(-0.017,0.008383472656,0.0127324117365));
#12739=CARTESIAN_POINT('',(-0.0165,0.009957394693,0.014390979498));
#12740=CARTESIAN_POINT('',(-0.0165,0.008908113335,0.013285267657));
#12741=CARTESIAN_POINT('',(-0.0165,0.007858831977,0.012179555816));
#12742=CARTESIAN_POINT('',(-0.0165,0.006809550619,0.011073843975));
#12743=CARTESIAN_POINT('',(-0.017,0.005373055884,0.0142662956955));
#12744=CARTESIAN_POINT('',(-0.0165,0.00495637454,0.012018084349));
#12745=CARTESIAN_POINT('',(-0.0165,0.00523416210266667,0.0135168919133333));
#12746=CARTESIAN_POINT('',(-0.0165,0.00551194966533333,0.0150156994776667));
#12747=CARTESIAN_POINT('',(-0.0165,0.005789737228,0.016514507042));
#12748=CARTESIAN_POINT('',(-0.019981842228,0.,0.));
#12749=CARTESIAN_POINT('',(-0.0165,0.,0.));
#12750=CARTESIAN_POINT('',(-0.017,0.004038624693,0.014699878673));
#12751=CARTESIAN_POINT('',(-0.0165,0.005022987878,0.016763639008));
#12752=CARTESIAN_POINT('',(-0.0165,0.00436674575466666,0.0153877987846667));
#12753=CARTESIAN_POINT('',(-0.0165,0.00371050363133333,0.0140119585613333));
#12754=CARTESIAN_POINT('',(-0.0165,0.003054261508,0.012636118338));
#12755=CARTESIAN_POINT('',(-0.017,0.000701551994,0.0152284190645));
#12756=CARTESIAN_POINT('',(-0.0165,0.001,0.012961481397));
#12757=CARTESIAN_POINT('',(-0.0165,0.000801034662678128,0.0144727731752463));
#12758=CARTESIAN_POINT('',(-0.0165,0.000602069325356256,0.0159840649534926));
#12759=CARTESIAN_POINT('',(-0.0165,0.000403103988034383,0.0174953567317388));
#12760=CARTESIAN_POINT('',(-0.019981842228,0.,0.));
#12761=CARTESIAN_POINT('',(-0.0165,0.,0.));
#12762=CARTESIAN_POINT('',(-0.017,-0.000701551994,0.0152284190645));
#12763=CARTESIAN_POINT('',(-0.0165,-0.000403103988,0.017495356732));
#12764=CARTESIAN_POINT('',(-0.0165,-0.000602069325333334,0.0159840649536667));
#12765=CARTESIAN_POINT('',(-0.0165,-0.000801034662666668,0.0144727731753333));
#12766=CARTESIAN_POINT('',(-0.0165,-0.001,0.012961481397));
#12767=CARTESIAN_POINT('',(-0.017,-0.004038624693,0.014699878673));
#12768=CARTESIAN_POINT('',(-0.0165,-0.003054261508,0.012636118338));
#12769=CARTESIAN_POINT('',(-0.0165,-0.00371050363121451,0.0140119585610842));
#12770=CARTESIAN_POINT('',(-0.0165,-0.00436674575442903,0.0153877987841684));
#12771=CARTESIAN_POINT('',(-0.0165,-0.00502298787764354,0.0167636390072527));
#12772=CARTESIAN_POINT('',(-0.019981842228,0.,0.));
#12773=CARTESIAN_POINT('',(-0.0165,0.,0.));
#12774=CARTESIAN_POINT('',(-0.017,-0.005373055884,0.0142662956955));
#12775=CARTESIAN_POINT('',(-0.0165,-0.005789737228,0.016514507042));
#12776=CARTESIAN_POINT('',(-0.0165,-0.00551194966533333,0.0150156994776667));
#12777=CARTESIAN_POINT('',(-0.0165,-0.00523416210266667,0.0135168919133333));
#12778=CARTESIAN_POINT('',(-0.0165,-0.00495637454,0.012018084349));
#12779=CARTESIAN_POINT('',(-0.017,-0.008383472656,0.0127324117365));
#12780=CARTESIAN_POINT('',(-0.0165,-0.006809550619,0.011073843975));
#12781=CARTESIAN_POINT('',(-0.0165,-0.007858831977,0.012179555816));
#12782=CARTESIAN_POINT('',(-0.0165,-0.008908113335,0.013285267657));
#12783=CARTESIAN_POINT('',(-0.0165,-0.009957394693,0.014390979498));
#12784=CARTESIAN_POINT('',(-0.019981842228,0.,0.));
#12785=CARTESIAN_POINT('',(-0.0165,0.,0.));
#12786=CARTESIAN_POINT('',(-0.017,-0.00951860762750001,0.0119076879045));
#12787=CARTESIAN_POINT('',(-0.0165,-0.010609630648,0.013917102339));
#12788=CARTESIAN_POINT('',(-0.0165,-0.00988228196766668,0.012577492716));
#12789=CARTESIAN_POINT('',(-0.0165,-0.00915493328733334,0.011237883093));
#12790=CARTESIAN_POINT('',(-0.0165,-0.00842758460700001,0.00989827347));
#12791=CARTESIAN_POINT('',(-0.017,-0.0119076879045,0.00951860762750001));
#12792=CARTESIAN_POINT('',(-0.0165,-0.00989827347,0.00842758460700001));
#12793=CARTESIAN_POINT('',(-0.0165,-0.0112378830929259,0.00915493328729313));
#12794=CARTESIAN_POINT('',(-0.0165,-0.0125774927158519,0.00988228196758625));
#12795=CARTESIAN_POINT('',(-0.0165,-0.0139171023387778,0.0106096306478794));
#12796=CARTESIAN_POINT('',(-0.019981842228,0.,0.));
#12797=CARTESIAN_POINT('',(-0.0165,0.,0.));
#12798=CARTESIAN_POINT('',(-0.017,-0.0127324117365,0.008383472656));
#12799=CARTESIAN_POINT('',(-0.0165,-0.014390979498,0.009957394693));
#12800=CARTESIAN_POINT('',(-0.0165,-0.013285267657,0.008908113335));
#12801=CARTESIAN_POINT('',(-0.0165,-0.012179555816,0.007858831977));
#12802=CARTESIAN_POINT('',(-0.0165,-0.011073843975,0.006809550619));
#12803=CARTESIAN_POINT('',(-0.017,-0.0142662956955,0.005373055884));
#12804=CARTESIAN_POINT('',(-0.0165,-0.012018084349,0.00495637454));
#12805=CARTESIAN_POINT('',(-0.0165,-0.0135168919133333,0.00523416210266667));
#12806=CARTESIAN_POINT('',(-0.0165,-0.0150156994776667,0.00551194966533333));
#12807=CARTESIAN_POINT('',(-0.0165,-0.016514507042,0.005789737228));
#12808=CARTESIAN_POINT('',(-0.019981842228,0.,0.));
#12809=CARTESIAN_POINT('',(-0.0165,0.,0.));
#12810=CARTESIAN_POINT('',(-0.017,-0.014699878673,0.004038624693));
#12811=CARTESIAN_POINT('',(-0.0165,-0.016763639008,0.005022987878));
#12812=CARTESIAN_POINT('',(-0.0165,-0.0153877987846667,0.00436674575466666));
#12813=CARTESIAN_POINT('',(-0.0165,-0.0140119585613333,0.00371050363133333));
#12814=CARTESIAN_POINT('',(-0.0165,-0.012636118338,0.003054261508));
#12815=CARTESIAN_POINT('',(-0.017,-0.0152284190645,0.000701551994));
#12816=CARTESIAN_POINT('',(-0.0165,-0.012961481397,0.001));
#12817=CARTESIAN_POINT('',(-0.0165,-0.0144727731753372,0.000801034662666156));
#12818=CARTESIAN_POINT('',(-0.0165,-0.0159840649536667,0.000602069325333334));
#12819=CARTESIAN_POINT('',(-0.0165,-0.017495356732,0.000403103988));
#12820=CARTESIAN_POINT('',(-0.019981842228,0.,0.));
#12821=CARTESIAN_POINT('',(-0.0165,0.,0.));
#12822=CARTESIAN_POINT('',(-0.017,-0.0152284190645,-0.000701551994));
#12823=CARTESIAN_POINT('',(-0.0165,-0.0174953567319272,-0.000403103988009584));
#12824=CARTESIAN_POINT('',(-0.0165,-0.0159840649536181,-0.000602069325339723));
#12825=CARTESIAN_POINT('',(-0.0165,-0.0144727731753091,-0.000801034662669862));
#12826=CARTESIAN_POINT('',(-0.0165,-0.012961481397,-0.001));
#12827=CARTESIAN_POINT('',(-0.017,-0.014699878673,-0.004038624693));
#12828=CARTESIAN_POINT('',(-0.0165,-0.012636118338,-0.003054261508));
#12829=CARTESIAN_POINT('',(-0.0165,-0.0140119585612395,-0.00371050363128858));
#12830=CARTESIAN_POINT('',(-0.0165,-0.015387798784479,-0.00436674575457716));
#12831=CARTESIAN_POINT('',(-0.0165,-0.0167636390077185,-0.00502298787786573));
#12832=CARTESIAN_POINT('',(-0.019981842228,0.,0.));
#12833=CARTESIAN_POINT('',(-0.0165,0.,0.));
#12834=CARTESIAN_POINT('',(-0.017,-0.0142662956955,-0.005373055884));
#12835=CARTESIAN_POINT('',(-0.0165,-0.016514507042,-0.005789737228));
#12836=CARTESIAN_POINT('',(-0.0165,-0.0150156994776667,-0.00551194966533333));
#12837=CARTESIAN_POINT('',(-0.0165,-0.0135168919133333,-0.00523416210266667));
#12838=CARTESIAN_POINT('',(-0.0165,-0.012018084349,-0.00495637454));
#12839=CARTESIAN_POINT('',(-0.017,-0.0127324117365,-0.008383472656));
#12840=CARTESIAN_POINT('',(-0.0165,-0.011073843975,-0.006809550619));
#12841=CARTESIAN_POINT('',(-0.0165,-0.012179555815912,-0.00785883197691647));
#12842=CARTESIAN_POINT('',(-0.0165,-0.013285267656824,-0.00890811333483294));
#12843=CARTESIAN_POINT('',(-0.0165,-0.0143909794977359,-0.00995739469274941));
#12844=CARTESIAN_POINT('',(-0.019981842228,0.,0.));
#12845=CARTESIAN_POINT('',(-0.0165,0.,0.));
#12846=CARTESIAN_POINT('',(-0.017,-0.0119076879045,-0.00951860762750001));
#12847=CARTESIAN_POINT('',(-0.0165,-0.013917102339,-0.010609630648));
#12848=CARTESIAN_POINT('',(-0.0165,-0.012577492716,-0.00988228196766668));
#12849=CARTESIAN_POINT('',(-0.0165,-0.011237883093,-0.00915493328733334));
#12850=CARTESIAN_POINT('',(-0.0165,-0.00989827347,-0.00842758460700001));
#12851=CARTESIAN_POINT('',(-0.017,-0.00951860762750001,-0.0119076879045));
#12852=CARTESIAN_POINT('',(-0.0165,-0.00842758460700001,-0.00989827347));
#12853=CARTESIAN_POINT('',(-0.0165,-0.00915493328733334,-0.011237883093));
#12854=CARTESIAN_POINT('',(-0.0165,-0.00988228196766667,-0.012577492716));
#12855=CARTESIAN_POINT('',(-0.0165,-0.010609630648,-0.013917102339));
#12856=CARTESIAN_POINT('',(-0.019981842228,0.,0.));
#12857=CARTESIAN_POINT('',(-0.0165,0.,0.));
#12858=CARTESIAN_POINT('',(-0.017,-0.008383472656,-0.0127324117365));
#12859=CARTESIAN_POINT('',(-0.0165,-0.009957394693,-0.014390979498));
#12860=CARTESIAN_POINT('',(-0.0165,-0.008908113335,-0.013285267657));
#12861=CARTESIAN_POINT('',(-0.0165,-0.007858831977,-0.012179555816));
#12862=CARTESIAN_POINT('',(-0.0165,-0.006809550619,-0.011073843975));
#12863=CARTESIAN_POINT('',(-0.017,-0.005373055884,-0.0142662956955));
#12864=CARTESIAN_POINT('',(-0.0165,-0.00495637454,-0.012018084349));
#12865=CARTESIAN_POINT('',(-0.0165,-0.00523416210264554,-0.0135168919132194));
#12866=CARTESIAN_POINT('',(-0.0165,-0.00551194966529108,-0.0150156994774387));
#12867=CARTESIAN_POINT('',(-0.0165,-0.00578973722793662,-0.016514507041658));
#12868=CARTESIAN_POINT('',(-0.019981842228,0.,0.));
#12869=CARTESIAN_POINT('',(-0.0165,0.,0.));
#12870=CARTESIAN_POINT('',(-0.017,-0.004038624693,-0.014699878673));
#12871=CARTESIAN_POINT('',(-0.0165,-0.005022987878,-0.016763639008));
#12872=CARTESIAN_POINT('',(-0.0165,-0.00436674575466666,-0.0153877987846667));
#12873=CARTESIAN_POINT('',(-0.0165,-0.00371050363133333,-0.0140119585613333));
#12874=CARTESIAN_POINT('',(-0.0165,-0.003054261508,-0.012636118338));
#12875=CARTESIAN_POINT('',(-0.017,-0.000701551994,-0.0152284190645));
#12876=CARTESIAN_POINT('',(-0.0165,-0.001,-0.012961481397));
#12877=CARTESIAN_POINT('',(-0.0165,-0.000801034662666668,-0.0144727731753333));
#12878=CARTESIAN_POINT('',(-0.0165,-0.000602069325333334,-0.0159840649536667));
#12879=CARTESIAN_POINT('',(-0.0165,-0.000403103988,-0.017495356732));
#12880=CARTESIAN_POINT('',(-0.019981842228,0.,0.));
#12881=CARTESIAN_POINT('',(-0.0165,0.,0.));
#12882=CARTESIAN_POINT('',(-0.017,0.000701551994,-0.0152284190645));
#12883=CARTESIAN_POINT('',(-0.0165,0.000403103988,-0.017495356732));
#12884=CARTESIAN_POINT('',(-0.0165,0.000602069325333334,-0.0159840649536667));
#12885=CARTESIAN_POINT('',(-0.0165,0.000801034662666668,-0.0144727731753333));
#12886=CARTESIAN_POINT('',(-0.0165,0.001,-0.012961481397));
#12887=CARTESIAN_POINT('',(-0.017,0.004038624693,-0.014699878673));
#12888=CARTESIAN_POINT('',(-0.0165,0.003054261508,-0.012636118338));
#12889=CARTESIAN_POINT('',(-0.0165,0.00371050363132807,-0.0140119585613223));
#12890=CARTESIAN_POINT('',(-0.0165,0.00436674575466666,-0.0153877987846667));
#12891=CARTESIAN_POINT('',(-0.0165,0.005022987878,-0.016763639008));
#12892=CARTESIAN_POINT('',(-0.019981842228,0.,0.));
#12893=CARTESIAN_POINT('',(-0.0165,0.,0.));
#12894=CARTESIAN_POINT('',(-0.017,0.005373055884,-0.0142662956955));
#12895=CARTESIAN_POINT('',(-0.0165,0.005789737228,-0.016514507042));
#12896=CARTESIAN_POINT('',(-0.0165,0.00551194966533333,-0.0150156994776667));
#12897=CARTESIAN_POINT('',(-0.0165,0.00523416210266667,-0.0135168919133333));
#12898=CARTESIAN_POINT('',(-0.0165,0.00495637454,-0.012018084349));
#12899=CARTESIAN_POINT('',(-0.017,0.008383472656,-0.0127324117365));
#12900=CARTESIAN_POINT('',(-0.0165,0.006809550619,-0.011073843975));
#12901=CARTESIAN_POINT('',(-0.0165,0.00785883197697961,-0.0121795558159785));
#12902=CARTESIAN_POINT('',(-0.0165,0.00890811333495922,-0.013285267656957));
#12903=CARTESIAN_POINT('',(-0.0165,0.00995739469293883,-0.0143909794979355));
#12904=CARTESIAN_POINT('',(-0.019981842228,0.,0.));
#12905=CARTESIAN_POINT('',(-0.0165,0.,0.));
#12906=CARTESIAN_POINT('',(-0.017,0.00951860762750001,-0.0119076879045));
#12907=CARTESIAN_POINT('',(-0.0165,0.010609630648,-0.013917102339));
#12908=CARTESIAN_POINT('',(-0.0165,0.00988228196766668,-0.012577492716));
#12909=CARTESIAN_POINT('',(-0.0165,0.00915493328733334,-0.011237883093));
#12910=CARTESIAN_POINT('',(-0.0165,0.00842758460700001,-0.00989827347));
#12911=CARTESIAN_POINT('',(-0.017,0.0119076879045,-0.00951860762750001));
#12912=CARTESIAN_POINT('',(-0.0165,0.00989827347,-0.00842758460700001));
#12913=CARTESIAN_POINT('',(-0.0165,0.011237883093,-0.00915493328733334));
#12914=CARTESIAN_POINT('',(-0.0165,0.012577492716,-0.00988228196766667));
#12915=CARTESIAN_POINT('',(-0.0165,0.013917102339,-0.010609630648));
#12916=CARTESIAN_POINT('',(-0.019981842228,0.,0.));
#12917=CARTESIAN_POINT('',(-0.0165,0.,0.));
#12918=CARTESIAN_POINT('',(-0.017,0.0127324117365,-0.008383472656));
#12919=CARTESIAN_POINT('',(-0.0165,0.014390979498,-0.009957394693));
#12920=CARTESIAN_POINT('',(-0.0165,0.013285267657,-0.008908113335));
#12921=CARTESIAN_POINT('',(-0.0165,0.012179555816,-0.007858831977));
#12922=CARTESIAN_POINT('',(-0.0165,0.011073843975,-0.006809550619));
#12923=CARTESIAN_POINT('',(-0.017,0.0142662956955,-0.005373055884));
#12924=CARTESIAN_POINT('',(-0.0165,0.012018084349,-0.00495637454));
#12925=CARTESIAN_POINT('',(-0.0165,0.0135168919133095,-0.00523416210266226));
#12926=CARTESIAN_POINT('',(-0.0165,0.0150156994776191,-0.00551194966532451));
#12927=CARTESIAN_POINT('',(-0.0165,0.0165145070419286,-0.00578973722798677));
#12928=CARTESIAN_POINT('',(-0.019981842228,0.,0.));
#12929=CARTESIAN_POINT('',(-0.0165,0.,0.));
#12930=CARTESIAN_POINT('',(-0.017,0.014699878673,-0.004038624693));
#12931=CARTESIAN_POINT('',(-0.0165,0.016763639008,-0.005022987878));
#12932=CARTESIAN_POINT('',(-0.0165,0.0153877987846667,-0.00436674575466666));
#12933=CARTESIAN_POINT('',(-0.0165,0.0140119585613333,-0.00371050363133333));
#12934=CARTESIAN_POINT('',(-0.0165,0.012636118338,-0.003054261508));
#12935=CARTESIAN_POINT('',(-0.017,0.0152284190645,-0.000701551994));
#12936=CARTESIAN_POINT('',(-0.0165,0.012961481397,-0.001));
#12937=CARTESIAN_POINT('',(-0.0165,0.0144727731751553,-0.000801034662690101));
#12938=CARTESIAN_POINT('',(-0.0165,0.0159840649533107,-0.000602069325380202));
#12939=CARTESIAN_POINT('',(-0.0165,0.017495356731466,-0.000403103988070302));
#12940=CARTESIAN_POINT('',(-0.034017463007,0.,0.));
#12941=CARTESIAN_POINT('',(-0.021,0.,0.));
#12942=CARTESIAN_POINT('',(-0.021,0.,0.0175));
#12943=CARTESIAN_POINT('',(-0.0165,0.0152307406985,-2.60208521396521E-20));
#12944=CARTESIAN_POINT('',(-0.0165,0.0143908616785,0.0044219993675));
#12945=CARTESIAN_POINT('',(-0.018,0.,-3.07046055247895E-18));
#12946=CARTESIAN_POINT('',(-0.018,0.,0.));
#12947=CARTESIAN_POINT('',(-0.018,0.,0.0165));
#12948=CARTESIAN_POINT('',(-0.0165,-0.0152307406985,-2.60208521396521E-20));
#12949=CARTESIAN_POINT('',(-0.0165,-0.0143908616785,0.0044219993675));
#12950=CARTESIAN_POINT('',(-0.0165,-0.012144626484,0.00870959063300001));
#12951=CARTESIAN_POINT('',(-0.0165,-0.00870959063300002,0.012144626484));
#12952=CARTESIAN_POINT('',(-0.0165,-0.0044219993675,0.0143908616785));
#12953=CARTESIAN_POINT('',(-0.0165,-1.74556549770166E-19,0.0152330629486464));
#12954=CARTESIAN_POINT('',(-0.0165,0.0044219993675,0.0143908616785));
#12955=CARTESIAN_POINT('',(-0.0165,0.00870959063300002,0.012144626484));
#12956=CARTESIAN_POINT('',(-0.0165,0.012144626484,0.00870959063300001));
#12957=CARTESIAN_POINT('',(-0.0165,0.0143908616785,-0.0044219993675));
#12958=CARTESIAN_POINT('',(-0.0165,0.012144626484,-0.00870959063300003));
#12959=CARTESIAN_POINT('',(-0.0165,0.00870959063300002,-0.012144626484));
#12960=CARTESIAN_POINT('',(-0.0165,0.0044219993675,-0.0143908616785));
#12961=CARTESIAN_POINT('',(-0.0165,-1.74556549770166E-19,-0.0152330629486464));
#12962=CARTESIAN_POINT('',(-0.0165,-0.0044219993675,-0.0143908616785));
#12963=CARTESIAN_POINT('',(-0.0165,-0.00870959063300002,-0.012144626484));
#12964=CARTESIAN_POINT('',(-0.0165,-0.012144626484,-0.00870959063300003));
#12965=CARTESIAN_POINT('',(-0.0165,-0.0143908616785,-0.0044219993675));
#12966=CARTESIAN_POINT('',(-0.021,0.,-3.07046055247895E-18));
#12967=CARTESIAN_POINT('',(-0.021,0.,0.));
#12968=CARTESIAN_POINT('',(-0.021,0.,0.0165));
#12969=CARTESIAN_POINT('',(-0.034017463007,0.,0.));
#18809=MECHANICAL_DESIGN_GEOMETRIC_PRESENTATION_REPRESENTATION('',(#8174),#18810);
#18810=(
GEOMETRIC_REPRESENTATION_CONTEXT(3)
GLOBAL_UNCERTAINTY_ASSIGNED_CONTEXT((#18817))
GLOBAL_UNIT_ASSIGNED_CONTEXT((#18826,#18825,#18824))
REPRESENTATION_CONTEXT('MAS-697','TOP_LEVEL_ASSEMBLY_PART')
);
#18811=(
GEOMETRIC_REPRESENTATION_CONTEXT(3)
GLOBAL_UNCERTAINTY_ASSIGNED_CONTEXT((#18818))
GLOBAL_UNIT_ASSIGNED_CONTEXT((#18826,#18825,#18824))
REPRESENTATION_CONTEXT('cassette body__ DE    15749','COMPONENT_PART')
);
#18817=UNCERTAINTY_MEASURE_WITH_UNIT(LENGTH_MEASURE(1.E-8),#18826,
'DISTANCE_ACCURACY_VALUE','Maximum Tolerance applied to model');
#18818=UNCERTAINTY_MEASURE_WITH_UNIT(LENGTH_MEASURE(2.E-5),#18826,
'DISTANCE_ACCURACY_VALUE','Maximum Tolerance applied to model');
#18824=(
NAMED_UNIT(*)
SI_UNIT($,.STERADIAN.)
SOLID_ANGLE_UNIT()
);
#18825=(
NAMED_UNIT(*)
PLANE_ANGLE_UNIT()
SI_UNIT($,.RADIAN.)
);
#18826=(
LENGTH_UNIT()
NAMED_UNIT(*)
SI_UNIT($,.METRE.)
);
#18828=PRODUCT_DEFINITION_SHAPE('','',#18841);
#18841=PRODUCT_DEFINITION('','',#18855,#18848);
#18848=PRODUCT_DEFINITION_CONTEXT('',#18890,'design');
#18855=PRODUCT_DEFINITION_FORMATION_WITH_SPECIFIED_SOURCE('','',#18869,
 .NOT_KNOWN.);
#18869=PRODUCT('cassette body__ DE    15749',
'cassette body__ DE    15749','cassette body__ DE    15749',(#18883));
#18883=PRODUCT_CONTEXT('',#18890,'mechanical');
#18890=APPLICATION_CONTEXT('managed model based 3d engineering');
ENDSEC;
END-ISO-10303-21;
